ISO-10303-21;
HEADER;
FILE_DESCRIPTION (('STEP AP203'),
    '1' );
FILE_NAME ('Part5_knurlingConnector.step',
    '2026-10-06T15:07:10',
    ( '' ),
    ( '' ),
    'SwSTEP 2.0',
    'SolidWorks 2024',
    '' );
FILE_SCHEMA (( 'AUTOMOTIVE_DESIGN' ));
ENDSEC;

DATA;
#6=EDGE_CURVE ( 'NONE', #31023, #30399, #20030, .T. ) ;
#8=AXIS2_PLACEMENT_3D ( 'NONE', #3231, #13394, #23612 ) ;
#13=SHAPE_REPRESENTATION ( 'Part5_knurlingConnector', ( #2865 ), #13509 ) ;
#15=ORIENTED_EDGE ( 'NONE', *, *, #21559, .T. ) ;
#21=CARTESIAN_POINT ( 'NONE',  ( 10.57125986779756843, 4.681538312723516171, 0.8254815157535410064 ) ) ;
#22=DIRECTION ( 'NONE',  ( 0.000000000000000000, 1.000000000000000000, 0.000000000000000000 ) ) ;
#23=EDGE_CURVE ( 'NONE', #10880, #2577, #7296, .T. ) ;
#27=ORIENTED_EDGE ( 'NONE', *, *, #10830, .T. ) ;
#38=DIRECTION ( 'NONE',  ( 1.000000000000000000, -8.574039729943018344E-17, -0.000000000000000000 ) ) ;
#39=CARTESIAN_POINT ( 'NONE',  ( 23.86000000273118715, -1.942864903642428587, -1.573300977624592756 ) ) ;
#51=DIRECTION ( 'NONE',  ( 6.062761635205658338E-17, 0.7071067811865558994, -0.7071067811865391350 ) ) ;
#61=VERTEX_POINT ( 'NONE', #14078 ) ;
#75=CARTESIAN_POINT ( 'NONE',  ( 10.57125986779756843, -1.115095498423343878, 4.884328206559833241 ) ) ;
#90=EDGE_CURVE ( 'NONE', #31165, #31196, #18949, .T. ) ;
#93=CARTESIAN_POINT ( 'NONE',  ( 9.999999999999998224, -4.753758587302148619, -3.462581523170091167E-33 ) ) ;
#97=VECTOR ( 'NONE', #5631, 999.9999999999998863 ) ;
#114=LINE ( 'NONE', #298, #18162 ) ;
#115=VERTEX_POINT ( 'NONE', #32150 ) ;
#119=VECTOR ( 'NONE', #15199, 1000.000000000000114 ) ;
#122=VECTOR ( 'NONE', #10002, 1000.000000000000000 ) ;
#130=EDGE_CURVE ( 'NONE', #2062, #25766, #16915, .T. ) ;
#132=CIRCLE ( 'NONE', #12926, 5.009999999999999787 ) ;
#149=ORIENTED_EDGE ( 'NONE', *, *, #3090, .F. ) ;
#150=CARTESIAN_POINT ( 'NONE',  ( -4.187842409712542721E-16, -4.884328206559843011, 1.115095498423292142 ) ) ;
#159=CARTESIAN_POINT ( 'NONE',  ( 10.00000000000000000, 2.718385644597173023, 4.208382051008202396 ) ) ;
#164=VECTOR ( 'NONE', #17000, 1000.000000000000114 ) ;
#168=CARTESIAN_POINT ( 'NONE',  ( 24.73500000136559507, 3.156283516753366047, 0.9349337715887203748 ) ) ;
#171=EDGE_CURVE ( 'NONE', #23760, #9712, #9390, .T. ) ;
#180=ORIENTED_EDGE ( 'NONE', *, *, #13228, .F. ) ;
#182=EDGE_LOOP ( 'NONE', ( #4676, #19441, #6640, #3021 ) ) ;
#188=CARTESIAN_POINT ( 'NONE',  ( 23.67250000136559507, 3.024605502323846729, -0.3178988483021056854 ) ) ;
#207=DIRECTION ( 'NONE',  ( -1.000000000000000000, 8.574039729943018344E-17, -0.000000000000000000 ) ) ;
#208=ORIENTED_EDGE ( 'NONE', *, *, #25908, .T. ) ;
#215=DIRECTION ( 'NONE',  ( 7.023442172597920956E-17, 0.8191520442889983489, -0.5735764363510366115 ) ) ;
#217=CARTESIAN_POINT ( 'NONE',  ( 22.29750000273118715, 2.594547506269380133, 0.7685399846772031918 ) ) ;
#219=VECTOR ( 'NONE', #6570, 1000.000000000000000 ) ;
#221=DIRECTION ( 'NONE',  ( 3.623545766764223251E-17, 0.4226182617407006070, -0.9063077870366493816 ) ) ;
#223=CARTESIAN_POINT ( 'NONE',  ( 24.11000000136559862, -3.156283516753370044, -0.9349337715887220401 ) ) ;
#228=VERTEX_POINT ( 'NONE', #15742 ) ;
#233=CARTESIAN_POINT ( 'NONE',  ( 22.67250000136559507, 2.363507492473148286, 1.913930629741525058 ) ) ;
#239=ORIENTED_EDGE ( 'NONE', *, *, #30794, .T. ) ;
#247=CARTESIAN_POINT ( 'NONE',  ( 10.57125986779756843, 0.8254815157535864145, -4.681538312723508177 ) ) ;
#252=LINE ( 'NONE', #7401, #30475 ) ;
#258=DIRECTION ( 'NONE',  ( 0.000000000000000000, 0.000000000000000000, -1.000000000000000000 ) ) ;
#263=ORIENTED_EDGE ( 'NONE', *, *, #4868, .T. ) ;
#264=VERTEX_POINT ( 'NONE', #28449 ) ;
#266=DIRECTION ( 'NONE',  ( 0.000000000000000000, 0.000000000000000000, -1.000000000000000000 ) ) ;
#270=VECTOR ( 'NONE', #15790, 999.9999999999998863 ) ;
#272=PLANE ( 'NONE',  #12904 ) ;
#285=VERTEX_POINT ( 'NONE', #15558 ) ;
#296=ORIENTED_EDGE ( 'NONE', *, *, #10528, .F. ) ;
#298=CARTESIAN_POINT ( 'NONE',  ( 1.394036994807660394E-16, 1.625881193364758337, -4.467071865485455540 ) ) ;
#311=CARTESIAN_POINT ( 'NONE',  ( 2.330754651808292648E-16, 2.718385644597173467, 4.208382051008202396 ) ) ;
#316=EDGE_LOOP ( 'NONE', ( #2684, #263, #10060, #23233 ) ) ;
#329=CARTESIAN_POINT ( 'NONE',  ( 2.619932554246601438E-16, 3.055657119358849982, -3.641590349731898879 ) ) ;
#336=DIRECTION ( 'NONE',  ( 8.574039729943018344E-17, 1.000000000000000000, 0.000000000000000000 ) ) ;
#340=CARTESIAN_POINT ( 'NONE',  ( 0.000000000000000000, 0.000000000000000000, 0.000000000000000000 ) ) ;
#344=CARTESIAN_POINT ( 'NONE',  ( 25.75999999999999801, 2.805042440084548172, 1.132414195126726364 ) ) ;
#347=CARTESIAN_POINT ( 'NONE',  ( 22.48500000136559507, 0.9349337715887185984, -3.156283516753368268 ) ) ;
#350=CARTESIAN_POINT ( 'NONE',  ( 3.122314033877900197E-16, 3.641590349731971710, -3.055657119358763829 ) ) ;
#356=ORIENTED_EDGE ( 'NONE', *, *, #4582, .F. ) ;
#361=ORIENTED_EDGE ( 'NONE', *, *, #14296, .F. ) ;
#366=CARTESIAN_POINT ( 'NONE',  ( 26.11000000000000298, 1.942864903642424146, 1.573300977624592534 ) ) ;
#374=CARTESIAN_POINT ( 'NONE',  ( 25.67250000136559507, 2.363507492473148286, 1.913930629741525058 ) ) ;
#377=ORIENTED_EDGE ( 'NONE', *, *, #23581, .T. ) ;
#380=CARTESIAN_POINT ( 'NONE',  ( 22.04750000136559507, -3.024605502323851169, 0.3178988483021052969 ) ) ;
#381=EDGE_CURVE ( 'NONE', #25477, #26129, #24703, .T. ) ;
#390=DIRECTION ( 'NONE',  ( 0.5000000000000002220, 0.09052430460833657544, 0.8612812260087741034 ) ) ;
#397=ORIENTED_EDGE ( 'NONE', *, *, #19596, .F. ) ;
#402=ORIENTED_EDGE ( 'NONE', *, *, #26636, .T. ) ;
#417=DIRECTION ( 'NONE',  ( -1.000000000000000000, 8.574039729943018344E-17, -0.000000000000000000 ) ) ;
#418=LINE ( 'NONE', #30860, #2758 ) ;
#426=CARTESIAN_POINT ( 'NONE',  ( 25.36241694306878358, -2.409633728563083999, 1.062054624121506530 ) ) ;
#431=EDGE_CURVE ( 'NONE', #18549, #32842, #2321, .T. ) ;
#432=ORIENTED_EDGE ( 'NONE', *, *, #6249, .F. ) ;
#444=CARTESIAN_POINT ( 'NONE',  ( 10.52034268205830259, 3.641590349731929077, 3.055657119358814011 ) ) ;
#456=LINE ( 'NONE', #31055, #2820 ) ;
#457=DESIGN_CONTEXT ( 'detailed design', #29768, 'design' ) ;
#488=CARTESIAN_POINT ( 'NONE',  ( 10.00000000000000178, -8.574039729943018837E-16, 0.000000000000000000 ) ) ;
#497=ORIENTED_EDGE ( 'NONE', *, *, #9027, .F. ) ;
#502=VERTEX_POINT ( 'NONE', #30290 ) ;
#505=ORIENTED_EDGE ( 'NONE', *, *, #30275, .T. ) ;
#510=DIRECTION ( 'NONE',  ( -7.023442172597817418E-17, -0.8191520442889873577, -0.5735764363510524877 ) ) ;
#512=CARTESIAN_POINT ( 'NONE',  ( 25.60999999999999943, -1.942864903642428587, -1.573300977624592756 ) ) ;
#528=CARTESIAN_POINT ( 'NONE',  ( 25.23500000273118715, 2.486304738420679783, -0.2613211581691337604 ) ) ;
#543=ORIENTED_EDGE ( 'NONE', *, *, #5001, .T. ) ;
#545=VERTEX_POINT ( 'NONE', #10382 ) ;
#550=CYLINDRICAL_SURFACE ( 'NONE', #17716, 5.010000000000000675 ) ;
#561=DIRECTION ( 'NONE',  ( -2.219124775574906615E-17, -0.2588190451025184080, -0.9659258262890689783 ) ) ;
#568=EDGE_CURVE ( 'NONE', #31503, #15557, #22908, .T. ) ;
#580=CARTESIAN_POINT ( 'NONE',  ( 22.54750000136559507, 1.913930629741522838, -2.363507492473150062 ) ) ;
#581=AXIS2_PLACEMENT_3D ( 'NONE', #10709, #10896, #26590 ) ;
#585=ORIENTED_EDGE ( 'NONE', *, *, #31853, .T. ) ;
#587=EDGE_CURVE ( 'NONE', #19482, #31424, #9790, .T. ) ;
#588=AXIS2_PLACEMENT_3D ( 'NONE', #14724, #17049, #17552 ) ;
#589=ORIENTED_EDGE ( 'NONE', *, *, #4285, .T. ) ;
#592=CARTESIAN_POINT ( 'NONE',  ( 22.80656763371926843, 0.8852964313267434049, -2.499999999999998224 ) ) ;
#595=CARTESIAN_POINT ( 'NONE',  ( 24.98500000136559507, -2.892927487894331406, 1.570731468192932523 ) ) ;
#603=VECTOR ( 'NONE', #13281, 999.9999999999998863 ) ;
#607=ORIENTED_EDGE ( 'NONE', *, *, #23916, .F. ) ;
#622=CIRCLE ( 'NONE', #17698, 5.010000000000000675 ) ;
#624=AXIS2_PLACEMENT_3D ( 'NONE', #18416, #31291, #8364 ) ;
#634=( BOUNDED_CURVE ( )  B_SPLINE_CURVE ( 2, ( #16762, #19452, #22119, #14577, #26963, #32332, #9391, #29801, #17064, #15388, #15560 ),
 .UNSPECIFIED., .F., .F. ) 
 B_SPLINE_CURVE_WITH_KNOTS ( ( 3, 2, 2, 2, 2, 3 ),
 ( 0.6966116191895003196, 0.6999999999999999556, 0.7249999999999999778, 0.7500000000000000000, 0.7750000000000000222, 0.7966116191895004084 ),
 .UNSPECIFIED. ) 
 CURVE ( )  GEOMETRIC_REPRESENTATION_ITEM ( )  RATIONAL_B_SPLINE_CURVE ( ( 0.9821626249036858880, 0.9896829947469992783, 1.000000000000000000, 0.9238795325112867385, 1.000000000000000000, 0.9238795325112867385, 1.000000000000000000, 0.9238795325112867385, 1.000000000000000000, 0.9341965377642874602, 0.9821626249036858880 ) ) 
 REPRESENTATION_ITEM ( '' )  );
#649=CARTESIAN_POINT ( 'NONE',  ( 22.50111451137534502, -3.256483526998273983E-15, 2.499999999999998668 ) ) ;
#651=VECTOR ( 'NONE', #390, 1000.000000000000000 ) ;
#654=VECTOR ( 'NONE', #21945, 1000.000000000000000 ) ;
#659=ORIENTED_EDGE ( 'NONE', *, *, #8107, .T. ) ;
#662=VECTOR ( 'NONE', #6430, 999.9999999999998863 ) ;
#668=CIRCLE ( 'NONE', #25743, 5.009999999999999787 ) ;
#669=CARTESIAN_POINT ( 'NONE',  ( 1.265925305626725584E-16, 1.476463073999702669, -4.787500056513350977 ) ) ;
#693=CARTESIAN_POINT ( 'NONE',  ( 25.85999999999999943, 1.573300977624590313, -1.942864903642426144 ) ) ;
#703=DIRECTION ( 'NONE',  ( 1.000000000000000000, -8.574039729943018344E-17, -0.000000000000000000 ) ) ;
#704=FACE_OUTER_BOUND ( 'NONE', #14822, .T. ) ;
#710=CARTESIAN_POINT ( 'NONE',  ( 24.79750000273118715, -2.594547506269383685, -0.7685399846772043020 ) ) ;
#714=AXIS2_PLACEMENT_3D ( 'NONE', #13186, #23388, #20888 ) ;
#720=DIRECTION ( 'NONE',  ( -1.000000000000000000, 8.574039729943018344E-17, -3.081487911019577365E-33 ) ) ;
#728=B_SPLINE_CURVE_WITH_KNOTS ( 'NONE', 3,
 ( #7940, #18129, #5442, #15635, #1066, #29001, #26493, #6100, #31020, #18311, #23647, #8763, #426, #5914, #13122, #18477, #21469, #8428, #31499, #29155, #16280, #8584, #10951, #10606, #23808, #28668, #21153, #6243, #3592, #13602, #31351, #18623 ),
 .UNSPECIFIED., .F., .F.,
 ( 4, 2, 2, 2, 2, 2, 2, 2, 2, 2, 2, 2, 2, 2, 2, 4 ),
 ( 0.0002608162019139872436, 0.0007834053667116245385, 0.001305994531509261942, 0.001828583696306898803, 0.002351172861104536532, 0.002873762025902174260, 0.003396351190699811555, 0.003918940355497449284, 0.004441529520295087012, 0.004964118685092724741, 0.005486707849890363337, 0.006009297014688001065, 0.006531886179485638794, 0.007577064509080915986, 0.008099653673878555449, 0.008622242838676193177 ),
 .UNSPECIFIED. ) ;
#730=CARTESIAN_POINT ( 'NONE',  ( -3.122314033877847442E-16, -3.641590349731908649, -3.055657119358837992 ) ) ;
#732=ORIENTED_EDGE ( 'NONE', *, *, #5555, .F. ) ;
#736=ORIENTED_EDGE ( 'NONE', *, *, #30321, .F. ) ;
#738=CARTESIAN_POINT ( 'NONE',  ( 0.000000000000000000, 0.000000000000000000, 0.000000000000000000 ) ) ;
#741=VECTOR ( 'NONE', #14947, 1000.000000000000000 ) ;
#746=ORIENTED_EDGE ( 'NONE', *, *, #27778, .F. ) ;
#753=DIRECTION ( 'NONE',  ( 8.541412920197221047E-17, 0.9961946980917459893, -0.08715574274765196250 ) ) ;
#761=AXIS2_PLACEMENT_3D ( 'NONE', #16484, #14658, #22192 ) ;
#767=CARTESIAN_POINT ( 'NONE',  ( 21.73500000136559507, 3.156283516753366047, 0.9349337715887203748 ) ) ;
#778=CARTESIAN_POINT ( 'NONE',  ( 23.25111450864416085, -3.256483526998273983E-15, 2.499999999999998668 ) ) ;
#779=ORIENTED_EDGE ( 'NONE', *, *, #24719, .T. ) ;
#791=DIRECTION ( 'NONE',  ( 1.000000000000000000, -8.574039729943018344E-17, -0.000000000000000000 ) ) ;
#792=LINE ( 'NONE', #25869, #9780 ) ;
#798=ADVANCED_FACE ( 'NONE', ( #16866 ), #27219, .F. ) ;
#810=VECTOR ( 'NONE', #16884, 1000.000000000000000 ) ;
#813=FACE_OUTER_BOUND ( 'NONE', #16299, .T. ) ;
#828=CARTESIAN_POINT ( 'NONE',  ( -3.830085165118321606E-16, -4.467071865485483961, 1.625881193364682620 ) ) ;
#836=ORIENTED_EDGE ( 'NONE', *, *, #20671, .T. ) ;
#857=ORIENTED_EDGE ( 'NONE', *, *, #25958, .F. ) ;
#866=VERTEX_POINT ( 'NONE', #1849 ) ;
#870=DIRECTION ( 'NONE',  ( -1.000000000000000000, 8.574039729943018344E-17, 0.000000000000000000 ) ) ;
#873=EDGE_CURVE ( 'NONE', #7332, #32468, #32589, .T. ) ;
#876=CARTESIAN_POINT ( 'NONE',  ( 22.86000000273118715, -1.942864903642428587, -1.573300977624592756 ) ) ;
#880=CARTESIAN_POINT ( 'NONE',  ( 10.00000000000000000, 3.055657119358849094, -3.641590349731898879 ) ) ;
#888=DIRECTION ( 'NONE',  ( 6.062761635205596708E-17, 0.7071067811865490160, -0.7071067811865460184 ) ) ;
#897=ORIENTED_EDGE ( 'NONE', *, *, #16464, .F. ) ;
#908=( BOUNDED_CURVE ( )  B_SPLINE_CURVE ( 2, ( #3312, #2835, #5963 ),
 .UNSPECIFIED., .F., .F. ) 
 B_SPLINE_CURVE_WITH_KNOTS ( ( 3, 3 ),
 ( 0.9966116191895003640, 1.000000000000000000 ),
 .UNSPECIFIED. ) 
 CURVE ( )  GEOMETRIC_REPRESENTATION_ITEM ( )  RATIONAL_B_SPLINE_CURVE ( ( 0.9821626249036858880, 0.9896829947469992783, 1.000000000000000000 ) ) 
 REPRESENTATION_ITEM ( '' )  );
#918=FACE_OUTER_BOUND ( 'NONE', #5499, .T. ) ;
#920=CARTESIAN_POINT ( 'NONE',  ( 24.36000000136559507, -1.570731468192933633, -2.892927487894330074 ) ) ;
#921=EDGE_CURVE ( 'NONE', #22025, #24661, #7837, .T. ) ;
#932=ORIENTED_EDGE ( 'NONE', *, *, #14409, .T. ) ;
#943=PLANE ( 'NONE',  #31003 ) ;
#959=ORIENTED_EDGE ( 'NONE', *, *, #29979, .F. ) ;
#967=CARTESIAN_POINT ( 'NONE',  ( 20.74999999999999645, 5.000000000000001776, 0.000000000000000000 ) ) ;
#972=CARTESIAN_POINT ( 'NONE',  ( 21.04750000136559507, -1.913930629741527500, 2.363507492473149618 ) ) ;
#975=DIRECTION ( 'NONE',  ( 1.000000000000000000, -8.574039729943018344E-17, -0.000000000000000000 ) ) ;
#982=CARTESIAN_POINT ( 'NONE',  ( 3.830085165118329002E-16, 4.467071865485494619, -1.625881193364653088 ) ) ;
#991=DIRECTION ( 'NONE',  ( 8.541412920197217349E-17, 0.9961946980917454342, 0.08715574274765866547 ) ) ;
#999=ADVANCED_FACE ( 'NONE', ( #13492 ), #31556, .F. ) ;
#1014=CARTESIAN_POINT ( 'NONE',  ( 21.67250000136559507, 2.363507492473148286, 1.913930629741525058 ) ) ;
#1016=CARTESIAN_POINT ( 'NONE',  ( 0.000000000000000000, 0.000000000000000000, 0.000000000000000000 ) ) ;
#1020=CARTESIAN_POINT ( 'NONE',  ( 21.54750000273118715, -0.7685399846772070775, 2.594547506269381465 ) ) ;
#1021=EDGE_CURVE ( 'NONE', #6901, #10948, #8474, .T. ) ;
#1031=LINE ( 'NONE', #3560, #15028 ) ;
#1041=ORIENTED_EDGE ( 'NONE', *, *, #12240, .F. ) ;
#1042=ORIENTED_EDGE ( 'NONE', *, *, #27738, .F. ) ;
#1045=CARTESIAN_POINT ( 'NONE',  ( 10.57125986779756843, -0.8254815157535575487, 4.681538312723514395 ) ) ;
#1049=CARTESIAN_POINT ( 'NONE',  ( 10.57125986779756843, -4.681538312723523276, 0.8254815157535098091 ) ) ;
#1062=ORIENTED_EDGE ( 'NONE', *, *, #23763, .F. ) ;
#1066=CARTESIAN_POINT ( 'NONE',  ( 25.28062539936192721, -0.8645097064285574007, 2.400641828158613489 ) ) ;
#1071=ADVANCED_FACE ( 'NONE', ( #10502 ), #26054, .F. ) ;
#1081=DIRECTION ( 'NONE',  ( -1.000000000000000000, 8.574039729943019576E-17, -6.162975822039154730E-33 ) ) ;
#1088=ORIENTED_EDGE ( 'NONE', *, *, #4910, .T. ) ;
#1094=EDGE_CURVE ( 'NONE', #6248, #3262, #23369, .T. ) ;
#1103=CARTESIAN_POINT ( 'NONE',  ( 25.75999999999999801, -2.208672634433321348E-15, 0.000000000000000000 ) ) ;
#1105=CARTESIAN_POINT ( 'NONE',  ( 24.00111451137534146, -6.623356326098185375E-16, -2.499999999999998224 ) ) ;
#1107=LINE ( 'NONE', #18839, #22532 ) ;
#1108=AXIS2_PLACEMENT_3D ( 'NONE', #17154, #27684, #24680 ) ;
#1121=CIRCLE ( 'NONE', #19809, 5.010000000000000675 ) ;
#1123=VECTOR ( 'NONE', #33016, 1000.000000000000000 ) ;
#1134=PLANE ( 'NONE',  #5432 ) ;
#1136=ADVANCED_FACE ( 'NONE', ( #32236 ), #24349, .T. ) ;
#1142=DIRECTION ( 'NONE',  ( -6.062761635205589313E-17, -0.7071067811865484609, -0.7071067811865465735 ) ) ;
#1144=FACE_OUTER_BOUND ( 'NONE', #1534, .T. ) ;
#1147=EDGE_LOOP ( 'NONE', ( #4926, #9709, #30639, #13226 ) ) ;
#1155=AXIS2_PLACEMENT_3D ( 'NONE', #16083, #31977, #19263 ) ;
#1163=ADVANCED_FACE ( 'NONE', ( #24677 ), #6449, .T. ) ;
#1170=ORIENTED_EDGE ( 'NONE', *, *, #25908, .F. ) ;
#1175=AXIS2_PLACEMENT_3D ( 'NONE', #26703, #3817, #13994 ) ;
#1176=CARTESIAN_POINT ( 'NONE',  ( 22.29750000000000654, -0.7685399846772070775, 2.594547506269381465 ) ) ;
#1188=AXIS2_PLACEMENT_3D ( 'NONE', #13728, #6065, #26611 ) ;
#1190=CARTESIAN_POINT ( 'NONE',  ( 22.98500000273118715, -0.2613211581691358698, -2.486304738420681559 ) ) ;
#1191=EDGE_CURVE ( 'NONE', #17091, #14136, #16829, .T. ) ;
#1193=ADVANCED_FACE ( 'NONE', ( #11322 ), #21529, .F. ) ;
#1199=VECTOR ( 'NONE', #21108, 1000.000000000000114 ) ;
#1210=FACE_OUTER_BOUND ( 'NONE', #15996, .T. ) ;
#1218=ORIENTED_EDGE ( 'NONE', *, *, #23365, .T. ) ;
#1234=CARTESIAN_POINT ( 'NONE',  ( 10.00000000000000178, -8.574039729943018837E-16, 0.000000000000000000 ) ) ;
#1235=CARTESIAN_POINT ( 'NONE',  ( 25.75999999999999801, -2.208672634433321348E-15, 0.000000000000000000 ) ) ;
#1244=DIRECTION ( 'NONE',  ( -1.000000000000000000, 8.574039729943017111E-17, -0.000000000000000000 ) ) ;
#1246=LINE ( 'NONE', #4223, #24696 ) ;
#1249=ORIENTED_EDGE ( 'NONE', *, *, #27778, .T. ) ;
#1251=VECTOR ( 'NONE', #20562, 1000.000000000000000 ) ;
#1258=EDGE_CURVE ( 'NONE', #3790, #6345, #12784, .T. ) ;
#1268=VERTEX_POINT ( 'NONE', #27361 ) ;
#1278=LINE ( 'NONE', #19135, #8517 ) ;
#1284=DIRECTION ( 'NONE',  ( -1.000000000000000000, 8.574039729943017111E-17, -0.000000000000000000 ) ) ;
#1287=CIRCLE ( 'NONE', #6071, 5.010000000000000675 ) ;
#1307=ORIENTED_EDGE ( 'NONE', *, *, #26956, .T. ) ;
#1317=ORIENTED_EDGE ( 'NONE', *, *, #12569, .T. ) ;
#1337=CARTESIAN_POINT ( 'NONE',  ( 10.00000000000000000, 3.407865132560179422, 3.672404558090050397 ) ) ;
#1343=EDGE_CURVE ( 'NONE', #5341, #24378, #12322, .T. ) ;
#1351=FACE_OUTER_BOUND ( 'NONE', #7864, .T. ) ;
#1354=DIRECTION ( 'NONE',  ( 1.000000000000000000, -0.000000000000000000, -0.000000000000000000 ) ) ;
#1356=CARTESIAN_POINT ( 'NONE',  ( 23.11000000000000298, 1.942864903642424146, 1.573300977624592534 ) ) ;
#1368=CARTESIAN_POINT ( 'NONE',  ( 20.48500000273118715, 0.2613211581691317065, 2.486304738420681559 ) ) ;
#1372=EDGE_CURVE ( 'NONE', #22295, #31644, #32843, .T. ) ;
#1384=CARTESIAN_POINT ( 'NONE',  ( -2.037945749704288773E-16, -2.376879293651036118, -4.116875700062107235 ) ) ;
#1385=ORIENTED_EDGE ( 'NONE', *, *, #4688, .F. ) ;
#1396=EDGE_CURVE ( 'NONE', #7526, #14757, #6774, .T. ) ;
#1411=EDGE_CURVE ( 'NONE', #11371, #264, #7953, .T. ) ;
#1422=ORIENTED_EDGE ( 'NONE', *, *, #24866, .T. ) ;
#1423=VERTEX_POINT ( 'NONE', #28534 ) ;
#1424=CARTESIAN_POINT ( 'NONE',  ( 21.79750000136559507, 0.3178988483021036315, 3.024605502323848949 ) ) ;
#1425=EDGE_CURVE ( 'NONE', #26729, #13791, #15811, .T. ) ;
#1429=CARTESIAN_POINT ( 'NONE',  ( 10.00000000000000000, -1.625881193364727917, 4.467071865485467086 ) ) ;
#1430=FACE_OUTER_BOUND ( 'NONE', #16288, .T. ) ;
#1439=CARTESIAN_POINT ( 'NONE',  ( 10.00000000000000178, 1.115095498423375409, -4.884328206559827024 ) ) ;
#1440=EDGE_CURVE ( 'NONE', #228, #10851, #28184, .T. ) ;
#1441=DIRECTION ( 'NONE',  ( 8.574039729943018344E-17, 1.000000000000000000, 0.000000000000000000 ) ) ;
#1443=DIRECTION ( 'NONE',  ( 0.000000000000000000, 0.000000000000000000, -1.000000000000000000 ) ) ;
#1465=CARTESIAN_POINT ( 'NONE',  ( 10.00000000000000178, -8.574039729943018837E-16, 0.000000000000000000 ) ) ;
#1477=CARTESIAN_POINT ( 'NONE',  ( -2.619932554246537343E-16, -3.055657119358776264, -3.641590349731960163 ) ) ;
#1482=DIRECTION ( 'NONE',  ( -1.000000000000000000, 8.574039729943022041E-17, -3.081487911019577365E-33 ) ) ;
#1486=CARTESIAN_POINT ( 'NONE',  ( 10.57125986779756843, -4.971152295393306275, 0.6226916219171877431 ) ) ;
#1494=ORIENTED_EDGE ( 'NONE', *, *, #26545, .T. ) ;
#1499=EDGE_LOOP ( 'NONE', ( #31808, #1754, #25386, #17203 ) ) ;
#1502=ORIENTED_EDGE ( 'NONE', *, *, #6427, .T. ) ;
#1505=CARTESIAN_POINT ( 'NONE',  ( 21.67249999999999943, -1.291182301015472378, -2.378061970571982098 ) ) ;
#1514=EDGE_CURVE ( 'NONE', #21342, #4101, #4869, .T. ) ;
#1517=EDGE_CURVE ( 'NONE', #25432, #22025, #1121, .T. ) ;
#1521=CARTESIAN_POINT ( 'NONE',  ( 25.48500000136559507, 0.9349337715887185984, -3.156283516753368268 ) ) ;
#1534=EDGE_LOOP ( 'NONE', ( #13575, #12250, #8340, #1062 ) ) ;
#1542=CARTESIAN_POINT ( 'NONE',  ( 10.00000000000000000, -2.376879293651037006, -4.116875700062107235 ) ) ;
#1545=ORIENTED_EDGE ( 'NONE', *, *, #13133, .T. ) ;
#1548=FACE_OUTER_BOUND ( 'NONE', #10560, .T. ) ;
#1553=LINE ( 'NONE', #8752, #7565 ) ;
#1564=VERTEX_POINT ( 'NONE', #1429 ) ;
#1566=EDGE_CURVE ( 'NONE', #25432, #26782, #19131, .T. ) ;
#1574=CARTESIAN_POINT ( 'NONE',  ( 23.36000000136559507, 0.9349337715887185984, -3.156283516753368268 ) ) ;
#1576=FACE_OUTER_BOUND ( 'NONE', #23149, .T. ) ;
#1578=CYLINDRICAL_SURFACE ( 'NONE', #13324, 5.010000000000000675 ) ;
#1580=DIRECTION ( 'NONE',  ( -3.623545766764194901E-17, -0.4226182617406968878, -0.9063077870366511579 ) ) ;
#1581=VECTOR ( 'NONE', #30520, 1000.000000000000000 ) ;
#1582=CARTESIAN_POINT ( 'NONE',  ( 10.00000000000000000, -2.376879293651037006, -4.116875700062107235 ) ) ;
#1592=CARTESIAN_POINT ( 'NONE',  ( 16.25784845243109800, -4.536028529981986301E-15, 0.000000000000000000 ) ) ;
#1593=CARTESIAN_POINT ( 'NONE',  ( 23.67250000273118715, -2.378061970571983430, 1.291182301015471490 ) ) ;
#1594=CARTESIAN_POINT ( 'NONE',  ( 21.25111450864416085, -3.256483526998273983E-15, 2.499999999999998668 ) ) ;
#1600=VECTOR ( 'NONE', #17835, 1000.000000000000000 ) ;
#1605=LINE ( 'NONE', #1792, #5332 ) ;
#1622=CARTESIAN_POINT ( 'NONE',  ( 25.75999999999999801, -2.208672634433321348E-15, 0.000000000000000000 ) ) ;
#1627=CARTESIAN_POINT ( 'NONE',  ( 25.69585612515879092, 2.874579352301957602, -0.7480745300778689488 ) ) ;
#1629=DIRECTION ( 'NONE',  ( 1.000000000000000000, -8.574039729943018344E-17, -0.000000000000000000 ) ) ;
#1639=DIRECTION ( 'NONE',  ( 0.000000000000000000, 0.9961946980917459893, -0.08715574274765196250 ) ) ;
#1648=VECTOR ( 'NONE', #9674, 1000.000000000000000 ) ;
#1660=DIRECTION ( 'NONE',  ( 0.000000000000000000, 1.000000000000000000, 0.000000000000000000 ) ) ;
#1666=CARTESIAN_POINT ( 'NONE',  ( 25.17249999999999943, 1.291182301015469047, 2.378061970571981654 ) ) ;
#1672=CARTESIAN_POINT ( 'NONE',  ( 10.00000000000000000, -4.467071865485462645, -1.625881193364742572 ) ) ;
#1673=VECTOR ( 'NONE', #18833, 1000.000000000000000 ) ;
#1681=DIRECTION ( 'NONE',  ( 0.000000000000000000, 1.000000000000000000, 0.000000000000000000 ) ) ;
#1683=PLANE ( 'NONE',  #18957 ) ;
#1684=CARTESIAN_POINT ( 'NONE',  ( 24.86000000136559507, 1.570731468192929858, 2.892927487894329630 ) ) ;
#1689=CARTESIAN_POINT ( 'NONE',  ( 25.10999999999999943, 1.942864903642424146, 1.573300977624592534 ) ) ;
#1703=LINE ( 'NONE', #27097, #25690 ) ;
#1706=CARTESIAN_POINT ( 'NONE',  ( 2.619932554246560023E-16, 3.055657119358801133, 3.641590349731939735 ) ) ;
#1712=CARTESIAN_POINT ( 'NONE',  ( -2.921917104085873590E-16, -3.407865132560205623, 3.672404558090026860 ) ) ;
#1714=CIRCLE ( 'NONE', #8101, 5.009999999999999787 ) ;
#1716=ORIENTED_EDGE ( 'NONE', *, *, #10389, .T. ) ;
#1718=CARTESIAN_POINT ( 'NONE',  ( -3.148734258548762383E-16, -3.672404558090014426, -3.407865132560218946 ) ) ;
#1727=FACE_OUTER_BOUND ( 'NONE', #16561, .T. ) ;
#1728=VECTOR ( 'NONE', #870, 1000.000000000000000 ) ;
#1738=ORIENTED_EDGE ( 'NONE', *, *, #6747, .F. ) ;
#1743=DIRECTION ( 'NONE',  ( 0.000000000000000000, -0.7071067811865410224, -0.7071067811865540120 ) ) ;
#1749=CARTESIAN_POINT ( 'NONE',  ( 10.52034268205830259, 3.024842911000744206, -3.993798362933278057 ) ) ;
#1754=ORIENTED_EDGE ( 'NONE', *, *, #6925, .T. ) ;
#1755=CARTESIAN_POINT ( 'NONE',  ( 22.17250000136559507, -2.363507492473152283, -1.913930629741525280 ) ) ;
#1767=CARTESIAN_POINT ( 'NONE',  ( 20.98500000136559862, -0.9349337715887248157, 3.156283516753367824 ) ) ;
#1768=DIRECTION ( 'NONE',  ( 0.000000000000000000, 0.2588190451025176309, 0.9659258262890692004 ) ) ;
#1769=AXIS2_PLACEMENT_3D ( 'NONE', #30449, #25430, #7870 ) ;
#1777=CARTESIAN_POINT ( 'NONE',  ( 10.00000000000000000, 1.625881193364696831, 4.467071865485476856 ) ) ;
#1792=CARTESIAN_POINT ( 'NONE',  ( -1.444447458290426890E-30, -1.659765939693074585E-14, 4.753758587302147731 ) ) ;
#1810=VECTOR ( 'NONE', #18847, 1000.000000000000000 ) ;
#1815=AXIS2_PLACEMENT_3D ( 'NONE', #11513, #13677, #21554 ) ;
#1819=LINE ( 'NONE', #13986, #16551 ) ;
#1822=DIRECTION ( 'NONE',  ( 0.000000000000000000, 1.000000000000000000, 0.000000000000000000 ) ) ;
#1827=FACE_OUTER_BOUND ( 'NONE', #29736, .T. ) ;
#1831=CARTESIAN_POINT ( 'NONE',  ( 10.55147673363119232, 4.208382051008229929, -2.718385644597129502 ) ) ;
#1838=EDGE_CURVE ( 'NONE', #7133, #16940, #6477, .T. ) ;
#1842=FACE_OUTER_BOUND ( 'NONE', #18102, .T. ) ;
#1843=EDGE_CURVE ( 'NONE', #9763, #13750, #19058, .T. ) ;
#1849=CARTESIAN_POINT ( 'NONE',  ( 10.00000000000000178, -3.024842911000664269, -3.993798362933342894 ) ) ;
#1852=VERTEX_POINT ( 'NONE', #11038 ) ;
#1853=ORIENTED_EDGE ( 'NONE', *, *, #21991, .T. ) ;
#1855=DIRECTION ( 'NONE',  ( 0.000000000000000000, 0.000000000000000000, -1.000000000000000000 ) ) ;
#1856=CARTESIAN_POINT ( 'NONE',  ( 23.29750000000000654, -0.7685399846772070775, 2.594547506269381465 ) ) ;
#1859=DIRECTION ( 'NONE',  ( 1.000000000000000000, -8.574039729943018344E-17, -0.000000000000000000 ) ) ;
#1863=LINE ( 'NONE', #21887, #1648 ) ;
#1867=LINE ( 'NONE', #14533, #23003 ) ;
#1871=DIRECTION ( 'NONE',  ( -3.623545766764218936E-17, -0.4226182617406998854, -0.9063077870366498257 ) ) ;
#1873=CARTESIAN_POINT ( 'NONE',  ( 24.92250000136559507, 0.3178988483021036315, 3.024605502323848949 ) ) ;
#1874=DIRECTION ( 'NONE',  ( -1.000000000000000000, 8.574039729943017111E-17, -0.000000000000000000 ) ) ;
#1876=CARTESIAN_POINT ( 'NONE',  ( 24.75111450864415730, -6.623356326098185375E-16, -2.499999999999998224 ) ) ;
#1880=ORIENTED_EDGE ( 'NONE', *, *, #2324, .T. ) ;
#1882=ORIENTED_EDGE ( 'NONE', *, *, #12809, .T. ) ;
#1886=SHAPE_REPRESENTATION_RELATIONSHIP ( 'NONE' , 'NONE' ,  #13, #11140 ) ;
#1891=VERTEX_POINT ( 'NONE', #3537 ) ;
#1895=ORIENTED_EDGE ( 'NONE', *, *, #20380, .T. ) ;
#1900=DIRECTION ( 'NONE',  ( 8.281886410780504864E-17, 0.9659258262890672020, 0.2588190451025252359 ) ) ;
#1908=DIRECTION ( 'NONE',  ( 1.000000000000000000, -8.574039729943018344E-17, -0.000000000000000000 ) ) ;
#1914=CARTESIAN_POINT ( 'NONE',  ( 10.55147673363119054, 4.208382051008190849, 2.718385644597189454 ) ) ;
#1915=ORIENTED_EDGE ( 'NONE', *, *, #1566, .F. ) ;
#1917=EDGE_CURVE ( 'NONE', #3400, #22947, #4520, .T. ) ;
#1927=ORIENTED_EDGE ( 'NONE', *, *, #22837, .T. ) ;
#1928=PLANE ( 'NONE',  #20947 ) ;
#1930=ORIENTED_EDGE ( 'NONE', *, *, #13371, .T. ) ;
#1932=CARTESIAN_POINT ( 'NONE',  ( 22.48500000136559507, 2.892927487894327410, -1.570731468192931635 ) ) ;
#1940=CARTESIAN_POINT ( 'NONE',  ( 22.61000000136559507, 3.156283516753366047, 0.9349337715887203748 ) ) ;
#1945=ADVANCED_FACE ( 'NONE', ( #14025 ), #12426, .F. ) ;
#1959=LINE ( 'NONE', #11981, #24534 ) ;
#1970=CYLINDRICAL_SURFACE ( 'NONE', #27252, 5.010000000000000675 ) ;
#1973=CARTESIAN_POINT ( 'NONE',  ( 10.00000000000000000, -0.8254815157535575487, 4.681538312723514395 ) ) ;
#1974=ADVANCED_FACE ( 'NONE', ( #16709 ), #24540, .F. ) ;
#1977=CARTESIAN_POINT ( 'NONE',  ( 0.000000000000000000, 0.000000000000000000, 0.000000000000000000 ) ) ;
#1980=CARTESIAN_POINT ( 'NONE',  ( 4.013969549054183686E-16, 4.681538312723517059, 0.8254815157535410064 ) ) ;
#1987=LINE ( 'NONE', #32417, #24169 ) ;
#1990=CARTESIAN_POINT ( 'NONE',  ( 25.17250000136559507, -3.024605502323851169, 0.3178988483021052969 ) ) ;
#1995=DIRECTION ( 'NONE',  ( 0.000000000000000000, 1.000000000000000000, 0.000000000000000000 ) ) ;
#2003=ADVANCED_FACE ( 'NONE', ( #19893 ), #22068, .T. ) ;
#2007=CARTESIAN_POINT ( 'NONE',  ( 23.67250000136559507, 3.024605502323846729, -0.3178988483021056854 ) ) ;
#2012=FACE_OUTER_BOUND ( 'NONE', #25615, .T. ) ;
#2014=CARTESIAN_POINT ( 'NONE',  ( 21.98499999999999943, 2.486304738420679783, -0.2613211581691337604 ) ) ;
#2020=CARTESIAN_POINT ( 'NONE',  ( 10.00000000000000178, -8.574039729943018837E-16, 0.000000000000000000 ) ) ;
#2022=EDGE_CURVE ( 'NONE', #19954, #15334, #11262, .T. ) ;
#2023=CARTESIAN_POINT ( 'NONE',  ( 24.54750000136559507, 1.913930629741522838, -2.363507492473150062 ) ) ;
#2030=ORIENTED_EDGE ( 'NONE', *, *, #23669, .F. ) ;
#2049=LINE ( 'NONE', #15063, #16097 ) ;
#2050=EDGE_CURVE ( 'NONE', #29481, #2193, #17690, .T. ) ;
#2058=CARTESIAN_POINT ( 'NONE',  ( 23.98500000136559507, -2.892927487894331406, 1.570731468192932301 ) ) ;
#2062=VERTEX_POINT ( 'NONE', #2658 ) ;
#2063=DIRECTION ( 'NONE',  ( 0.000000000000000000, -0.08715574274766195451, 0.9961946980917452121 ) ) ;
#2073=ORIENTED_EDGE ( 'NONE', *, *, #10428, .T. ) ;
#2075=DIRECTION ( 'NONE',  ( 1.000000000000000000, -8.574039729943018344E-17, -0.000000000000000000 ) ) ;
#2076=PLANE ( 'NONE',  #5865 ) ;
#2077=ORIENTED_EDGE ( 'NONE', *, *, #13405, .T. ) ;
#2081=ORIENTED_EDGE ( 'NONE', *, *, #26832, .T. ) ;
#2087=CARTESIAN_POINT ( 'NONE',  ( 25.42250000136559507, 1.913930629741522838, -2.363507492473150062 ) ) ;
#2088=DIRECTION ( 'NONE',  ( -1.000000000000000000, 8.574039729943018344E-17, -3.081487911019577365E-33 ) ) ;
#2102=EDGE_LOOP ( 'NONE', ( #6416, #17791, #19276, #30267 ) ) ;
#2104=DIRECTION ( 'NONE',  ( 1.000000000000000000, 0.000000000000000000, 0.000000000000000000 ) ) ;
#2105=VERTEX_POINT ( 'NONE', #12524 ) ;
#2112=ADVANCED_FACE ( 'NONE', ( #23228, #10351 ), #9853, .T. ) ;
#2115=CARTESIAN_POINT ( 'NONE',  ( -3.122314033877847442E-16, -3.641590349731908649, -3.055657119358837992 ) ) ;
#2120=VERTEX_POINT ( 'NONE', #25227 ) ;
#2128=CARTESIAN_POINT ( 'NONE',  ( 10.00000000000000178, -8.574039729943018837E-16, 0.000000000000000000 ) ) ;
#2131=PLANE ( 'NONE',  #10758 ) ;
#2139=AXIS2_PLACEMENT_3D ( 'NONE', #26654, #24322, #8930 ) ;
#2140=CARTESIAN_POINT ( 'NONE',  ( 25.48500000136559862, 0.9349337715887185984, -3.156283516753368268 ) ) ;
#2154=AXIS2_PLACEMENT_3D ( 'NONE', #7909, #2426, #12917 ) ;
#2160=CARTESIAN_POINT ( 'NONE',  ( 23.92250000136559507, 0.3178988483021036315, 3.024605502323848949 ) ) ;
#2167=PLANE ( 'NONE',  #24609 ) ;
#2180=DIRECTION ( 'NONE',  ( 1.000000000000000000, -8.574039729943018344E-17, -0.000000000000000000 ) ) ;
#2193=VERTEX_POINT ( 'NONE', #31562 ) ;
#2204=LINE ( 'NONE', #15556, #30468 ) ;
#2208=PLANE ( 'NONE',  #10703 ) ;
#2217=CARTESIAN_POINT ( 'NONE',  ( 24.79750000136559507, 0.3178988483021036315, 3.024605502323848949 ) ) ;
#2220=CARTESIAN_POINT ( 'NONE',  ( 10.55147673363118876, 2.718385644597232975, -4.208382051008164204 ) ) ;
#2223=PLANE ( 'NONE',  #27907 ) ;
#2229=VECTOR ( 'NONE', #30387, 999.9999999999998863 ) ;
#2250=CYLINDRICAL_SURFACE ( 'NONE', #6459, 2.499999999999997780 ) ;
#2253=DIRECTION ( 'NONE',  ( 0.000000000000000000, 0.7071067811865510144, -0.7071067811865441310 ) ) ;
#2255=EDGE_LOOP ( 'NONE', ( #19539, #23813, #8408, #3849, #9389, #29009, #23566, #16293, #23949, #22491, #18386, #25816, #17016, #5848, #19508 ) ) ;
#2259=VECTOR ( 'NONE', #30566, 1000.000000000000114 ) ;
#2261=ADVANCED_FACE ( 'NONE', ( #15700 ), #19173, .T. ) ;
#2290=CARTESIAN_POINT ( 'NONE',  ( 10.00000000000000178, -5.003758587302150396, -0.2500000000000023870 ) ) ;
#2297=CARTESIAN_POINT ( 'NONE',  ( 10.57125986779756843, 4.681538312723528605, -0.8254815157534771686 ) ) ;
#2300=DIRECTION ( 'NONE',  ( 8.574039729943018344E-17, 1.000000000000000000, 0.000000000000000000 ) ) ;
#2307=VECTOR ( 'NONE', #19080, 1000.000000000000000 ) ;
#2321=CIRCLE ( 'NONE', #9769, 5.009999999999999787 ) ;
#2324=EDGE_CURVE ( 'NONE', #32756, #6345, #14156, .T. ) ;
#2327=CARTESIAN_POINT ( 'NONE',  ( 25.36000000136559862, -1.570731468192933633, -2.892927487894330074 ) ) ;
#2345=DIRECTION ( 'NONE',  ( 0.000000000000000000, 0.000000000000000000, -1.000000000000000000 ) ) ;
#2350=DIRECTION ( 'NONE',  ( 0.000000000000000000, 1.000000000000000000, 0.000000000000000000 ) ) ;
#2351=CARTESIAN_POINT ( 'NONE',  ( 22.67250000136559507, 3.024605502323846729, -0.3178988483021056854 ) ) ;
#2357=DIRECTION ( 'NONE',  ( 0.000000000000000000, 1.000000000000000000, 0.000000000000000000 ) ) ;
#2368=CARTESIAN_POINT ( 'NONE',  ( 22.29750000136559507, -2.363507492473152283, -1.913930629741525280 ) ) ;
#2369=ADVANCED_FACE ( 'NONE', ( #27367 ), #31895, .F. ) ;
#2374=DIRECTION ( 'NONE',  ( 8.541412920197209954E-17, 0.9961946980917444350, 0.08715574274767161345 ) ) ;
#2376=EDGE_LOOP ( 'NONE', ( #2741, #23359, #6753, #23925 ) ) ;
#2381=CIRCLE ( 'NONE', #28006, 5.010000000000000675 ) ;
#2403=DIRECTION ( 'NONE',  ( 7.023442172597821116E-17, 0.8191520442889873577, 0.5735764363510524877 ) ) ;
#2404=CARTESIAN_POINT ( 'NONE',  ( 24.42250000136559507, 1.913930629741522838, -2.363507492473150062 ) ) ;
#2408=CIRCLE ( 'NONE', #25152, 5.010000000000000675 ) ;
#2426=DIRECTION ( 'NONE',  ( 1.000000000000000000, -8.574039729943018344E-17, -0.000000000000000000 ) ) ;
#2430=DIRECTION ( 'NONE',  ( 7.472768010110926752E-18, 0.08715574274765534868, 0.9961946980917457672 ) ) ;
#2440=DIRECTION ( 'NONE',  ( 1.000000000000000000, -8.574039729943018344E-17, -0.000000000000000000 ) ) ;
#2451=ORIENTED_EDGE ( 'NONE', *, *, #3980, .T. ) ;
#2459=EDGE_LOOP ( 'NONE', ( #29247, #23738, #22150, #15242 ) ) ;
#2470=CARTESIAN_POINT ( 'NONE',  ( 10.00000000000000178, -8.574039729943018837E-16, 0.000000000000000000 ) ) ;
#2474=CARTESIAN_POINT ( 'NONE',  ( -4.013969549054180728E-16, -4.681538312723511730, -0.8254815157535732029 ) ) ;
#2490=CARTESIAN_POINT ( 'NONE',  ( 23.04750000136559862, -1.913930629741527500, 2.363507492473149618 ) ) ;
#2491=DIRECTION ( 'NONE',  ( -7.023442172597817418E-17, -0.8191520442889869136, -0.5735764363510531538 ) ) ;
#2510=CARTESIAN_POINT ( 'NONE',  ( 22.42250000136559507, -0.3178988483021076838, -3.024605502323848949 ) ) ;
#2515=DIRECTION ( 'NONE',  ( 8.281886410780486375E-17, 0.9659258262890655367, 0.2588190451025310090 ) ) ;
#2524=CARTESIAN_POINT ( 'NONE',  ( 24.04750000136559507, -1.913930629741527500, 2.363507492473149618 ) ) ;
#2528=CARTESIAN_POINT ( 'NONE',  ( -2.619932554246580731E-16, -3.055657119358825557, 3.641590349731918863 ) ) ;
#2529=CARTESIAN_POINT ( 'NONE',  ( 10.52034268205830614, 3.641590349731970822, -3.055657119358763829 ) ) ;
#2531=CARTESIAN_POINT ( 'NONE',  ( -5.338982705820479523E-17, -0.6226916219171703126, -4.971152295393308052 ) ) ;
#2535=ORIENTED_EDGE ( 'NONE', *, *, #6188, .T. ) ;
#2541=EDGE_LOOP ( 'NONE', ( #23957, #31888, #19910, #25346 ) ) ;
#2542=ADVANCED_FACE ( 'NONE', ( #26026 ), #21316, .T. ) ;
#2546=DIRECTION ( 'NONE',  ( 1.000000000000000000, -0.000000000000000000, -0.000000000000000000 ) ) ;
#2548=DIRECTION ( 'NONE',  ( -8.574039729943018344E-17, -1.000000000000000000, 0.000000000000000000 ) ) ;
#2558=CARTESIAN_POINT ( 'NONE',  ( 10.00000000000000178, -8.574039729943018837E-16, 0.000000000000000000 ) ) ;
#2559=CARTESIAN_POINT ( 'NONE',  ( 23.98500000273118715, -0.2613211581691358698, -2.486304738420681559 ) ) ;
#2560=DIRECTION ( 'NONE',  ( 1.000000000000000000, -8.574039729943018344E-17, -0.000000000000000000 ) ) ;
#2564=CYLINDRICAL_SURFACE ( 'NONE', #25794, 2.499999999999997780 ) ;
#2565=DIRECTION ( 'NONE',  ( 1.000000000000000000, -0.000000000000000000, -0.000000000000000000 ) ) ;
#2569=DIRECTION ( 'NONE',  ( 0.000000000000000000, -0.5735764363510388320, -0.8191520442889969056 ) ) ;
#2572=ORIENTED_EDGE ( 'NONE', *, *, #16111, .F. ) ;
#2577=VERTEX_POINT ( 'NONE', #31224 ) ;
#2578=CARTESIAN_POINT ( 'NONE',  ( -2.037945749704337831E-16, -2.376879293651093406, 4.116875700062075261 ) ) ;
#2581=ORIENTED_EDGE ( 'NONE', *, *, #10917, .T. ) ;
#2582=ORIENTED_EDGE ( 'NONE', *, *, #11610, .T. ) ;
#2584=EDGE_LOOP ( 'NONE', ( #10800, #23822, #7840, #28718 ) ) ;
#2596=LINE ( 'NONE', #12271, #4250 ) ;
#2611=CARTESIAN_POINT ( 'NONE',  ( 10.55147673363118876, -4.458382051008177527, -2.285372942705001797 ) ) ;
#2618=ORIENTED_EDGE ( 'NONE', *, *, #1411, .F. ) ;
#2624=ADVANCED_FACE ( 'NONE', ( #5784 ), #18824, .T. ) ;
#2635=CARTESIAN_POINT ( 'NONE',  ( -2.143509932485916364E-17, -0.2500000000000183187, 5.003758587302147731 ) ) ;
#2638=VERTEX_POINT ( 'NONE', #5935 ) ;
#2650=EDGE_CURVE ( 'NONE', #285, #1891, #13625, .T. ) ;
#2658=CARTESIAN_POINT ( 'NONE',  ( -3.822634483660894942E-16, -4.458382051008176639, -2.285372942705001797 ) ) ;
#2660=CARTESIAN_POINT ( 'NONE',  ( 23.04750000136559862, -1.913930629741527500, 2.363507492473149618 ) ) ;
#2661=DIRECTION ( 'NONE',  ( 1.000000000000000000, -8.574039729943018344E-17, -0.000000000000000000 ) ) ;
#2668=CARTESIAN_POINT ( 'NONE',  ( 25.75999999999999801, -2.208672634433321348E-15, 0.000000000000000000 ) ) ;
#2676=CARTESIAN_POINT ( 'NONE',  ( 25.75999999999999801, -2.208672634433321348E-15, 0.000000000000000000 ) ) ;
#2678=CARTESIAN_POINT ( 'NONE',  ( 23.04750000136559862, -1.913930629741527500, 2.363507492473149618 ) ) ;
#2681=DIRECTION ( 'NONE',  ( 1.000000000000000000, -8.574039729943018344E-17, -0.000000000000000000 ) ) ;
#2684=ORIENTED_EDGE ( 'NONE', *, *, #27284, .T. ) ;
#2692=VECTOR ( 'NONE', #17454, 1000.000000000000000 ) ;
#2701=LINE ( 'NONE', #28259, #20444 ) ;
#2703=CARTESIAN_POINT ( 'NONE',  ( 22.23500000273118715, 2.486304738420679783, -0.2613211581691337604 ) ) ;
#2708=CARTESIAN_POINT ( 'NONE',  ( 25.73500000136559507, 1.570731468192929858, 2.892927487894329186 ) ) ;
#2713=DIRECTION ( 'NONE',  ( 1.000000000000000000, -8.574039729943018344E-17, -0.000000000000000000 ) ) ;
#2715=ADVANCED_FACE ( 'NONE', ( #9085 ), #16617, .T. ) ;
#2718=CARTESIAN_POINT ( 'NONE',  ( 22.73500000136559862, 1.570731468192929858, 2.892927487894329186 ) ) ;
#2719=VECTOR ( 'NONE', #17645, 1000.000000000000227 ) ;
#2720=DIRECTION ( 'NONE',  ( 7.770718973608970028E-17, 0.9063077870366497146, -0.4226182617406998299 ) ) ;
#2734=CARTESIAN_POINT ( 'NONE',  ( 4.187842409712536805E-16, 4.884328206559836794, 1.115095498423326559 ) ) ;
#2741=ORIENTED_EDGE ( 'NONE', *, *, #22289, .T. ) ;
#2743=CARTESIAN_POINT ( 'NONE',  ( 2.143509932486214652E-17, 0.2500000000000532907, -5.003758587302145955 ) ) ;
#2746=LINE ( 'NONE', #12920, #31591 ) ;
#2758=VECTOR ( 'NONE', #7931, 1000.000000000000000 ) ;
#2761=LINE ( 'NONE', #28803, #270 ) ;
#2770=CIRCLE ( 'NONE', #19847, 5.010000000000000675 ) ;
#2788=EDGE_LOOP ( 'NONE', ( #25595, #11177, #27135, #6110 ) ) ;
#2793=CARTESIAN_POINT ( 'NONE',  ( 10.00000000000000000, 4.681538312723516171, 0.8254815157535410064 ) ) ;
#2807=CARTESIAN_POINT ( 'NONE',  ( 21.05656763645044904, 0.8852964313267427388, -2.499999999999999112 ) ) ;
#2810=FACE_OUTER_BOUND ( 'NONE', #20822, .T. ) ;
#2820=VECTOR ( 'NONE', #21328, 1000.000000000000227 ) ;
#2823=EDGE_CURVE ( 'NONE', #29918, #11672, #24820, .T. ) ;
#2824=VECTOR ( 'NONE', #17973, 1000.000000000000227 ) ;
#2825=VECTOR ( 'NONE', #28937, 1000.000000000000227 ) ;
#2835=CARTESIAN_POINT ( 'NONE',  ( 20.49290772595112742, 0.1310194482076003919, 2.499999999999998668 ) ) ;
#2842=AXIS2_PLACEMENT_3D ( 'NONE', #11680, #30108, #16522 ) ;
#2844=AXIS2_PLACEMENT_3D ( 'NONE', #12873, #23095, #22 ) ;
#2865=AXIS2_PLACEMENT_3D ( 'NONE', #14796, #7619, #2104 ) ;
#2875=AXIS2_PLACEMENT_3D ( 'NONE', #28041, #30378, #4975 ) ;
#2877=PRODUCT_DEFINITION_SHAPE ( 'NONE', 'NONE',  #21105 ) ;
#2879=FACE_OUTER_BOUND ( 'NONE', #1499, .T. ) ;
#2883=AXIS2_PLACEMENT_3D ( 'NONE', #4618, #14793, #22826 ) ;
#2884=AXIS2_PLACEMENT_3D ( 'NONE', #10025, #7514, #4189 ) ;
#2898=CARTESIAN_POINT ( 'NONE',  ( 26.17249999999999943, 1.291182301015469047, 2.378061970571981654 ) ) ;
#2902=VERTEX_POINT ( 'NONE', #9933 ) ;
#2907=CARTESIAN_POINT ( 'NONE',  ( 23.04750000136559862, -3.024605502323851169, 0.3178988483021052969 ) ) ;
#2908=VECTOR ( 'NONE', #28633, 1000.000000000000227 ) ;
#2909=CARTESIAN_POINT ( 'NONE',  ( 10.00000000000000000, 3.993798362933308255, 3.024842911000705570 ) ) ;
#2915=CARTESIAN_POINT ( 'NONE',  ( 25.11000000273118715, 1.573300977624590313, -1.942864903642426144 ) ) ;
#2933=EDGE_CURVE ( 'NONE', #10256, #23098, #19802, .T. ) ;
#2936=LINE ( 'NONE', #28291, #9609 ) ;
#2937=ORIENTED_EDGE ( 'NONE', *, *, #5783, .T. ) ;
#2956=DIRECTION ( 'NONE',  ( -1.000000000000000000, 8.574039729943017111E-17, -0.000000000000000000 ) ) ;
#2958=CARTESIAN_POINT ( 'NONE',  ( 0.000000000000000000, 0.000000000000000000, 0.000000000000000000 ) ) ;
#2964=ORIENTED_EDGE ( 'NONE', *, *, #3466, .T. ) ;
#2967=CARTESIAN_POINT ( 'NONE',  ( 10.00000000000000178, -8.574039729943018837E-16, 0.000000000000000000 ) ) ;
#2976=VERTEX_POINT ( 'NONE', #3246 ) ;
#2985=EDGE_CURVE ( 'NONE', #264, #2193, #25829, .T. ) ;
#2986=CARTESIAN_POINT ( 'NONE',  ( 25.75999999999999801, -2.208672634433321348E-15, 0.000000000000000000 ) ) ;
#2987=DIRECTION ( 'NONE',  ( 6.062761635205572056E-17, 0.7071067811865465735, -0.7071067811865484609 ) ) ;
#2992=DIRECTION ( 'NONE',  ( 1.000000000000000000, -8.574039729943018344E-17, -0.000000000000000000 ) ) ;
#2997=CARTESIAN_POINT ( 'NONE',  ( 23.92250000000000298, 2.378061970571979433, -1.291182301015470602 ) ) ;
#3015=CARTESIAN_POINT ( 'NONE',  ( 25.75999999999999801, -2.208672634433321348E-15, 0.000000000000000000 ) ) ;
#3021=ORIENTED_EDGE ( 'NONE', *, *, #24403, .F. ) ;
#3029=CARTESIAN_POINT ( 'NONE',  ( 20.98500000136559862, -0.9349337715887247047, 3.156283516753367824 ) ) ;
#3034=VERTEX_POINT ( 'NONE', #20967 ) ;
#3035=CARTESIAN_POINT ( 'NONE',  ( 10.00000000000000178, 0.2500000000000544564, -5.003758587302146843 ) ) ;
#3046=VERTEX_POINT ( 'NONE', #28500 ) ;
#3058=LINE ( 'NONE', #13853, #1728 ) ;
#3066=CARTESIAN_POINT ( 'NONE',  ( 22.29750000136559507, -0.3178988483021076838, -3.024605502323848949 ) ) ;
#3071=VERTEX_POINT ( 'NONE', #25282 ) ;
#3083=ORIENTED_EDGE ( 'NONE', *, *, #25966, .T. ) ;
#3086=VERTEX_POINT ( 'NONE', #4566 ) ;
#3088=LINE ( 'NONE', #13245, #19881 ) ;
#3090=EDGE_CURVE ( 'NONE', #20203, #3086, #3220, .T. ) ;
#3100=DIRECTION ( 'NONE',  ( -3.623545766764251600E-17, -0.4226182617407038267, 0.9063077870366479383 ) ) ;
#3112=CARTESIAN_POINT ( 'NONE',  ( 23.61000000136559507, 2.892927487894327410, -1.570731468192931635 ) ) ;
#3121=DIRECTION ( 'NONE',  ( 1.000000000000000000, -8.574039729943018344E-17, -0.000000000000000000 ) ) ;
#3126=CARTESIAN_POINT ( 'NONE',  ( 10.00000000000000000, 3.641590349731970822, -3.055657119358763829 ) ) ;
#3130=LINE ( 'NONE', #20526, #23978 ) ;
#3133=ORIENTED_EDGE ( 'NONE', *, *, #22371, .F. ) ;
#3140=CARTESIAN_POINT ( 'NONE',  ( 23.00111451137534502, -1.283275288181523244E-15, -2.499999999999998668 ) ) ;
#3157=CARTESIAN_POINT ( 'NONE',  ( 10.56183597391177464, 4.753758587302147731, 0.000000000000000000 ) ) ;
#3169=ORIENTED_EDGE ( 'NONE', *, *, #27366, .T. ) ;
#3170=CYLINDRICAL_SURFACE ( 'NONE', #25709, 5.010000000000000675 ) ;
#3186=VERTEX_POINT ( 'NONE', #28763 ) ;
#3196=CARTESIAN_POINT ( 'NONE',  ( 25.92249999999999943, 2.378061970571979433, -1.291182301015470824 ) ) ;
#3206=CARTESIAN_POINT ( 'NONE',  ( 25.75999999999999801, 0.8512451026088739825, 2.902758476911987628 ) ) ;
#3211=CARTESIAN_POINT ( 'NONE',  ( 21.79750000136559507, 0.3178988483021036315, 3.024605502323848949 ) ) ;
#3212=CARTESIAN_POINT ( 'NONE',  ( 10.57125986779756843, -4.884328206559843899, 1.115095498423292142 ) ) ;
#3216=ADVANCED_FACE ( 'NONE', ( #18427 ), #18572, .F. ) ;
#3217=DIRECTION ( 'NONE',  ( 0.000000000000000000, 1.000000000000000000, 0.000000000000000000 ) ) ;
#3219=ORIENTED_EDGE ( 'NONE', *, *, #25311, .F. ) ;
#3220=CIRCLE ( 'NONE', #9055, 5.009999999999999787 ) ;
#3225=LINE ( 'NONE', #10913, #22517 ) ;
#3231=CARTESIAN_POINT ( 'NONE',  ( 10.00000000000000178, -8.574039729943018837E-16, 0.000000000000000000 ) ) ;
#3234=VERTEX_POINT ( 'NONE', #8228 ) ;
#3245=DIRECTION ( 'NONE',  ( 1.000000000000000000, -0.000000000000000000, -0.000000000000000000 ) ) ;
#3246=CARTESIAN_POINT ( 'NONE',  ( 10.00000000000000178, 3.407865132560231380, -3.672404558090005100 ) ) ;
#3250=ADVANCED_FACE ( 'NONE', ( #7884 ), #12885, .T. ) ;
#3259=DIRECTION ( 'NONE',  ( 0.000000000000000000, 0.2588190451025241812, -0.9659258262890673130 ) ) ;
#3260=EDGE_CURVE ( 'NONE', #13354, #24212, #17632, .T. ) ;
#3262=VERTEX_POINT ( 'NONE', #2909 ) ;
#3263=CARTESIAN_POINT ( 'NONE',  ( 24.54750000136559507, 1.913930629741522838, -2.363507492473150062 ) ) ;
#3274=LINE ( 'NONE', #18630, #19740 ) ;
#3277=CARTESIAN_POINT ( 'NONE',  ( 24.42250000136559507, 1.913930629741522838, -2.363507492473150062 ) ) ;
#3279=ORIENTED_EDGE ( 'NONE', *, *, #26530, .F. ) ;
#3286=CARTESIAN_POINT ( 'NONE',  ( 25.75999999999999801, -2.208672634433321348E-15, 0.000000000000000000 ) ) ;
#3307=VECTOR ( 'NONE', #1874, 1000.000000000000000 ) ;
#3312=CARTESIAN_POINT ( 'NONE',  ( 20.50111451137534857, -3.256483526998273983E-15, 2.499999999999998668 ) ) ;
#3313=VECTOR ( 'NONE', #7778, 999.9999999999998863 ) ;
#3314=EDGE_CURVE ( 'NONE', #9752, #6678, #9631, .T. ) ;
#3321=AXIS2_PLACEMENT_3D ( 'NONE', #32670, #14601, #1743 ) ;
#3322=EDGE_CURVE ( 'NONE', #13354, #25477, #1819, .T. ) ;
#3326=PLANE ( 'NONE',  #7047 ) ;
#3339=ORIENTED_EDGE ( 'NONE', *, *, #9034, .T. ) ;
#3349=AXIS2_PLACEMENT_3D ( 'NONE', #6670, #14008, #1995 ) ;
#3360=ORIENTED_EDGE ( 'NONE', *, *, #31151, .F. ) ;
#3366=VECTOR ( 'NONE', #30673, 1000.000000000000000 ) ;
#3369=CARTESIAN_POINT ( 'NONE',  ( 10.52034268205830259, 3.055657119358849094, -3.641590349731898879 ) ) ;
#3375=VECTOR ( 'NONE', #24383, 999.9999999999998863 ) ;
#3382=CARTESIAN_POINT ( 'NONE',  ( 20.86000000136559507, -0.9349337715887248157, 3.156283516753367824 ) ) ;
#3384=CARTESIAN_POINT ( 'NONE',  ( -3.529825581556913254E-16, -4.116875700062066379, -2.376879293651108060 ) ) ;
#3385=ORIENTED_EDGE ( 'NONE', *, *, #25958, .T. ) ;
#3390=CARTESIAN_POINT ( 'NONE',  ( 21.36000000273118715, 1.942864903642424146, 1.573300977624592534 ) ) ;
#3400=VERTEX_POINT ( 'NONE', #16669 ) ;
#3406=VERTEX_POINT ( 'NONE', #26882 ) ;
#3411=CIRCLE ( 'NONE', #13434, 6.000000000000000888 ) ;
#3417=VECTOR ( 'NONE', #31959, 1000.000000000000000 ) ;
#3438=VECTOR ( 'NONE', #20465, 1000.000000000000000 ) ;
#3440=DIRECTION ( 'NONE',  ( 1.000000000000000000, -0.000000000000000000, -0.000000000000000000 ) ) ;
#3442=CARTESIAN_POINT ( 'NONE',  ( 23.73500000136559152, 3.156283516753366047, 0.9349337715887203748 ) ) ;
#3450=ORIENTED_EDGE ( 'NONE', *, *, #130, .T. ) ;
#3452=DIRECTION ( 'NONE',  ( -1.000000000000000000, 8.574039729943017111E-17, -0.000000000000000000 ) ) ;
#3455=CARTESIAN_POINT ( 'NONE',  ( 23.23500000000000298, 0.2613211581691317065, 2.486304738420681559 ) ) ;
#3462=CARTESIAN_POINT ( 'NONE',  ( 10.00000000000000000, -4.116875700062067267, -2.376879293651108060 ) ) ;
#3463=VERTEX_POINT ( 'NONE', #30066 ) ;
#3466=EDGE_CURVE ( 'NONE', #7281, #2902, #29233, .T. ) ;
#3480=CARTESIAN_POINT ( 'NONE',  ( 10.00000000000000000, 2.285372942705016897, -4.458382051008168645 ) ) ;
#3481=LINE ( 'NONE', #31874, #32687 ) ;
#3488=CARTESIAN_POINT ( 'NONE',  ( 25.75999999999999801, -2.208672634433321348E-15, 0.000000000000000000 ) ) ;
#3516=FACE_OUTER_BOUND ( 'NONE', #18801, .T. ) ;
#3527=CARTESIAN_POINT ( 'NONE',  ( -2.330754651808268490E-16, -2.718385644597144157, -4.208382051008221048 ) ) ;
#3537=CARTESIAN_POINT ( 'NONE',  ( 1.394036994807608625E-16, 1.625881193364697719, 4.467071865485476856 ) ) ;
#3546=CARTESIAN_POINT ( 'NONE',  ( 22.42250000136559507, 1.913930629741522838, -2.363507492473150062 ) ) ;
#3549=CARTESIAN_POINT ( 'NONE',  ( 10.55147673363119232, 2.376879293651063652, 4.116875700062091248 ) ) ;
#3550=CARTESIAN_POINT ( 'NONE',  ( 21.86000000273118715, -1.942864903642428587, -1.573300977624592756 ) ) ;
#3558=VERTEX_POINT ( 'NONE', #17845 ) ;
#3560=CARTESIAN_POINT ( 'NONE',  ( 10.52034268205830614, 3.407865132560178978, 3.672404558090050397 ) ) ;
#3572=DIRECTION ( 'NONE',  ( -4.917867153433088392E-17, -0.5735764363510558184, 0.8191520442889849152 ) ) ;
#3581=LINE ( 'NONE', #8897, #219 ) ;
#3592=CARTESIAN_POINT ( 'NONE',  ( 25.53801055518932017, -0.6886950482053056932, -2.722715053693994136 ) ) ;
#3606=CARTESIAN_POINT ( 'NONE',  ( 0.000000000000000000, 0.000000000000000000, 0.000000000000000000 ) ) ;
#3609=DIRECTION ( 'NONE',  ( 1.000000000000000000, -8.574039729943018344E-17, -0.000000000000000000 ) ) ;
#3611=VERTEX_POINT ( 'NONE', #16138 ) ;
#3613=CARTESIAN_POINT ( 'NONE',  ( 10.00000000000000000, 3.024842911000744650, -3.993798362933278057 ) ) ;
#3617=CARTESIAN_POINT ( 'NONE',  ( 10.00000000000000000, -4.116875700062067267, -2.376879293651108060 ) ) ;
#3620=CARTESIAN_POINT ( 'NONE',  ( -1.394036994807583480E-16, -1.625881193364668409, -4.467071865485488402 ) ) ;
#3624=ADVANCED_FACE ( 'NONE', ( #23344 ), #943, .F. ) ;
#3643=CARTESIAN_POINT ( 'NONE',  ( 10.55147673363119232, -4.458382051008210389, 2.285372942704937849 ) ) ;
#3644=CARTESIAN_POINT ( 'NONE',  ( 25.75999999999999801, -2.208672634433321348E-15, 0.000000000000000000 ) ) ;
#3645=CARTESIAN_POINT ( 'NONE',  ( 10.00000000000000178, -1.946309384392625796, 4.616489984850526085 ) ) ;
#3648=CARTESIAN_POINT ( 'NONE',  ( 10.52034268205830259, -3.641590349731909537, -3.055657119358837992 ) ) ;
#3653=DIRECTION ( 'NONE',  ( 8.574039729943018344E-17, 1.000000000000000000, 0.000000000000000000 ) ) ;
#3666=EDGE_CURVE ( 'NONE', #29657, #4019, #252, .T. ) ;
#3679=ORIENTED_EDGE ( 'NONE', *, *, #7930, .F. ) ;
#3683=CARTESIAN_POINT ( 'NONE',  ( 22.61000000000000298, -1.942864903642428587, -1.573300977624592756 ) ) ;
#3684=EDGE_CURVE ( 'NONE', #21342, #8558, #2936, .T. ) ;
#3712=VECTOR ( 'NONE', #5463, 1000.000000000000114 ) ;
#3714=ORIENTED_EDGE ( 'NONE', *, *, #23741, .F. ) ;
#3719=DIRECTION ( 'NONE',  ( 8.574039729943018344E-17, 1.000000000000000000, 0.000000000000000000 ) ) ;
#3722=EDGE_LOOP ( 'NONE', ( #6797, #26155, #30190, #21610 ) ) ;
#3725=DIRECTION ( 'NONE',  ( 7.023442172597838372E-17, 0.8191520442889889120, 0.5735764363510502672 ) ) ;
#3731=VECTOR ( 'NONE', #13612, 1000.000000000000000 ) ;
#3737=VECTOR ( 'NONE', #17304, 999.9999999999998863 ) ;
#3739=DIRECTION ( 'NONE',  ( -7.023442172597853164E-17, -0.8191520442889907994, -0.5735764363510474917 ) ) ;
#3749=VECTOR ( 'NONE', #8442, 1000.000000000000000 ) ;
#3753=DIRECTION ( 'NONE',  ( -1.000000000000000000, 8.574039729943019576E-17, -0.000000000000000000 ) ) ;
#3756=CARTESIAN_POINT ( 'NONE',  ( 25.36000000136559507, 0.9349337715887185984, -3.156283516753368268 ) ) ;
#3763=CARTESIAN_POINT ( 'NONE',  ( 21.61000000273118715, -1.573300977624594976, 1.942864903642425700 ) ) ;
#3776=DIRECTION ( 'NONE',  ( 0.000000000000000000, 0.000000000000000000, -1.000000000000000000 ) ) ;
#3778=DIRECTION ( 'NONE',  ( 3.623545766764243588E-17, 0.4226182617407029385, -0.9063077870366482713 ) ) ;
#3790=VERTEX_POINT ( 'NONE', #730 ) ;
#3797=AXIS2_PLACEMENT_3D ( 'NONE', #30382, #17655, #4979 ) ;
#3801=VECTOR ( 'NONE', #9121, 1000.000000000000000 ) ;
#3810=CARTESIAN_POINT ( 'NONE',  ( 25.72720924917965846, 2.995293602030530078, 0.1965175717148812951 ) ) ;
#3816=FACE_OUTER_BOUND ( 'NONE', #19515, .T. ) ;
#3817=DIRECTION ( 'NONE',  ( 1.000000000000000000, -0.000000000000000000, -0.000000000000000000 ) ) ;
#3844=ORIENTED_EDGE ( 'NONE', *, *, #10178, .F. ) ;
#3845=CARTESIAN_POINT ( 'NONE',  ( 10.00000000000000178, -8.574039729943018837E-16, 0.000000000000000000 ) ) ;
#3849=ORIENTED_EDGE ( 'NONE', *, *, #8074, .F. ) ;
#3853=CARTESIAN_POINT ( 'NONE',  ( 24.17249999999999943, 1.291182301015469047, 2.378061970571981654 ) ) ;
#3859=PLANE ( 'NONE',  #10177 ) ;
#3866=VECTOR ( 'NONE', #3452, 1000.000000000000000 ) ;
#3868=DIRECTION ( 'NONE',  ( -6.062761635205572056E-17, -0.7071067811865465735, -0.7071067811865484609 ) ) ;
#3888=VECTOR ( 'NONE', #26251, 1000.000000000000114 ) ;
#3896=DIRECTION ( 'NONE',  ( -2.219124775575015083E-17, -0.2588190451025310090, 0.9659258262890655367 ) ) ;
#3901=CARTESIAN_POINT ( 'NONE',  ( 10.00000000000000000, 3.641590349731929077, 3.055657119358814011 ) ) ;
#3902=VECTOR ( 'NONE', #2374, 1000.000000000000000 ) ;
#3905=VECTOR ( 'NONE', #10022, 1000.000000000000000 ) ;
#3912=VECTOR ( 'NONE', #23072, 1000.000000000000000 ) ;
#3929=EDGE_LOOP ( 'NONE', ( #19829, #19666, #1317, #11345 ) ) ;
#3931=VERTEX_POINT ( 'NONE', #22260 ) ;
#3935=DIRECTION ( 'NONE',  ( -7.472768010111378190E-18, -0.08715574274766135776, 0.9961946980917453232 ) ) ;
#3940=CARTESIAN_POINT ( 'NONE',  ( 25.17250000136559507, -2.363507492473152283, -1.913930629741525280 ) ) ;
#3954=CARTESIAN_POINT ( 'NONE',  ( 10.00000000000000178, -8.574039729943018837E-16, 0.000000000000000000 ) ) ;
#3980=EDGE_CURVE ( 'NONE', #1891, #4614, #1703, .T. ) ;
#3987=VERTEX_POINT ( 'NONE', #1384 ) ;
#3996=CARTESIAN_POINT ( 'NONE',  ( 10.00000000000000000, -4.116875700062100130, 2.376879293651050329 ) ) ;
#4001=EDGE_LOOP ( 'NONE', ( #7404, #31991, #7042, #20900 ) ) ;
#4019=VERTEX_POINT ( 'NONE', #32469 ) ;
#4021=CARTESIAN_POINT ( 'NONE',  ( 10.55147673363119054, 4.116875700062082366, 2.376879293651078751 ) ) ;
#4023=CARTESIAN_POINT ( 'NONE',  ( 23.67250000000000298, -1.291182301015472378, -2.378061970571982098 ) ) ;
#4025=DIRECTION ( 'NONE',  ( 4.917867153433032309E-17, 0.5735764363510496011, -0.8191520442889893561 ) ) ;
#4028=DIRECTION ( 'NONE',  ( 6.062761635205589313E-17, 0.7071067811865484609, 0.7071067811865465735 ) ) ;
#4031=ORIENTED_EDGE ( 'NONE', *, *, #13751, .F. ) ;
#4038=LINE ( 'NONE', #9692, #23565 ) ;
#4039=CARTESIAN_POINT ( 'NONE',  ( 10.00000000000000000, 4.884328206559851004, -1.115095498423258391 ) ) ;
#4044=EDGE_LOOP ( 'NONE', ( #4344, #779, #17512, #15466 ) ) ;
#4066=PLANE ( 'NONE',  #13309 ) ;
#4072=EDGE_CURVE ( 'NONE', #2577, #30211, #32136, .T. ) ;
#4090=ORIENTED_EDGE ( 'NONE', *, *, #21198, .T. ) ;
#4094=EDGE_LOOP ( 'NONE', ( #32039, #9240, #30605, #31332 ) ) ;
#4095=LINE ( 'NONE', #9420, #18216 ) ;
#4098=DIRECTION ( 'NONE',  ( 0.000000000000000000, 1.000000000000000000, 0.000000000000000000 ) ) ;
#4101=VERTEX_POINT ( 'NONE', #4859 ) ;
#4113=CARTESIAN_POINT ( 'NONE',  ( 23.79750000273118715, -2.594547506269383685, -0.7685399846772043020 ) ) ;
#4130=CARTESIAN_POINT ( 'NONE',  ( 10.52034268205830614, -3.641590349731950393, 3.055657119358789142 ) ) ;
#4136=DIRECTION ( 'NONE',  ( 1.000000000000000000, -8.574039729943018344E-17, -0.000000000000000000 ) ) ;
#4138=EDGE_CURVE ( 'NONE', #20071, #115, #7523, .T. ) ;
#4149=CARTESIAN_POINT ( 'NONE',  ( -3.830085165118302378E-16, -4.467071865485461757, -1.625881193364742572 ) ) ;
#4154=PLANE ( 'NONE',  #17241 ) ;
#4170=CARTESIAN_POINT ( 'NONE',  ( 24.60999999999999943, -1.942864903642428587, -1.573300977624592756 ) ) ;
#4184=EDGE_CURVE ( 'NONE', #32821, #5447, #20351, .T. ) ;
#4185=CARTESIAN_POINT ( 'NONE',  ( 25.23500000136559507, -3.156283516753370488, -0.9349337715887220401 ) ) ;
#4189=DIRECTION ( 'NONE',  ( 0.000000000000000000, 0.08715574274764853469, 0.9961946980917464334 ) ) ;
#4194=ORIENTED_EDGE ( 'NONE', *, *, #10389, .F. ) ;
#4198=ORIENTED_EDGE ( 'NONE', *, *, #12253, .F. ) ;
#4214=ORIENTED_EDGE ( 'NONE', *, *, #9124, .T. ) ;
#4215=FACE_OUTER_BOUND ( 'NONE', #9448, .T. ) ;
#4217=CARTESIAN_POINT ( 'NONE',  ( 2.037945749704362236E-16, 2.376879293651122271, -4.116875700062057497 ) ) ;
#4218=CARTESIAN_POINT ( 'NONE',  ( 25.04750000136559507, -3.024605502323851169, 0.3178988483021052969 ) ) ;
#4223=CARTESIAN_POINT ( 'NONE',  ( 10.56183597391177464, -1.750323540954535505E-14, 4.753758587302147731 ) ) ;
#4227=ORIENTED_EDGE ( 'NONE', *, *, #8514, .F. ) ;
#4230=EDGE_CURVE ( 'NONE', #31957, #24212, #30443, .T. ) ;
#4235=VERTEX_POINT ( 'NONE', #4703 ) ;
#4242=CARTESIAN_POINT ( 'NONE',  ( 21.67250000136559507, 2.363507492473148286, 1.913930629741525058 ) ) ;
#4244=ORIENTED_EDGE ( 'NONE', *, *, #17005, .T. ) ;
#4250=VECTOR ( 'NONE', #25334, 1000.000000000000000 ) ;
#4254=CARTESIAN_POINT ( 'NONE',  ( 22.98500000136559507, -2.892927487894331406, 1.570731468192932301 ) ) ;
#4264=CYLINDRICAL_SURFACE ( 'NONE', #25759, 2.499999999999997780 ) ;
#4272=CARTESIAN_POINT ( 'NONE',  ( 10.00000000000000178, 4.971152295393311604, -0.6226916219171535483 ) ) ;
#4285=EDGE_CURVE ( 'NONE', #7137, #15697, #4332, .T. ) ;
#4291=VECTOR ( 'NONE', #5322, 1000.000000000000000 ) ;
#4294=DIRECTION ( 'NONE',  ( -7.770718973608971261E-17, -0.9063077870366493816, -0.4226182617407005515 ) ) ;
#4297=CARTESIAN_POINT ( 'NONE',  ( 25.59647104375314441, 0.9427069350839755169, -2.712103814530933743 ) ) ;
#4300=VECTOR ( 'NONE', #26617, 1000.000000000000000 ) ;
#4303=FACE_OUTER_BOUND ( 'NONE', #9384, .T. ) ;
#4309=DIRECTION ( 'NONE',  ( 1.000000000000000000, -8.574039729943018344E-17, -0.000000000000000000 ) ) ;
#4312=CARTESIAN_POINT ( 'NONE',  ( 24.48500000273118715, 0.2613211581691317065, 2.486304738420681559 ) ) ;
#4318=CARTESIAN_POINT ( 'NONE',  ( 25.42250000136559507, -0.3178988483021076838, -3.024605502323848949 ) ) ;
#4324=ORIENTED_EDGE ( 'NONE', *, *, #14019, .F. ) ;
#4325=CARTESIAN_POINT ( 'NONE',  ( -1.394036994807634510E-16, -1.625881193364727917, 4.467071865485467086 ) ) ;
#4332=CIRCLE ( 'NONE', #27285, 5.000000000000002665 ) ;
#4335=CARTESIAN_POINT ( 'NONE',  ( 23.00111451137534502, -1.283275288181523244E-15, -2.499999999999998668 ) ) ;
#4341=CARTESIAN_POINT ( 'NONE',  ( 23.48500000000000298, -2.486304738420683780, 0.2613211581691335383 ) ) ;
#4344=ORIENTED_EDGE ( 'NONE', *, *, #20308, .F. ) ;
#4358=LINE ( 'NONE', #14537, #810 ) ;
#4360=CARTESIAN_POINT ( 'NONE',  ( 25.04750000136559507, -1.913930629741527500, 2.363507492473149618 ) ) ;
#4361=AXIS2_PLACEMENT_3D ( 'NONE', #23605, #8543, #11220 ) ;
#4365=CARTESIAN_POINT ( 'NONE',  ( 24.92249999999999943, 2.378061970571979433, -1.291182301015470602 ) ) ;
#4379=AXIS2_PLACEMENT_3D ( 'NONE', #340, #10513, #18196 ) ;
#4395=EDGE_CURVE ( 'NONE', #23437, #29657, #24098, .T. ) ;
#4402=AXIS2_PLACEMENT_3D ( 'NONE', #30318, #27125, #4416 ) ;
#4404=CARTESIAN_POINT ( 'NONE',  ( 25.17250000136559507, -2.363507492473152283, -1.913930629741525280 ) ) ;
#4407=DIRECTION ( 'NONE',  ( -3.623545766764139434E-17, -0.4226182617406906705, -0.9063077870366540445 ) ) ;
#4410=CARTESIAN_POINT ( 'NONE',  ( 10.57125986779756843, -0.6226916219171712008, -4.971152295393308052 ) ) ;
#4411=VERTEX_POINT ( 'NONE', #14015 ) ;
#4416=DIRECTION ( 'NONE',  ( 0.000000000000000000, -0.9961946980917466554, 0.08715574274764535667 ) ) ;
#4418=ORIENTED_EDGE ( 'NONE', *, *, #13371, .F. ) ;
#4433=CARTESIAN_POINT ( 'NONE',  ( 24.17250000136559507, -2.363507492473152283, -1.913930629741525280 ) ) ;
#4440=ORIENTED_EDGE ( 'NONE', *, *, #5741, .T. ) ;
#4444=CARTESIAN_POINT ( 'NONE',  ( 22.67250000136559507, 2.363507492473148286, 1.913930629741525058 ) ) ;
#4448=DIRECTION ( 'NONE',  ( 1.000000000000000000, -8.574039729943018344E-17, -0.000000000000000000 ) ) ;
#4463=EDGE_CURVE ( 'NONE', #17640, #22010, #24999, .T. ) ;
#4469=ORIENTED_EDGE ( 'NONE', *, *, #17760, .F. ) ;
#4482=ORIENTED_EDGE ( 'NONE', *, *, #14680, .F. ) ;
#4492=DIRECTION ( 'NONE',  ( 1.000000000000000000, -8.574039729943018344E-17, -0.000000000000000000 ) ) ;
#4501=CARTESIAN_POINT ( 'NONE',  ( 20.98500000273118715, -0.2613211581691358698, -2.486304738420681559 ) ) ;
#4505=CARTESIAN_POINT ( 'NONE',  ( 25.04750000136559507, -1.913930629741527500, 2.363507492473149618 ) ) ;
#4507=CARTESIAN_POINT ( 'NONE',  ( 25.75999999999998380, 2.578868840510358584, 1.660716374619295443 ) ) ;
#4515=EDGE_CURVE ( 'NONE', #18559, #11672, #16979, .T. ) ;
#4520=LINE ( 'NONE', #6833, #11910 ) ;
#4522=CARTESIAN_POINT ( 'NONE',  ( 25.73500000136559507, 3.156283516753366047, 0.9349337715887203748 ) ) ;
#4525=ORIENTED_EDGE ( 'NONE', *, *, #10065, .T. ) ;
#4550=( NAMED_UNIT ( * ) SI_UNIT ( $, .STERADIAN. ) SOLID_ANGLE_UNIT ( ) );
#4558=ORIENTED_EDGE ( 'NONE', *, *, #30929, .T. ) ;
#4559=DIRECTION ( 'NONE',  ( 1.000000000000000000, -0.000000000000000000, -0.000000000000000000 ) ) ;
#4566=CARTESIAN_POINT ( 'NONE',  ( 5.338982705821348503E-17, 0.6226916219172716760, -4.971152295393295617 ) ) ;
#4577=DIRECTION ( 'NONE',  ( 0.000000000000000000, 0.000000000000000000, -1.000000000000000000 ) ) ;
#4582=EDGE_CURVE ( 'NONE', #16032, #15630, #18325, .T. ) ;
#4584=CARTESIAN_POINT ( 'NONE',  ( 25.00111451137534146, -4.139597703811366476E-17, -2.499999999999998668 ) ) ;
#4588=ORIENTED_EDGE ( 'NONE', *, *, #10902, .F. ) ;
#4594=CARTESIAN_POINT ( 'NONE',  ( 23.54750000136559507, 3.024605502323846729, -0.3178988483021056854 ) ) ;
#4601=CARTESIAN_POINT ( 'NONE',  ( 23.73500000136559152, 1.570731468192929858, 2.892927487894329186 ) ) ;
#4608=DIRECTION ( 'NONE',  ( 0.000000000000000000, 1.000000000000000000, 0.000000000000000000 ) ) ;
#4614=VERTEX_POINT ( 'NONE', #11112 ) ;
#4618=CARTESIAN_POINT ( 'NONE',  ( 10.00000000000000178, -8.574039729943018837E-16, 0.000000000000000000 ) ) ;
#4631=DIRECTION ( 'NONE',  ( -1.000000000000000000, 8.574039729943018344E-17, -0.000000000000000000 ) ) ;
#4634=LINE ( 'NONE', #1973, #20469 ) ;
#4639=CARTESIAN_POINT ( 'NONE',  ( 10.00000000000000000, 0.8254815157535864145, -4.681538312723508177 ) ) ;
#4641=CARTESIAN_POINT ( 'NONE',  ( 10.56870887191539587, -4.787500056513379398, 1.476463073999619846 ) ) ;
#4646=PLANE ( 'NONE',  #7067 ) ;
#4647=VERTEX_POINT ( 'NONE', #31511 ) ;
#4648=EDGE_CURVE ( 'NONE', #1423, #21855, #28390, .T. ) ;
#4672=ADVANCED_FACE ( 'NONE', ( #26505 ), #29168, .F. ) ;
#4673=CARTESIAN_POINT ( 'NONE',  ( 23.54750000136559862, 1.913930629741522838, -2.363507492473150062 ) ) ;
#4676=ORIENTED_EDGE ( 'NONE', *, *, #12412, .T. ) ;
#4688=EDGE_CURVE ( 'NONE', #27483, #32821, #16295, .T. ) ;
#4689=EDGE_CURVE ( 'NONE', #31644, #3406, #6584, .T. ) ;
#4698=EDGE_CURVE ( 'NONE', #285, #16126, #4095, .T. ) ;
#4700=ORIENTED_EDGE ( 'NONE', *, *, #31970, .T. ) ;
#4703=CARTESIAN_POINT ( 'NONE',  ( 10.00000000000000000, -4.116875700062099241, 2.376879293651050329 ) ) ;
#4706=( BOUNDED_CURVE ( )  B_SPLINE_CURVE ( 2, ( #25489, #5265, #15439, #24776, #32818, #11721, #14882, #12387, #9538, #26958, #17059 ),
 .UNSPECIFIED., .F., .F. ) 
 B_SPLINE_CURVE_WITH_KNOTS ( ( 3, 2, 2, 2, 2, 3 ),
 ( 0.4966116191895003640, 0.5000000000000000000, 0.5250000000000000222, 0.5500000000000000444, 0.5749999999999999556, 0.5966116191895003418 ),
 .UNSPECIFIED. ) 
 CURVE ( )  GEOMETRIC_REPRESENTATION_ITEM ( )  RATIONAL_B_SPLINE_CURVE ( ( 0.9821626249036858880, 0.9896829947469992783, 1.000000000000000000, 0.9238795325112867385, 1.000000000000000000, 0.9238795325112867385, 1.000000000000000000, 0.9238795325112867385, 1.000000000000000000, 0.9341965377642874602, 0.9821626249036858880 ) ) 
 REPRESENTATION_ITEM ( '' )  );
#4712=ORIENTED_EDGE ( 'NONE', *, *, #18621, .T. ) ;
#4715=CARTESIAN_POINT ( 'NONE',  ( 22.42250000273118715, 1.291182301015469047, 2.378061970571981654 ) ) ;
#4726=CARTESIAN_POINT ( 'NONE',  ( 23.04750000136559862, -3.024605502323851169, 0.3178988483021052969 ) ) ;
#4727=ADVANCED_FACE ( 'NONE', ( #12748 ), #2250, .F. ) ;
#4732=CARTESIAN_POINT ( 'NONE',  ( 2.037945749704362236E-16, 2.376879293651122271, -4.116875700062057497 ) ) ;
#4735=ORIENTED_EDGE ( 'NONE', *, *, #381, .T. ) ;
#4743=EDGE_CURVE ( 'NONE', #12746, #1423, #7913, .T. ) ;
#4774=DIRECTION ( 'NONE',  ( 8.281886410780533213E-17, 0.9659258262890707547, -0.2588190451025115246 ) ) ;
#4788=FACE_OUTER_BOUND ( 'NONE', #19682, .T. ) ;
#4795=DIRECTION ( 'NONE',  ( 0.000000000000000000, 1.000000000000000000, 0.000000000000000000 ) ) ;
#4828=CARTESIAN_POINT ( 'NONE',  ( 22.79750000136559862, 2.363507492473148286, 1.913930629741525058 ) ) ;
#4840=VERTEX_POINT ( 'NONE', #15603 ) ;
#4841=CARTESIAN_POINT ( 'NONE',  ( -4.013969549054180728E-16, -4.681538312723511730, -0.8254815157535732029 ) ) ;
#4845=LINE ( 'NONE', #20578, #19392 ) ;
#4859=CARTESIAN_POINT ( 'NONE',  ( 10.00000000000000000, -3.993798362933289159, -3.024842911000733547 ) ) ;
#4866=AXIS2_PLACEMENT_3D ( 'NONE', #21984, #11779, #29690 ) ;
#4868=EDGE_CURVE ( 'NONE', #12161, #20071, #2746, .T. ) ;
#4869=CIRCLE ( 'NONE', #22480, 5.010000000000000675 ) ;
#4870=EDGE_CURVE ( 'NONE', #27483, #20748, #10925, .T. ) ;
#4874=CARTESIAN_POINT ( 'NONE',  ( 2.619932554246601438E-16, 3.055657119358849982, -3.641590349731898879 ) ) ;
#4889=CARTESIAN_POINT ( 'NONE',  ( 23.67250000136559507, 2.363507492473148286, 1.913930629741525058 ) ) ;
#4900=AXIS2_PLACEMENT_3D ( 'NONE', #23685, #23836, #26376 ) ;
#4905=DIRECTION ( 'NONE',  ( -1.000000000000000000, 8.574039729943018344E-17, -0.000000000000000000 ) ) ;
#4907=ORIENTED_EDGE ( 'NONE', *, *, #22837, .F. ) ;
#4910=EDGE_CURVE ( 'NONE', #15944, #31503, #7577, .T. ) ;
#4913=VECTOR ( 'NONE', #23708, 1000.000000000000114 ) ;
#4921=EDGE_CURVE ( 'NONE', #31196, #16940, #5595, .T. ) ;
#4922=ADVANCED_FACE ( 'NONE', ( #26471 ), #550, .T. ) ;
#4926=ORIENTED_EDGE ( 'NONE', *, *, #27007, .T. ) ;
#4938=EDGE_CURVE ( 'NONE', #32336, #264, #1714, .T. ) ;
#4958=VECTOR ( 'NONE', #8904, 1000.000000000000114 ) ;
#4964=ORIENTED_EDGE ( 'NONE', *, *, #15500, .T. ) ;
#4971=DIRECTION ( 'NONE',  ( -8.541412920197207489E-17, -0.9961946980917444350, -0.08715574274767159957 ) ) ;
#4972=FACE_OUTER_BOUND ( 'NONE', #31095, .T. ) ;
#4975=DIRECTION ( 'NONE',  ( 0.000000000000000000, 0.08715574274766134388, -0.9961946980917452121 ) ) ;
#4979=DIRECTION ( 'NONE',  ( 0.000000000000000000, 0.4226182617406968878, 0.9063077870366511579 ) ) ;
#4984=AXIS2_PLACEMENT_3D ( 'NONE', #11667, #16507, #11174 ) ;
#4994=CARTESIAN_POINT ( 'NONE',  ( 21.61000000136559507, 2.892927487894327410, -1.570731468192931635 ) ) ;
#4999=EDGE_CURVE ( 'NONE', #15334, #25541, #3088, .T. ) ;
#5000=CARTESIAN_POINT ( 'NONE',  ( 4.104821569165022408E-16, 4.787500056513387392, -1.476463073999588538 ) ) ;
#5001=EDGE_CURVE ( 'NONE', #17100, #6901, #29461, .T. ) ;
#5003=LINE ( 'NONE', #15186, #15453 ) ;
#5006=EDGE_CURVE ( 'NONE', #5447, #30423, #21275, .T. ) ;
#5008=VECTOR ( 'NONE', #8875, 1000.000000000000000 ) ;
#5017=PRODUCT_DEFINITION_FORMATION_WITH_SPECIFIED_SOURCE ( 'ANY', '', #5241, .NOT_KNOWN. ) ;
#5020=CARTESIAN_POINT ( 'NONE',  ( 24.54750000136559507, 1.913930629741522838, -2.363507492473150062 ) ) ;
#5023=ORIENTED_EDGE ( 'NONE', *, *, #5122, .F. ) ;
#5025=CARTESIAN_POINT ( 'NONE',  ( 10.00000000000000178, -8.574039729943018837E-16, 0.000000000000000000 ) ) ;
#5026=CARTESIAN_POINT ( 'NONE',  ( 10.52034268205830259, 3.993798362933308255, 3.024842911000705570 ) ) ;
#5027=DIRECTION ( 'NONE',  ( 8.281886410780493770E-17, 0.9659258262890664248, 0.2588190451025276784 ) ) ;
#5035=CARTESIAN_POINT ( 'NONE',  ( 22.61000000136559507, 2.892927487894327410, -1.570731468192931635 ) ) ;
#5042=CARTESIAN_POINT ( 'NONE',  ( 25.75999999999999801, -2.208672634433321348E-15, 0.000000000000000000 ) ) ;
#5048=CIRCLE ( 'NONE', #21597, 5.010000000000000675 ) ;
#5049=VERTEX_POINT ( 'NONE', #15918 ) ;
#5053=ORIENTED_EDGE ( 'NONE', *, *, #23741, .T. ) ;
#5059=ORIENTED_EDGE ( 'NONE', *, *, #23, .T. ) ;
#5070=CARTESIAN_POINT ( 'NONE',  ( 21.17250000136559507, -2.363507492473152283, -1.913930629741525280 ) ) ;
#5071=DIRECTION ( 'NONE',  ( 0.000000000000000000, 1.000000000000000000, 0.000000000000000000 ) ) ;
#5086=ADVANCED_FACE ( 'NONE', ( #12176 ), #26777, .F. ) ;
#5091=DIRECTION ( 'NONE',  ( 0.000000000000000000, 0.9961946980917455452, -0.08715574274765799934 ) ) ;
#5119=ORIENTED_EDGE ( 'NONE', *, *, #21285, .F. ) ;
#5122=EDGE_CURVE ( 'NONE', #15836, #30672, #16564, .T. ) ;
#5123=ORIENTED_EDGE ( 'NONE', *, *, #25553, .F. ) ;
#5136=PLANE ( 'NONE',  #6363 ) ;
#5141=CARTESIAN_POINT ( 'NONE',  ( 21.29750000273119070, 2.594547506269380133, 0.7685399846772031918 ) ) ;
#5142=CARTESIAN_POINT ( 'NONE',  ( 10.00000000000000000, 3.055657119358800244, 3.641590349731939735 ) ) ;
#5155=CARTESIAN_POINT ( 'NONE',  ( 22.73500000136559862, 3.156283516753366047, 0.9349337715887203748 ) ) ;
#5161=ORIENTED_EDGE ( 'NONE', *, *, #32082, .F. ) ;
#5168=DIRECTION ( 'NONE',  ( 0.000000000000000000, 0.9659258262890682012, -0.2588190451025209060 ) ) ;
#5172=CARTESIAN_POINT ( 'NONE',  ( 22.36000000136559152, -1.570731468192933633, -2.892927487894330074 ) ) ;
#5179=CARTESIAN_POINT ( 'NONE',  ( 21.92249999999999943, 2.378061970571979433, -1.291182301015470602 ) ) ;
#5185=FACE_OUTER_BOUND ( 'NONE', #28644, .T. ) ;
#5187=CARTESIAN_POINT ( 'NONE',  ( 21.04750000136559507, -1.913930629741527500, 2.363507492473149618 ) ) ;
#5189=LINE ( 'NONE', #7858, #14553 ) ;
#5195=CARTESIAN_POINT ( 'NONE',  ( 0.000000000000000000, 0.000000000000000000, 0.000000000000000000 ) ) ;
#5198=VERTEX_POINT ( 'NONE', #15005 ) ;
#5203=ORIENTED_EDGE ( 'NONE', *, *, #17005, .F. ) ;
#5204=VERTEX_POINT ( 'NONE', #4335 ) ;
#5215=CARTESIAN_POINT ( 'NONE',  ( 23.92250000136559507, -1.913930629741527500, 2.363507492473149618 ) ) ;
#5216=CARTESIAN_POINT ( 'NONE',  ( 10.57125986779756843, -0.8254815157535575487, 4.681538312723514395 ) ) ;
#5223=CARTESIAN_POINT ( 'NONE',  ( 21.42250000136559507, 1.913930629741522838, -2.363507492473150062 ) ) ;
#5232=FACE_OUTER_BOUND ( 'NONE', #3929, .T. ) ;
#5237=VERTEX_POINT ( 'NONE', #22376 ) ;
#5239=ORIENTED_EDGE ( 'NONE', *, *, #19818, .T. ) ;
#5241=PRODUCT ( 'Part5_knurlingConnector', 'Part5_knurlingConnector', '', ( #20896 ) ) ;
#5248=EDGE_CURVE ( 'NONE', #20824, #12746, #32592, .T. ) ;
#5251=CARTESIAN_POINT ( 'NONE',  ( 10.00000000000000000, -3.641590349731950393, 3.055657119358789142 ) ) ;
#5262=CARTESIAN_POINT ( 'NONE',  ( 10.00000000000000000, 1.625881193364757449, -4.467071865485455540 ) ) ;
#5265=CARTESIAN_POINT ( 'NONE',  ( 23.74290772321994325, -0.1310194482076047495, -2.499999999999998668 ) ) ;
#5269=DIRECTION ( 'NONE',  ( -6.062761635205574522E-17, -0.7071067811865465735, 0.7071067811865484609 ) ) ;
#5288=EDGE_LOOP ( 'NONE', ( #6593, #1502, #30752, #18414 ) ) ;
#5290=CARTESIAN_POINT ( 'NONE',  ( -1.668773398854329396E-16, -1.946309384392623576, 4.616489984850525197 ) ) ;
#5314=AXIS2_PLACEMENT_3D ( 'NONE', #23939, #28651, #21445 ) ;
#5315=ADVANCED_FACE ( 'NONE', ( #8328 ), #3326, .F. ) ;
#5317=ORIENTED_EDGE ( 'NONE', *, *, #10004, .T. ) ;
#5322=DIRECTION ( 'NONE',  ( -1.000000000000000000, 8.574039729943018344E-17, 0.000000000000000000 ) ) ;
#5325=ORIENTED_EDGE ( 'NONE', *, *, #6925, .F. ) ;
#5332=VECTOR ( 'NONE', #11794, 1000.000000000000114 ) ;
#5334=VERTEX_POINT ( 'NONE', #5976 ) ;
#5341=VERTEX_POINT ( 'NONE', #967 ) ;
#5345=DIRECTION ( 'NONE',  ( 6.062761635205570824E-17, 0.7071067811865460184, 0.7071067811865490160 ) ) ;
#5351=ORIENTED_EDGE ( 'NONE', *, *, #14019, .T. ) ;
#5370=CARTESIAN_POINT ( 'NONE',  ( 22.00111451137534502, -1.241879311143409511E-16, -2.499999999999998668 ) ) ;
#5375=CARTESIAN_POINT ( 'NONE',  ( 23.61000000136559507, 3.156283516753366047, 0.9349337715887203748 ) ) ;
#5377=DIRECTION ( 'NONE',  ( 7.023442172597869187E-17, 0.8191520442889931308, -0.5735764363510441610 ) ) ;
#5383=DIRECTION ( 'NONE',  ( 0.000000000000000000, 1.000000000000000000, 0.000000000000000000 ) ) ;
#5384=CARTESIAN_POINT ( 'NONE',  ( 20.86000000136559507, -0.9349337715887248157, 3.156283516753367824 ) ) ;
#5394=ORIENTED_EDGE ( 'NONE', *, *, #4688, .T. ) ;
#5426=CARTESIAN_POINT ( 'NONE',  ( 10.00000000000000178, 1.946309384392655994, -4.616489984850514539 ) ) ;
#5432=AXIS2_PLACEMENT_3D ( 'NONE', #25906, #10660, #21205 ) ;
#5434=AXIS2_PLACEMENT_3D ( 'NONE', #15109, #12107, #33009 ) ;
#5436=DIRECTION ( 'NONE',  ( -4.917867153432966982E-17, -0.5735764363510419406, -0.8191520442889946851 ) ) ;
#5442=CARTESIAN_POINT ( 'NONE',  ( 25.25913793397114304, -0.3481264064496775723, 2.506178704810730018 ) ) ;
#5447=VERTEX_POINT ( 'NONE', #8959 ) ;
#5452=ORIENTED_EDGE ( 'NONE', *, *, #30008, .T. ) ;
#5453=VERTEX_POINT ( 'NONE', #3645 ) ;
#5455=AXIS2_PLACEMENT_3D ( 'NONE', #31871, #8939, #17315 ) ;
#5463=DIRECTION ( 'NONE',  ( -7.023442172597914793E-17, -0.8191520442889983489, 0.5735764363510366115 ) ) ;
#5475=AXIS2_PLACEMENT_3D ( 'NONE', #12006, #4309, #27546 ) ;
#5483=AXIS2_PLACEMENT_3D ( 'NONE', #21255, #19075, #24253 ) ;
#5498=AXIS2_PLACEMENT_3D ( 'NONE', #21234, #5839, #16024 ) ;
#5499=EDGE_LOOP ( 'NONE', ( #12565, #24807, #26354 ) ) ;
#5506=CARTESIAN_POINT ( 'NONE',  ( 25.24177585798616974, 0.08698857045690901180, 2.506775857986155209 ) ) ;
#5510=VECTOR ( 'NONE', #14204, 1000.000000000000000 ) ;
#5515=EDGE_CURVE ( 'NONE', #28105, #18235, #24498, .T. ) ;
#5520=DIRECTION ( 'NONE',  ( 8.574039729943018344E-17, 1.000000000000000000, 0.000000000000000000 ) ) ;
#5526=CARTESIAN_POINT ( 'NONE',  ( 1.959487840848961122E-16, 2.285372942705017341, -4.458382051008168645 ) ) ;
#5528=CARTESIAN_POINT ( 'NONE',  ( 23.98500000136559507, -0.9349337715887247047, 3.156283516753367824 ) ) ;
#5531=DIRECTION ( 'NONE',  ( 0.000000000000000000, 1.000000000000000000, 0.000000000000000000 ) ) ;
#5553=DIRECTION ( 'NONE',  ( -7.023442172597867955E-17, -0.8191520442889927978, 0.5735764363510447161 ) ) ;
#5555=EDGE_CURVE ( 'NONE', #4411, #24998, #6952, .T. ) ;
#5572=CARTESIAN_POINT ( 'NONE',  ( 22.17250000136559507, -2.363507492473152283, -1.913930629741525280 ) ) ;
#5583=LINE ( 'NONE', #7569, #16200 ) ;
#5593=ORIENTED_EDGE ( 'NONE', *, *, #25518, .F. ) ;
#5595=LINE ( 'NONE', #13883, #16631 ) ;
#5612=ADVANCED_FACE ( 'NONE', ( #24852 ), #7295, .F. ) ;
#5616=CARTESIAN_POINT ( 'NONE',  ( -9.560873106161779341E-17, -1.115095498423275266, -4.884328206559847452 ) ) ;
#5617=ADVANCED_FACE ( 'NONE', ( #4788 ), #1970, .T. ) ;
#5625=ORIENTED_EDGE ( 'NONE', *, *, #7930, .T. ) ;
#5631=DIRECTION ( 'NONE',  ( -8.281886410780525818E-17, -0.9659258262890700886, 0.2588190451025141336 ) ) ;
#5641=DIRECTION ( 'NONE',  ( 0.000000000000000000, -0.9659258262890646485, -0.2588190451025343397 ) ) ;
#5644=ADVANCED_FACE ( 'NONE', ( #4972 ), #27364, .F. ) ;
#5662=DIRECTION ( 'NONE',  ( 0.000000000000000000, 0.8191520442889912434, -0.5735764363510469366 ) ) ;
#5664=EDGE_CURVE ( 'NONE', #32100, #32058, #14655, .T. ) ;
#5665=ORIENTED_EDGE ( 'NONE', *, *, #25084, .F. ) ;
#5685=CARTESIAN_POINT ( 'NONE',  ( 10.00000000000000000, 3.055657119358800244, 3.641590349731939735 ) ) ;
#5712=CARTESIAN_POINT ( 'NONE',  ( 10.00000000000000178, -8.574039729943018837E-16, 0.000000000000000000 ) ) ;
#5718=CARTESIAN_POINT ( 'NONE',  ( 24.92250000273118360, -1.291182301015472378, -2.378061970571982098 ) ) ;
#5720=LINE ( 'NONE', #16540, #20989 ) ;
#5728=DIRECTION ( 'NONE',  ( 7.023442172597789069E-17, 0.8191520442889833609, 0.5735764363510581498 ) ) ;
#5740=CARTESIAN_POINT ( 'NONE',  ( 10.00000000000000178, -8.574039729943018837E-16, 0.000000000000000000 ) ) ;
#5741=EDGE_CURVE ( 'NONE', #13056, #2105, #28347, .T. ) ;
#5745=ORIENTED_EDGE ( 'NONE', *, *, #22060, .F. ) ;
#5754=CARTESIAN_POINT ( 'NONE',  ( 10.57125986779756843, 1.115095498423307463, 4.884328206559839458 ) ) ;
#5758=LINE ( 'NONE', #15937, #13476 ) ;
#5760=DIRECTION ( 'NONE',  ( 0.000000000000000000, 0.8191520442889946851, -0.5735764363510419406 ) ) ;
#5762=CARTESIAN_POINT ( 'NONE',  ( 21.92250000136559507, 0.3178988483021036315, 3.024605502323848949 ) ) ;
#5763=ADVANCED_FACE ( 'NONE', ( #7637 ), #5136, .F. ) ;
#5774=VERTEX_POINT ( 'NONE', #5290 ) ;
#5783=EDGE_CURVE ( 'NONE', #19432, #15936, #3130, .T. ) ;
#5784=FACE_OUTER_BOUND ( 'NONE', #22974, .T. ) ;
#5793=CARTESIAN_POINT ( 'NONE',  ( 24.25111450864415730, -3.256483526998273983E-15, 2.499999999999998668 ) ) ;
#5803=CARTESIAN_POINT ( 'NONE',  ( 23.50111451137534857, -3.256483526998273983E-15, 2.499999999999998668 ) ) ;
#5809=DIRECTION ( 'NONE',  ( 0.000000000000000000, -0.9063077870366526012, 0.4226182617406938902 ) ) ;
#5811=ORIENTED_EDGE ( 'NONE', *, *, #28212, .F. ) ;
#5818=CARTESIAN_POINT ( 'NONE',  ( -2.593512329575665296E-16, -3.024842911000718448, 3.993798362933297597 ) ) ;
#5839=DIRECTION ( 'NONE',  ( 1.000000000000000000, -0.000000000000000000, -0.000000000000000000 ) ) ;
#5848=ORIENTED_EDGE ( 'NONE', *, *, #21813, .T. ) ;
#5853=CARTESIAN_POINT ( 'NONE',  ( 21.42250000136559507, 1.913930629741522838, -2.363507492473150062 ) ) ;
#5858=CARTESIAN_POINT ( 'NONE',  ( 22.73500000273118715, -2.486304738420683780, 0.2613211581691335383 ) ) ;
#5859=EDGE_CURVE ( 'NONE', #23691, #32336, #23827, .T. ) ;
#5865=AXIS2_PLACEMENT_3D ( 'NONE', #7763, #28141, #5091 ) ;
#5868=ORIENTED_EDGE ( 'NONE', *, *, #18571, .F. ) ;
#5871=CARTESIAN_POINT ( 'NONE',  ( -2.619932554246580731E-16, -3.055657119358825557, 3.641590349731918863 ) ) ;
#5882=ORIENTED_EDGE ( 'NONE', *, *, #4910, .F. ) ;
#5911=CARTESIAN_POINT ( 'NONE',  ( 24.23500000136559507, -3.156283516753370044, -0.9349337715887220401 ) ) ;
#5914=CARTESIAN_POINT ( 'NONE',  ( 25.37609862591745369, -2.542614276119973038, 0.7358597233275829819 ) ) ;
#5919=EDGE_CURVE ( 'NONE', #17341, #19305, #1278, .T. ) ;
#5926=VERTEX_POINT ( 'NONE', #3613 ) ;
#5935=CARTESIAN_POINT ( 'NONE',  ( 10.00000000000000178, -3.993798362933331791, 3.024842911000678924 ) ) ;
#5944=CARTESIAN_POINT ( 'NONE',  ( 25.75999999999999801, -2.208672634433321348E-15, 0.000000000000000000 ) ) ;
#5947=AXIS2_PLACEMENT_3D ( 'NONE', #11403, #8394, #21601 ) ;
#5960=DIRECTION ( 'NONE',  ( 0.000000000000000000, 0.000000000000000000, -1.000000000000000000 ) ) ;
#5963=CARTESIAN_POINT ( 'NONE',  ( 20.48500000273118715, 0.2613211581691317065, 2.486304738420681559 ) ) ;
#5964=CIRCLE ( 'NONE', #15022, 5.010000000000000675 ) ;
#5976=CARTESIAN_POINT ( 'NONE',  ( 10.00000000000000000, -0.8254815157535566605, 4.681538312723513506 ) ) ;
#5981=CARTESIAN_POINT ( 'NONE',  ( 21.29750000136559507, -2.363507492473152283, -1.913930629741525280 ) ) ;
#5987=CARTESIAN_POINT ( 'NONE',  ( 10.00000000000000000, -4.458382051008177527, -2.285372942705001797 ) ) ;
#5989=VECTOR ( 'NONE', #1482, 1000.000000000000000 ) ;
#5991=ORIENTED_EDGE ( 'NONE', *, *, #3260, .F. ) ;
#5994=DIRECTION ( 'NONE',  ( -1.000000000000000000, 8.574039729943017111E-17, -0.000000000000000000 ) ) ;
#5997=DIRECTION ( 'NONE',  ( -1.000000000000000000, 8.574039729943018344E-17, -0.000000000000000000 ) ) ;
#5999=EDGE_CURVE ( 'NONE', #30211, #22618, #32519, .T. ) ;
#6011=VECTOR ( 'NONE', #7372, 1000.000000000000000 ) ;
#6020=VERTEX_POINT ( 'NONE', #19801 ) ;
#6033=B_SPLINE_CURVE_WITH_KNOTS ( 'NONE', 3,
 ( #22050, #27208, #9149, #21710, #4507, #24881 ),
 .UNSPECIFIED., .F., .F.,
 ( 4, 2, 4 ),
 ( 3.736708725176135323E-17, 0.001196153005899993748, 0.002392306011799950199 ),
 .UNSPECIFIED. ) ;
#6038=EDGE_CURVE ( 'NONE', #28338, #7332, #6762, .T. ) ;
#6057=CARTESIAN_POINT ( 'NONE',  ( 10.00000000000000000, -3.641590349731950393, 3.055657119358789142 ) ) ;
#6064=ORIENTED_EDGE ( 'NONE', *, *, #16968, .T. ) ;
#6065=DIRECTION ( 'NONE',  ( 7.023442172597900002E-17, 0.8191520442889966835, -0.5735764363510392760 ) ) ;
#6070=VECTOR ( 'NONE', #22048, 1000.000000000000000 ) ;
#6071=AXIS2_PLACEMENT_3D ( 'NONE', #2967, #13123, #28669 ) ;
#6074=LINE ( 'NONE', #1045, #4300 ) ;
#6100=CARTESIAN_POINT ( 'NONE',  ( 25.31491971536988927, -1.639151784509444987, 1.999968332672603877 ) ) ;
#6110=ORIENTED_EDGE ( 'NONE', *, *, #7356, .F. ) ;
#6115=AXIS2_PLACEMENT_3D ( 'NONE', #24329, #11967, #26520 ) ;
#6116=LINE ( 'NONE', #3462, #3749 ) ;
#6120=DIRECTION ( 'NONE',  ( -1.000000000000000000, 8.574039729943018344E-17, -0.000000000000000000 ) ) ;
#6128=DIRECTION ( 'NONE',  ( 1.000000000000000000, -8.574039729943018344E-17, -0.000000000000000000 ) ) ;
#6130=CARTESIAN_POINT ( 'NONE',  ( 24.10999999999999943, 1.942864903642424146, 1.573300977624592534 ) ) ;
#6135=ORIENTED_EDGE ( 'NONE', *, *, #21668, .F. ) ;
#6150=FACE_OUTER_BOUND ( 'NONE', #32449, .T. ) ;
#6160=EDGE_CURVE ( 'NONE', #21430, #32821, #15112, .T. ) ;
#6165=DIRECTION ( 'NONE',  ( -7.770718973608931818E-17, -0.9063077870366451627, -0.4226182617407097108 ) ) ;
#6168=LINE ( 'NONE', #16354, #29534 ) ;
#6169=( BOUNDED_SURFACE ( )  B_SPLINE_SURFACE ( 1, 2, ( 
 ( #14826, #29738, #25025, #14984, #25204, #17004, #27206, #2140, #4318, #2327, #22715, #14496, #1990, #17182, #4505, #12163, #22361, #26156, #8427, #12659, #20983, #31203, #3263, #18620, #17860, #920, #11098, #5911, #15330, #22862, #33064, #15178, #28815, #28667, #7468, #3442, #26004, #3112, #7661, #27880, #8282, #10949, #30578, #18475, #13425, #20198, #2490, #21151, #13267, #20360, #15941, #5155, #28058, #23471, #580, #16104, #31350, #26336, #13601, #17668, #25382, #10769, #23806, #9987, #5762, #32918, #23644, #767, #30394, #4994, #10139, #23271, #24636, #10399, #12883, #7104, #17926, #7883, #28117, #1767, #24974 ),
 ( #12262, #2708, #374, #20609, #9771, #10548, #2087, #11962, #30815, #7734, #32521, #22472, #19646, #18075, #29685, #9583, #6764, #19803, #15391, #22159, #32689, #23102, #24821, #19993, #25599, #16954, #29840, #223, #17305, #14620, #5215, #30011, #27501, #4601, #14776, #5375, #28268, #15563, #25780, #32370, #9429, #30657, #13070, #27151, #2907, #4254, #14427, #6917, #17113, #27324, #4444, #1940, #12113, #22310, #3546, #31301, #8523, #31614, #18726, #25948, #16036, #24059, #18917, #13705, #15746, #23906, #1014, #13549, #18570, #11198, #5853, #28452, #8041, #13214, #28762, #10705, #21406, #28930, #26267, #3382, #26448 ) ),
 .UNSPECIFIED., .F., .F., .F. ) 
 B_SPLINE_SURFACE_WITH_KNOTS ( ( 2, 2 ),
 ( 3, 2, 2, 2, 2, 2, 2, 2, 2, 2, 2, 2, 2, 2, 2, 2, 2, 2, 2, 2, 2, 2, 2, 2, 2, 2, 2, 2, 2, 2, 2, 2, 2, 2, 2, 2, 2, 2, 2, 2, 3 ),
 ( 0.000000000000000000, 1.000000000000000000 ),
 ( 0.000000000000000000, 0.02500000000000000139, 0.05000000000000000278, 0.07499999999999999722, 0.1000000000000000056, 0.1250000000000000000, 0.1499999999999999944, 0.1749999999999999889, 0.2000000000000000111, 0.2250000000000000056, 0.2500000000000000000, 0.2750000000000000222, 0.2999999999999999889, 0.3250000000000000111, 0.3499999999999999778, 0.3750000000000000000, 0.4000000000000000222, 0.4249999999999999889, 0.4500000000000000111, 0.4749999999999999778, 0.5000000000000000000, 0.5250000000000000222, 0.5500000000000000444, 0.5749999999999999556, 0.5999999999999999778, 0.6250000000000000000, 0.6500000000000000222, 0.6750000000000000444, 0.6999999999999999556, 0.7249999999999999778, 0.7500000000000000000, 0.7750000000000000222, 0.8000000000000000444, 0.8249999999999999556, 0.8499999999999999778, 0.8750000000000000000, 0.9000000000000000222, 0.9250000000000000444, 0.9499999999999999556, 0.9749999999999999778, 1.000000000000000000 ),
 .UNSPECIFIED. ) 
 GEOMETRIC_REPRESENTATION_ITEM ( )  RATIONAL_B_SPLINE_SURFACE ( (
 ( 1.000000000000000000, 0.9238795325112867385, 1.000000000000000000, 0.9238795325112867385, 1.000000000000000000, 0.9238795325112867385, 1.000000000000000000, 0.9238795325112867385, 1.000000000000000000, 0.9238795325112867385, 1.000000000000000000, 0.9238795325112867385, 1.000000000000000000, 0.9238795325112867385, 1.000000000000000000, 0.9238795325112867385, 1.000000000000000000, 0.9238795325112867385, 1.000000000000000000, 0.9238795325112867385, 1.000000000000000000, 0.9238795325112867385, 1.000000000000000000, 0.9238795325112867385, 1.000000000000000000, 0.9238795325112867385, 1.000000000000000000, 0.9238795325112867385, 1.000000000000000000, 0.9238795325112867385, 1.000000000000000000, 0.9238795325112867385, 1.000000000000000000, 0.9238795325112867385, 1.000000000000000000, 0.9238795325112867385, 1.000000000000000000, 0.9238795325112867385, 1.000000000000000000, 0.9238795325112867385, 1.000000000000000000, 0.9238795325112867385, 1.000000000000000000, 0.9238795325112867385, 1.000000000000000000, 0.9238795325112867385, 1.000000000000000000, 0.9238795325112867385, 1.000000000000000000, 0.9238795325112867385, 1.000000000000000000, 0.9238795325112867385, 1.000000000000000000, 0.9238795325112867385, 1.000000000000000000, 0.9238795325112867385, 1.000000000000000000, 0.9238795325112867385, 1.000000000000000000, 0.9238795325112867385, 1.000000000000000000, 0.9238795325112867385, 1.000000000000000000, 0.9238795325112867385, 1.000000000000000000, 0.9238795325112867385, 1.000000000000000000, 0.9238795325112867385, 1.000000000000000000, 0.9238795325112867385, 1.000000000000000000, 0.9238795325112867385, 1.000000000000000000, 0.9238795325112867385, 1.000000000000000000, 0.9238795325112867385, 1.000000000000000000, 0.9238795325112867385, 1.000000000000000000, 0.9238795325112867385, 1.000000000000000000),
 ( 1.000000000000000000, 0.9238795325112867385, 1.000000000000000000, 0.9238795325112867385, 1.000000000000000000, 0.9238795325112867385, 1.000000000000000000, 0.9238795325112867385, 1.000000000000000000, 0.9238795325112867385, 1.000000000000000000, 0.9238795325112867385, 1.000000000000000000, 0.9238795325112867385, 1.000000000000000000, 0.9238795325112867385, 1.000000000000000000, 0.9238795325112867385, 1.000000000000000000, 0.9238795325112867385, 1.000000000000000000, 0.9238795325112867385, 1.000000000000000000, 0.9238795325112867385, 1.000000000000000000, 0.9238795325112867385, 1.000000000000000000, 0.9238795325112867385, 1.000000000000000000, 0.9238795325112867385, 1.000000000000000000, 0.9238795325112867385, 1.000000000000000000, 0.9238795325112867385, 1.000000000000000000, 0.9238795325112867385, 1.000000000000000000, 0.9238795325112867385, 1.000000000000000000, 0.9238795325112867385, 1.000000000000000000, 0.9238795325112867385, 1.000000000000000000, 0.9238795325112867385, 1.000000000000000000, 0.9238795325112867385, 1.000000000000000000, 0.9238795325112867385, 1.000000000000000000, 0.9238795325112867385, 1.000000000000000000, 0.9238795325112867385, 1.000000000000000000, 0.9238795325112867385, 1.000000000000000000, 0.9238795325112867385, 1.000000000000000000, 0.9238795325112867385, 1.000000000000000000, 0.9238795325112867385, 1.000000000000000000, 0.9238795325112867385, 1.000000000000000000, 0.9238795325112867385, 1.000000000000000000, 0.9238795325112867385, 1.000000000000000000, 0.9238795325112867385, 1.000000000000000000, 0.9238795325112867385, 1.000000000000000000, 0.9238795325112867385, 1.000000000000000000, 0.9238795325112867385, 1.000000000000000000, 0.9238795325112867385, 1.000000000000000000, 0.9238795325112867385, 1.000000000000000000, 0.9238795325112867385, 1.000000000000000000) ) ) 
 REPRESENTATION_ITEM ( '' )  SURFACE ( )  );
#6188=EDGE_CURVE ( 'NONE', #502, #18404, #23462, .T. ) ;
#6207=ORIENTED_EDGE ( 'NONE', *, *, #1258, .T. ) ;
#6224=LINE ( 'NONE', #16408, #8614 ) ;
#6236=CARTESIAN_POINT ( 'NONE',  ( 10.55147673363119232, 4.116875700062115229, -2.376879293651021019 ) ) ;
#6243=CARTESIAN_POINT ( 'NONE',  ( 25.53161554397954092, -0.8571990387063047612, -2.667681220810584009 ) ) ;
#6248=VERTEX_POINT ( 'NONE', #3901 ) ;
#6249=EDGE_CURVE ( 'NONE', #32816, #13791, #6919, .T. ) ;
#6253=CARTESIAN_POINT ( 'NONE',  ( 22.92250000000000298, 2.378061970571979433, -1.291182301015470602 ) ) ;
#6257=ORIENTED_EDGE ( 'NONE', *, *, #32044, .F. ) ;
#6263=EDGE_CURVE ( 'NONE', #2976, #10851, #25616, .T. ) ;
#6275=DIRECTION ( 'NONE',  ( 1.000000000000000000, -0.000000000000000000, -0.000000000000000000 ) ) ;
#6276=EDGE_CURVE ( 'NONE', #4235, #3463, #11568, .T. ) ;
#6296=DIRECTION ( 'NONE',  ( 0.000000000000000000, 1.000000000000000000, 0.000000000000000000 ) ) ;
#6322=ADVANCED_FACE ( 'NONE', ( #14380 ), #4066, .F. ) ;
#6335=CARTESIAN_POINT ( 'NONE',  ( 25.29749999999999943, -0.7685399846772070775, 2.594547506269381465 ) ) ;
#6340=CARTESIAN_POINT ( 'NONE',  ( 10.55147673363118876, -2.285372942704986698, 4.458382051008185520 ) ) ;
#6343=ORIENTED_EDGE ( 'NONE', *, *, #4689, .T. ) ;
#6345=VERTEX_POINT ( 'NONE', #1718 ) ;
#6346=EDGE_CURVE ( 'NONE', #8252, #22534, #634, .T. ) ;
#6348=CARTESIAN_POINT ( 'NONE',  ( 20.54750000273118715, -0.7685399846772070775, 2.594547506269381465 ) ) ;
#6349=LINE ( 'NONE', #3212, #28430 ) ;
#6363=AXIS2_PLACEMENT_3D ( 'NONE', #444, #26024, #15311 ) ;
#6372=LINE ( 'NONE', #1542, #28387 ) ;
#6384=CARTESIAN_POINT ( 'NONE',  ( 24.79750000273118715, -2.594547506269383685, -0.7685399846772043020 ) ) ;
#6394=ORIENTED_EDGE ( 'NONE', *, *, #6747, .T. ) ;
#6400=PLANE ( 'NONE',  #12889 ) ;
#6416=ORIENTED_EDGE ( 'NONE', *, *, #8751, .F. ) ;
#6420=CARTESIAN_POINT ( 'NONE',  ( 10.56183597391177464, 4.888740217817763464E-14, -4.753758587302147731 ) ) ;
#6422=AXIS2_PLACEMENT_3D ( 'NONE', #16555, #29446, #24267 ) ;
#6427=EDGE_CURVE ( 'NONE', #6020, #10425, #15061, .T. ) ;
#6430=DIRECTION ( 'NONE',  ( 2.219124775574899835E-17, 0.2588190451025176309, 0.9659258262890692004 ) ) ;
#6447=AXIS2_PLACEMENT_3D ( 'NONE', #11015, #21216, #31909 ) ;
#6449=CYLINDRICAL_SURFACE ( 'NONE', #9090, 5.010000000000000675 ) ;
#6459=AXIS2_PLACEMENT_3D ( 'NONE', #20291, #28297, #258 ) ;
#6463=ADVANCED_FACE ( 'NONE', ( #25441 ), #2208, .F. ) ;
#6466=DIRECTION ( 'NONE',  ( 0.000000000000000000, -0.9063077870366551547, 0.4226182617406882835 ) ) ;
#6471=CARTESIAN_POINT ( 'NONE',  ( 10.52034268205830259, -3.055657119358826446, 3.641590349731918863 ) ) ;
#6477=CIRCLE ( 'NONE', #624, 5.009999999999999787 ) ;
#6480=VERTEX_POINT ( 'NONE', #29106 ) ;
#6482=DIRECTION ( 'NONE',  ( 2.219124775574819717E-17, 0.2588190451025081940, 0.9659258262890716429 ) ) ;
#6501=ORIENTED_EDGE ( 'NONE', *, *, #4515, .T. ) ;
#6506=AXIS2_PLACEMENT_3D ( 'NONE', #19499, #22317, #4608 ) ;
#6507=CARTESIAN_POINT ( 'NONE',  ( 23.17250000000000298, 1.291182301015469047, 2.378061970571981654 ) ) ;
#6510=FACE_OUTER_BOUND ( 'NONE', #29487, .T. ) ;
#6513=VECTOR ( 'NONE', #15205, 1000.000000000000000 ) ;
#6516=DIRECTION ( 'NONE',  ( 7.770718973608945377E-17, 0.9063077870366468280, 0.4226182617407062136 ) ) ;
#6521=VECTOR ( 'NONE', #30181, 1000.000000000000000 ) ;
#6525=EDGE_CURVE ( 'NONE', #15485, #23867, #32602, .T. ) ;
#6526=CARTESIAN_POINT ( 'NONE',  ( 25.71477796605635291, 3.113678757437459588, 0.5295765639727612051 ) ) ;
#6538=AXIS2_PLACEMENT_3D ( 'NONE', #26147, #8755, #14592 ) ;
#6552=ORIENTED_EDGE ( 'NONE', *, *, #5248, .F. ) ;
#6555=ORIENTED_EDGE ( 'NONE', *, *, #24372, .F. ) ;
#6570=DIRECTION ( 'NONE',  ( -1.000000000000000000, 8.574039729943017111E-17, -3.081487911019577365E-33 ) ) ;
#6571=EDGE_CURVE ( 'NONE', #25432, #14457, #1863, .T. ) ;
#6572=VECTOR ( 'NONE', #10905, 1000.000000000000000 ) ;
#6574=CARTESIAN_POINT ( 'NONE',  ( 24.99290772595112031, -0.1310194482076040834, -2.499999999999998668 ) ) ;
#6582=ORIENTED_EDGE ( 'NONE', *, *, #26791, .T. ) ;
#6584=( BOUNDED_CURVE ( )  B_SPLINE_CURVE ( 2, ( #21483, #19128, #31698, #13442, #8776, #10963, #18981, #3756, #29319, #13922, #3940, #18487, #21165, #595, #24141, #10786, #21001, #31216, #8293, #28680, #15952, #26171, #3277, #31363, #14612, #24313, #4433, #9261, #9759, #24625, #6598, #9076, #12105, #29675, #30001, #14261, #4594, #6906, #22463, #1574, #24457, #11601, #6754, #14769, #9573, #19633, #7259, #27646, #21797, #16795, #32360, #22302, #19483, #1932, #32512, #29831, #12252, #16945, #1755, #32680, #19300, #17103, #27141, #24813, #1424, #19793, #4242, #19984, #11952, #26992, #29501, #7092, #14414, #17297, #11761, #24967, #27313, #30185, #21964, #32189, #22149 ),
 .UNSPECIFIED., .F., .F. ) 
 B_SPLINE_CURVE_WITH_KNOTS ( ( 3, 2, 2, 2, 2, 2, 2, 2, 2, 2, 2, 2, 2, 2, 2, 2, 2, 2, 2, 2, 2, 2, 2, 2, 2, 2, 2, 2, 2, 2, 2, 2, 2, 2, 2, 2, 2, 2, 2, 2, 3 ),
 ( 0.007661791872508488463, 0.02500000000000000139, 0.05000000000000000278, 0.07499999999999999722, 0.1000000000000000056, 0.1250000000000000000, 0.1499999999999999944, 0.1749999999999999889, 0.2000000000000000111, 0.2250000000000000056, 0.2500000000000000000, 0.2750000000000000222, 0.2999999999999999889, 0.3250000000000000111, 0.3499999999999999778, 0.3750000000000000000, 0.4000000000000000222, 0.4249999999999999889, 0.4500000000000000111, 0.4749999999999999778, 0.5000000000000000000, 0.5250000000000000222, 0.5500000000000000444, 0.5749999999999999556, 0.5999999999999999778, 0.6250000000000000000, 0.6500000000000000222, 0.6750000000000000444, 0.6999999999999999556, 0.7249999999999999778, 0.7500000000000000000, 0.7750000000000000222, 0.8000000000000000444, 0.8249999999999999556, 0.8499999999999999778, 0.8750000000000000000, 0.9000000000000000222, 0.9249999999999999334, 0.9499999999999999556, 0.9749999999999999778, 1.000000000000000000 ),
 .UNSPECIFIED. ) 
 CURVE ( )  GEOMETRIC_REPRESENTATION_ITEM ( )  RATIONAL_B_SPLINE_CURVE ( ( 0.9676416783621932804, 0.9472082996767494656, 1.000000000000000000, 0.9238795325112867385, 1.000000000000000000, 0.9238795325112867385, 1.000000000000000000, 0.9238795325112867385, 1.000000000000000000, 0.9238795325112867385, 1.000000000000000000, 0.9238795325112867385, 1.000000000000000000, 0.9238795325112867385, 1.000000000000000000, 0.9238795325112867385, 1.000000000000000000, 0.9238795325112867385, 1.000000000000000000, 0.9238795325112867385, 1.000000000000000000, 0.9238795325112867385, 1.000000000000000000, 0.9238795325112867385, 1.000000000000000000, 0.9238795325112867385, 1.000000000000000000, 0.9238795325112867385, 1.000000000000000000, 0.9238795325112867385, 1.000000000000000000, 0.9238795325112867385, 1.000000000000000000, 0.9238795325112867385, 1.000000000000000000, 0.9238795325112867385, 1.000000000000000000, 0.9238795325112867385, 1.000000000000000000, 0.9238795325112867385, 1.000000000000000000, 0.9238795325112867385, 1.000000000000000000, 0.9238795325112867385, 1.000000000000000000, 0.9238795325112867385, 1.000000000000000000, 0.9238795325112867385, 1.000000000000000000, 0.9238795325112867385, 1.000000000000000000, 0.9238795325112867385, 1.000000000000000000, 0.9238795325112867385, 1.000000000000000000, 0.9238795325112867385, 1.000000000000000000, 0.9238795325112867385, 1.000000000000000000, 0.9238795325112867385, 1.000000000000000000, 0.9238795325112867385, 1.000000000000000000, 0.9238795325112867385, 1.000000000000000000, 0.9238795325112867385, 1.000000000000000000, 0.9238795325112867385, 1.000000000000000000, 0.9238795325112867385, 1.000000000000000000, 0.9238795325112867385, 1.000000000000000000, 0.9238795325112867385, 1.000000000000000000, 0.9238795325112867385, 1.000000000000000000, 0.9238795325112867385, 1.000000000000000000, 0.9238795325112867385, 1.000000000000000000 ) ) 
 REPRESENTATION_ITEM ( '' )  );
#6590=ORIENTED_EDGE ( 'NONE', *, *, #9460, .F. ) ;
#6592=AXIS2_PLACEMENT_3D ( 'NONE', #488, #10673, #16004 ) ;
#6593=ORIENTED_EDGE ( 'NONE', *, *, #15276, .T. ) ;
#6597=ORIENTED_EDGE ( 'NONE', *, *, #28548, .F. ) ;
#6598=CARTESIAN_POINT ( 'NONE',  ( 23.92250000136559507, -1.913930629741527500, 2.363507492473149618 ) ) ;
#6604=VERTEX_POINT ( 'NONE', #1672 ) ;
#6610=AXIS2_PLACEMENT_3D ( 'NONE', #7384, #1908, #19608 ) ;
#6614=CARTESIAN_POINT ( 'NONE',  ( 10.00000000000000000, -4.208382051008212166, 2.718385644597159256 ) ) ;
#6618=CARTESIAN_POINT ( 'NONE',  ( 9.999999999999998224, -4.681538312723522388, 0.8254815157535101422 ) ) ;
#6630=VERTEX_POINT ( 'NONE', #32444 ) ;
#6634=ORIENTED_EDGE ( 'NONE', *, *, #20016, .T. ) ;
#6640=ORIENTED_EDGE ( 'NONE', *, *, #8126, .F. ) ;
#6653=PLANE ( 'NONE',  #8065 ) ;
#6655=LINE ( 'NONE', #28887, #23077 ) ;
#6657=AXIS2_PLACEMENT_3D ( 'NONE', #18859, #29062, #6296 ) ;
#6660=CYLINDRICAL_SURFACE ( 'NONE', #20938, 5.010000000000000675 ) ;
#6669=ORIENTED_EDGE ( 'NONE', *, *, #7184, .T. ) ;
#6670=CARTESIAN_POINT ( 'NONE',  ( 25.75999999999999801, -2.208672634433321348E-15, 0.000000000000000000 ) ) ;
#6675=ADVANCED_FACE ( 'NONE', ( #2012 ), #3859, .F. ) ;
#6678=VERTEX_POINT ( 'NONE', #9353 ) ;
#6681=DIRECTION ( 'NONE',  ( -8.281886410780517190E-17, -0.9659258262890689783, 0.2588190451025184080 ) ) ;
#6683=CARTESIAN_POINT ( 'NONE',  ( 23.79750000000001009, 0.7685399846772009713, -2.594547506269381909 ) ) ;
#6685=LINE ( 'NONE', #16874, #13860 ) ;
#6690=FACE_OUTER_BOUND ( 'NONE', #8286, .T. ) ;
#6696=FACE_OUTER_BOUND ( 'NONE', #19299, .T. ) ;
#6711=FACE_OUTER_BOUND ( 'NONE', #4044, .T. ) ;
#6722=DIRECTION ( 'NONE',  ( 0.4999999999999960587, -0.09052430460833682524, -0.8612812260087764349 ) ) ;
#6726=DIRECTION ( 'NONE',  ( 0.000000000000000000, 0.8191520442889907994, 0.5735764363510474917 ) ) ;
#6727=DIRECTION ( 'NONE',  ( -1.000000000000000000, 8.574039729943018344E-17, -0.000000000000000000 ) ) ;
#6742=ORIENTED_EDGE ( 'NONE', *, *, #23281, .F. ) ;
#6747=EDGE_CURVE ( 'NONE', #545, #2577, #24581, .T. ) ;
#6753=ORIENTED_EDGE ( 'NONE', *, *, #30829, .T. ) ;
#6754=CARTESIAN_POINT ( 'NONE',  ( 23.17250000136559862, -2.363507492473152283, -1.913930629741525280 ) ) ;
#6758=DIRECTION ( 'NONE',  ( 1.000000000000000000, -8.574039729943018344E-17, -0.000000000000000000 ) ) ;
#6762=LINE ( 'NONE', #1582, #15438 ) ;
#6764=CARTESIAN_POINT ( 'NONE',  ( 24.79750000136559507, 0.3178988483021036315, 3.024605502323848949 ) ) ;
#6770=ADVANCED_FACE ( 'NONE', ( #15355 ), #7689, .F. ) ;
#6774=( BOUNDED_CURVE ( )  B_SPLINE_CURVE ( 2, ( #26355, #12974, #13135 ),
 .UNSPECIFIED., .F., .F. ) 
 B_SPLINE_CURVE_WITH_KNOTS ( ( 3, 3 ),
 ( 0.9966116191895003640, 1.000000000000000000 ),
 .UNSPECIFIED. ) 
 CURVE ( )  GEOMETRIC_REPRESENTATION_ITEM ( )  RATIONAL_B_SPLINE_CURVE ( ( 0.9821626249036858880, 0.9896829947469992783, 1.000000000000000000 ) ) 
 REPRESENTATION_ITEM ( '' )  );
#6781=LINE ( 'NONE', #22175, #19977 ) ;
#6797=ORIENTED_EDGE ( 'NONE', *, *, #90, .T. ) ;
#6802=ORIENTED_EDGE ( 'NONE', *, *, #23782, .T. ) ;
#6811=DIRECTION ( 'NONE',  ( 1.000000000000000000, -0.000000000000000000, -0.000000000000000000 ) ) ;
#6814=ORIENTED_EDGE ( 'NONE', *, *, #23034, .T. ) ;
#6817=LINE ( 'NONE', #7170, #6070 ) ;
#6819=CARTESIAN_POINT ( 'NONE',  ( 10.56870887191539587, -4.787500056513357194, -1.476463073999686015 ) ) ;
#6820=VERTEX_POINT ( 'NONE', #15517 ) ;
#6822=FACE_OUTER_BOUND ( 'NONE', #19671, .T. ) ;
#6833=CARTESIAN_POINT ( 'NONE',  ( 10.52034268205830614, -3.055657119358777152, -3.641590349731960163 ) ) ;
#6834=FACE_OUTER_BOUND ( 'NONE', #10356, .T. ) ;
#6835=CARTESIAN_POINT ( 'NONE',  ( 23.98499999999999943, 2.486304738420679783, -0.2613211581691337604 ) ) ;
#6845=ORIENTED_EDGE ( 'NONE', *, *, #13133, .F. ) ;
#6848=CARTESIAN_POINT ( 'NONE',  ( 24.48500000136559507, 0.9349337715887185984, -3.156283516753368268 ) ) ;
#6857=VERTEX_POINT ( 'NONE', #26656 ) ;
#6883=CARTESIAN_POINT ( 'NONE',  ( 23.17250000136559862, -2.363507492473152283, -1.913930629741525280 ) ) ;
#6887=DIRECTION ( 'NONE',  ( 0.000000000000000000, 0.2588190451025318417, -0.9659258262890653146 ) ) ;
#6889=DIRECTION ( 'NONE',  ( -8.281886410780492538E-17, -0.9659258262890664248, -0.2588190451025276229 ) ) ;
#6892=ADVANCED_FACE ( 'NONE', ( #6711 ), #27095, .F. ) ;
#6897=ORIENTED_EDGE ( 'NONE', *, *, #13405, .F. ) ;
#6901=VERTEX_POINT ( 'NONE', #14365 ) ;
#6906=CARTESIAN_POINT ( 'NONE',  ( 23.48500000136559862, 2.892927487894327410, -1.570731468192931635 ) ) ;
#6917=CARTESIAN_POINT ( 'NONE',  ( 22.86000000136559507, -0.9349337715887248157, 3.156283516753367824 ) ) ;
#6919=CIRCLE ( 'NONE', #5314, 5.010000000000000675 ) ;
#6924=CARTESIAN_POINT ( 'NONE',  ( 21.50111451137534146, -3.256483526998273983E-15, 2.499999999999998668 ) ) ;
#6925=EDGE_CURVE ( 'NONE', #1564, #32584, #21425, .T. ) ;
#6934=AXIS2_PLACEMENT_3D ( 'NONE', #21801, #32007, #14266 ) ;
#6936=CARTESIAN_POINT ( 'NONE',  ( 10.55147673363119232, -2.376879293651037006, -4.116875700062107235 ) ) ;
#6938=DIRECTION ( 'NONE',  ( -1.000000000000000000, 8.574039729943019576E-17, -0.000000000000000000 ) ) ;
#6944=CARTESIAN_POINT ( 'NONE',  ( 10.52034268205830614, 3.055657119358800244, 3.641590349731939735 ) ) ;
#6952=LINE ( 'NONE', #25004, #2719 ) ;
#6969=PLANE ( 'NONE',  #18812 ) ;
#6979=CARTESIAN_POINT ( 'NONE',  ( 10.00000000000000178, 2.718385644597235196, -4.208382051008164204 ) ) ;
#6980=DIRECTION ( 'NONE',  ( 0.000000000000000000, -0.9961946980917449901, -0.08715574274766552110 ) ) ;
#6985=CIRCLE ( 'NONE', #13910, 5.009999999999999787 ) ;
#6986=ORIENTED_EDGE ( 'NONE', *, *, #29059, .T. ) ;
#6989=ADVANCED_FACE ( 'NONE', ( #26189, #29525 ), #16312, .T. ) ;
#6997=CARTESIAN_POINT ( 'NONE',  ( 24.17250000136559507, -3.024605502323851169, 0.3178988483021052969 ) ) ;
#7003=CIRCLE ( 'NONE', #29978, 5.009999999999999787 ) ;
#7024=DIRECTION ( 'NONE',  ( 1.000000000000000000, -0.000000000000000000, -0.000000000000000000 ) ) ;
#7034=VECTOR ( 'NONE', #3778, 1000.000000000000114 ) ;
#7037=VECTOR ( 'NONE', #30778, 1000.000000000000000 ) ;
#7041=ORIENTED_EDGE ( 'NONE', *, *, #14680, .T. ) ;
#7042=ORIENTED_EDGE ( 'NONE', *, *, #13830, .F. ) ;
#7047=AXIS2_PLACEMENT_3D ( 'NONE', #20379, #7679, #5168 ) ;
#7059=EDGE_CURVE ( 'NONE', #25696, #14457, #8792, .T. ) ;
#7060=AXIS2_PLACEMENT_3D ( 'NONE', #247, #18440, #2569 ) ;
#7062=DIRECTION ( 'NONE',  ( -1.000000000000000000, 8.574039729943017111E-17, -3.081487911019577365E-33 ) ) ;
#7063=CARTESIAN_POINT ( 'NONE',  ( 24.73500000136559507, 1.570731468192929858, 2.892927487894329186 ) ) ;
#7067=AXIS2_PLACEMENT_3D ( 'NONE', #12653, #25020, #10131 ) ;
#7068=CARTESIAN_POINT ( 'NONE',  ( 9.999999999999998224, -4.753758587302148619, 3.462581523170091167E-33 ) ) ;
#7070=VERTEX_POINT ( 'NONE', #23684 ) ;
#7071=DIRECTION ( 'NONE',  ( 8.541412920197216117E-17, 0.9961946980917452121, 0.08715574274766195451 ) ) ;
#7075=PLANE ( 'NONE',  #4402 ) ;
#7084=VECTOR ( 'NONE', #11959, 1000.000000000000000 ) ;
#7086=DIRECTION ( 'NONE',  ( -1.000000000000000000, 8.574039729943018344E-17, -0.000000000000000000 ) ) ;
#7088=VECTOR ( 'NONE', #24914, 1000.000000000000000 ) ;
#7092=CARTESIAN_POINT ( 'NONE',  ( 21.36000000136559507, 0.9349337715887185984, -3.156283516753368268 ) ) ;
#7093=CONICAL_SURFACE ( 'NONE', #23113, 2.499999999999996891, 1.029744258676653867 ) ;
#7099=ORIENTED_EDGE ( 'NONE', *, *, #4743, .T. ) ;
#7104=CARTESIAN_POINT ( 'NONE',  ( 21.23500000136559507, -3.156283516753370044, -0.9349337715887220401 ) ) ;
#7121=ORIENTED_EDGE ( 'NONE', *, *, #18571, .T. ) ;
#7133=VERTEX_POINT ( 'NONE', #29334 ) ;
#7137=VERTEX_POINT ( 'NONE', #11299 ) ;
#7139=ORIENTED_EDGE ( 'NONE', *, *, #921, .F. ) ;
#7146=EDGE_CURVE ( 'NONE', #6630, #115, #16632, .T. ) ;
#7149=CIRCLE ( 'NONE', #25847, 5.009999999999999787 ) ;
#7151=CARTESIAN_POINT ( 'NONE',  ( -7.077711312404582636E-17, -0.8254815157535566605, 4.681538312723514395 ) ) ;
#7154=CARTESIAN_POINT ( 'NONE',  ( 21.50111451137534146, -3.256483526998273983E-15, 2.499999999999998668 ) ) ;
#7160=DIRECTION ( 'NONE',  ( -1.000000000000000000, 8.574039729943018344E-17, -0.000000000000000000 ) ) ;
#7165=DIRECTION ( 'NONE',  ( -1.000000000000000000, 8.574039729943018344E-17, -0.000000000000000000 ) ) ;
#7167=EDGE_CURVE ( 'NONE', #13750, #4019, #11286, .T. ) ;
#7170=CARTESIAN_POINT ( 'NONE',  ( 10.52034268205830614, -3.407865132560155885, -3.672404558090073490 ) ) ;
#7172=CARTESIAN_POINT ( 'NONE',  ( 10.52034268205830614, -3.055657119358777152, -3.641590349731960163 ) ) ;
#7173=ORIENTED_EDGE ( 'NONE', *, *, #6276, .F. ) ;
#7184=EDGE_CURVE ( 'NONE', #26383, #31932, #22166, .T. ) ;
#7187=CARTESIAN_POINT ( 'NONE',  ( 24.04750000136559507, -1.913930629741527500, 2.363507492473149618 ) ) ;
#7196=ORIENTED_EDGE ( 'NONE', *, *, #130, .F. ) ;
#7198=ORIENTED_EDGE ( 'NONE', *, *, #16741, .F. ) ;
#7213=DIRECTION ( 'NONE',  ( 0.000000000000000000, 1.000000000000000000, 0.000000000000000000 ) ) ;
#7220=CARTESIAN_POINT ( 'NONE',  ( -3.958196854299239160E-16, -4.616489984850518091, -1.946309384392639119 ) ) ;
#7231=CARTESIAN_POINT ( 'NONE',  ( -4.075891499408641642E-16, -4.753758587302147731, 0.000000000000000000 ) ) ;
#7237=CARTESIAN_POINT ( 'NONE',  ( 23.23500000136559862, -1.570731468192933633, -2.892927487894330074 ) ) ;
#7242=FACE_OUTER_BOUND ( 'NONE', #2102, .T. ) ;
#7259=CARTESIAN_POINT ( 'NONE',  ( 22.92250000136559862, -1.913930629741527500, 2.363507492473149618 ) ) ;
#7263=EDGE_LOOP ( 'NONE', ( #29765, #16999, #24033, #32810 ) ) ;
#7279=DIRECTION ( 'NONE',  ( 0.7071067811865449082, 0.000000000000000000, -0.7071067811865501263 ) ) ;
#7281=VERTEX_POINT ( 'NONE', #6924 ) ;
#7284=ORIENTED_EDGE ( 'NONE', *, *, #11546, .T. ) ;
#7294=LINE ( 'NONE', #17485, #7515 ) ;
#7295=PLANE ( 'NONE',  #1108 ) ;
#7296=LINE ( 'NONE', #5251, #24153 ) ;
#7302=CARTESIAN_POINT ( 'NONE',  ( 21.36000000273118715, 1.942864903642424146, 1.573300977624592534 ) ) ;
#7312=ORIENTED_EDGE ( 'NONE', *, *, #23281, .T. ) ;
#7315=ORIENTED_EDGE ( 'NONE', *, *, #22254, .T. ) ;
#7330=CARTESIAN_POINT ( 'NONE',  ( 25.24521618911088794, -7.644457093038323125E-15, 2.510216189110891172 ) ) ;
#7332=VERTEX_POINT ( 'NONE', #20494 ) ;
#7335=CARTESIAN_POINT ( 'NONE',  ( 23.98500000136559507, -0.9349337715887248157, 3.156283516753367824 ) ) ;
#7343=CARTESIAN_POINT ( 'NONE',  ( 21.85999999999999943, 1.573300977624590313, -1.942864903642426144 ) ) ;
#7354=CARTESIAN_POINT ( 'NONE',  ( 10.00000000000000178, -1.476463073999608300, -4.787500056513382951 ) ) ;
#7356=EDGE_CURVE ( 'NONE', #15944, #27411, #418, .T. ) ;
#7359=VERTEX_POINT ( 'NONE', #25837 ) ;
#7364=ORIENTED_EDGE ( 'NONE', *, *, #29647, .T. ) ;
#7366=EDGE_LOOP ( 'NONE', ( #10033, #7041, #27811, #5882 ) ) ;
#7372=DIRECTION ( 'NONE',  ( -1.000000000000000000, 8.574039729943022041E-17, -1.232595164407830946E-32 ) ) ;
#7377=ORIENTED_EDGE ( 'NONE', *, *, #25300, .F. ) ;
#7384=CARTESIAN_POINT ( 'NONE',  ( 10.00000000000000178, -8.574039729943018837E-16, 0.000000000000000000 ) ) ;
#7385=CARTESIAN_POINT ( 'NONE',  ( 24.54750000136559507, 3.024605502323846729, -0.3178988483021056854 ) ) ;
#7386=EDGE_CURVE ( 'NONE', #32142, #4411, #7003, .T. ) ;
#7401=CARTESIAN_POINT ( 'NONE',  ( 10.56183597391177464, -5.003758587302149508, 0.2499999999999991951 ) ) ;
#7404=ORIENTED_EDGE ( 'NONE', *, *, #1191, .T. ) ;
#7416=CARTESIAN_POINT ( 'NONE',  ( 10.56870887191539587, -4.467071865485484850, 1.625881193364682620 ) ) ;
#7419=DIRECTION ( 'NONE',  ( 8.574039729943018344E-17, 1.000000000000000000, 0.000000000000000000 ) ) ;
#7435=ORIENTED_EDGE ( 'NONE', *, *, #6038, .F. ) ;
#7438=CARTESIAN_POINT ( 'NONE',  ( 3.608283490412332364E-16, 4.208382051008191738, 2.718385644597189454 ) ) ;
#7441=ORIENTED_EDGE ( 'NONE', *, *, #24039, .T. ) ;
#7456=CIRCLE ( 'NONE', #18657, 5.009999999999999787 ) ;
#7463=ORIENTED_EDGE ( 'NONE', *, *, #31794, .T. ) ;
#7468=CARTESIAN_POINT ( 'NONE',  ( 23.79750000136559507, 2.363507492473148286, 1.913930629741525058 ) ) ;
#7475=ORIENTED_EDGE ( 'NONE', *, *, #15715, .T. ) ;
#7480=EDGE_CURVE ( 'NONE', #22295, #6678, #13410, .T. ) ;
#7490=DIRECTION ( 'NONE',  ( 8.574039729943018344E-17, 1.000000000000000000, 0.000000000000000000 ) ) ;
#7491=CARTESIAN_POINT ( 'NONE',  ( 22.48500000136559507, 0.9349337715887185984, -3.156283516753368268 ) ) ;
#7492=CARTESIAN_POINT ( 'NONE',  ( 0.000000000000000000, 0.000000000000000000, 0.000000000000000000 ) ) ;
#7499=CARTESIAN_POINT ( 'NONE',  ( 10.00000000000000000, -4.971152295393299170, -0.6226916219172567990 ) ) ;
#7510=CARTESIAN_POINT ( 'NONE',  ( 22.86000000136559862, 1.570731468192929858, 2.892927487894329630 ) ) ;
#7511=VECTOR ( 'NONE', #8229, 1000.000000000000000 ) ;
#7514=DIRECTION ( 'NONE',  ( 8.541412920197227210E-17, 0.9961946980917464334, -0.08715574274764853469 ) ) ;
#7515=VECTOR ( 'NONE', #4971, 1000.000000000000000 ) ;
#7516=CARTESIAN_POINT ( 'NONE',  ( 0.000000000000000000, 0.000000000000000000, 0.000000000000000000 ) ) ;
#7518=EDGE_LOOP ( 'NONE', ( #26450, #10575, #14186, #28645 ) ) ;
#7521=VECTOR ( 'NONE', #25426, 1000.000000000000000 ) ;
#7523=LINE ( 'NONE', #12702, #13897 ) ;
#7526=VERTEX_POINT ( 'NONE', #17077 ) ;
#7535=CARTESIAN_POINT ( 'NONE',  ( 25.75999999999999801, -2.208672634433321348E-15, -2.499999999999997780 ) ) ;
#7541=VECTOR ( 'NONE', #4294, 1000.000000000000227 ) ;
#7547=ORIENTED_EDGE ( 'NONE', *, *, #28090, .T. ) ;
#7553=EDGE_CURVE ( 'NONE', #13056, #4840, #622, .T. ) ;
#7563=EDGE_LOOP ( 'NONE', ( #7475, #22925, #23293, #7173 ) ) ;
#7565=VECTOR ( 'NONE', #21287, 1000.000000000000000 ) ;
#7568=CIRCLE ( 'NONE', #31099, 5.010000000000000675 ) ;
#7569=CARTESIAN_POINT ( 'NONE',  ( 4.013969549054193054E-16, 4.681538312723529494, -0.8254815157534771686 ) ) ;
#7573=VECTOR ( 'NONE', #25942, 999.9999999999998863 ) ;
#7577=CIRCLE ( 'NONE', #30558, 5.010000000000000675 ) ;
#7583=ORIENTED_EDGE ( 'NONE', *, *, #26769, .T. ) ;
#7593=VECTOR ( 'NONE', #9355, 999.9999999999998863 ) ;
#7600=CARTESIAN_POINT ( 'NONE',  ( 10.00000000000000178, -8.574039729943018837E-16, 0.000000000000000000 ) ) ;
#7602=VECTOR ( 'NONE', #7086, 1000.000000000000000 ) ;
#7616=VECTOR ( 'NONE', #4407, 1000.000000000000000 ) ;
#7619=DIRECTION ( 'NONE',  ( 0.000000000000000000, 0.000000000000000000, 1.000000000000000000 ) ) ;
#7633=CARTESIAN_POINT ( 'NONE',  ( 25.75999999999999801, 0.8512451026088739825, 2.902758476911987628 ) ) ;
#7637=FACE_OUTER_BOUND ( 'NONE', #31058, .T. ) ;
#7647=DIRECTION ( 'NONE',  ( 0.000000000000000000, 1.000000000000000000, 0.000000000000000000 ) ) ;
#7661=CARTESIAN_POINT ( 'NONE',  ( 23.54750000136559862, 1.913930629741522838, -2.363507492473150062 ) ) ;
#7666=LINE ( 'NONE', #30584, #26828 ) ;
#7678=CARTESIAN_POINT ( 'NONE',  ( 25.23836956833649836, 0.1740941550253437553, 2.498860794741531777 ) ) ;
#7679=DIRECTION ( 'NONE',  ( -2.219124775574928185E-17, -0.2588190451025209060, -0.9659258262890682012 ) ) ;
#7684=CARTESIAN_POINT ( 'NONE',  ( 25.04750000136559507, -1.913930629741527500, 2.363507492473149618 ) ) ;
#7689=PLANE ( 'NONE',  #25678 ) ;
#7693=ORIENTED_EDGE ( 'NONE', *, *, #5999, .T. ) ;
#7695=ORIENTED_EDGE ( 'NONE', *, *, #30179, .T. ) ;
#7701=CARTESIAN_POINT ( 'NONE',  ( 21.29750000136559507, -2.363507492473152283, -1.913930629741525280 ) ) ;
#7714=VERTEX_POINT ( 'NONE', #7068 ) ;
#7717=CARTESIAN_POINT ( 'NONE',  ( 10.52034268205830259, -3.024842911000718892, 3.993798362933297597 ) ) ;
#7721=EDGE_LOOP ( 'NONE', ( #31047, #5452, #3450, #22937 ) ) ;
#7722=EDGE_CURVE ( 'NONE', #30399, #27411, #10057, .T. ) ;
#7726=CARTESIAN_POINT ( 'NONE',  ( 20.86000000136559152, 0.2613211581691317065, 2.486304738420681559 ) ) ;
#7728=DIRECTION ( 'NONE',  ( -1.000000000000000000, 8.574039729943018344E-17, 0.000000000000000000 ) ) ;
#7734=CARTESIAN_POINT ( 'NONE',  ( 25.23500000136559507, -1.570731468192933633, -2.892927487894330074 ) ) ;
#7735=CARTESIAN_POINT ( 'NONE',  ( 21.79750000136559507, 2.363507492473148286, 1.913930629741525058 ) ) ;
#7741=CARTESIAN_POINT ( 'NONE',  ( 23.67250000273118360, -2.378061970571983430, 1.291182301015471712 ) ) ;
#7744=DIRECTION ( 'NONE',  ( -8.281886410780519655E-17, -0.9659258262890698665, 0.2588190451025149663 ) ) ;
#7747=ORIENTED_EDGE ( 'NONE', *, *, #15037, .F. ) ;
#7753=CARTESIAN_POINT ( 'NONE',  ( 20.64125000204838756, 0.2896100032356176412, 2.755455120372265476 ) ) ;
#7763=CARTESIAN_POINT ( 'NONE',  ( 10.52034268205830259, 3.641590349731929077, 3.055657119358814011 ) ) ;
#7764=ORIENTED_EDGE ( 'NONE', *, *, #1425, .F. ) ;
#7770=CARTESIAN_POINT ( 'NONE',  ( 10.00000000000000178, 4.208382051008192626, 2.718385644597191231 ) ) ;
#7778=DIRECTION ( 'NONE',  ( 8.541412920197206256E-17, 0.9961946980917449901, 0.08715574274766552110 ) ) ;
#7782=CARTESIAN_POINT ( 'NONE',  ( -3.830085165118302378E-16, -4.467071865485461757, -1.625881193364742572 ) ) ;
#7785=EDGE_CURVE ( 'NONE', #9508, #17100, #22782, .T. ) ;
#7803=ORIENTED_EDGE ( 'NONE', *, *, #4230, .F. ) ;
#7808=DIRECTION ( 'NONE',  ( 8.281886410780482677E-17, 0.9659258262890646485, 0.2588190451025343397 ) ) ;
#7810=DIRECTION ( 'NONE',  ( 6.062761635205612732E-17, 0.7071067811865510144, -0.7071067811865441310 ) ) ;
#7814=FACE_OUTER_BOUND ( 'NONE', #26893, .T. ) ;
#7830=ORIENTED_EDGE ( 'NONE', *, *, #19980, .T. ) ;
#7837=LINE ( 'NONE', #30257, #4291 ) ;
#7840=ORIENTED_EDGE ( 'NONE', *, *, #18575, .T. ) ;
#7842=DIRECTION ( 'NONE',  ( 1.000000000000000000, -8.574039729943018344E-17, -0.000000000000000000 ) ) ;
#7843=CARTESIAN_POINT ( 'NONE',  ( 21.11000000136559152, -2.892927487894331406, 1.570731468192932301 ) ) ;
#7855=CARTESIAN_POINT ( 'NONE',  ( 22.42250000136559507, -0.3178988483021076838, -3.024605502323848949 ) ) ;
#7858=CARTESIAN_POINT ( 'NONE',  ( 10.00000000000000000, 4.681538312723516171, 0.8254815157535410064 ) ) ;
#7859=CARTESIAN_POINT ( 'NONE',  ( 24.50111451137534146, -3.256483526998273983E-15, 2.499999999999998668 ) ) ;
#7860=( BOUNDED_CURVE ( )  B_SPLINE_CURVE ( 2, ( #23986, #27012, #18653, #13949, #24476, #26667, #28854, #23841, #11472, #16151, #1594 ),
 .UNSPECIFIED., .F., .F. ) 
 B_SPLINE_CURVE_WITH_KNOTS ( ( 3, 2, 2, 2, 2, 3 ),
 ( 0.8966116191895003862, 0.9000000000000000222, 0.9250000000000000444, 0.9499999999999999556, 0.9749999999999999778, 0.9966116191895003640 ),
 .UNSPECIFIED. ) 
 CURVE ( )  GEOMETRIC_REPRESENTATION_ITEM ( )  RATIONAL_B_SPLINE_CURVE ( ( 0.9821626249036858880, 0.9896829947469992783, 1.000000000000000000, 0.9238795325112867385, 1.000000000000000000, 0.9238795325112867385, 1.000000000000000000, 0.9238795325112867385, 1.000000000000000000, 0.9341965377642874602, 0.9821626249036858880 ) ) 
 REPRESENTATION_ITEM ( '' )  );
#7862=PLANE ( 'NONE',  #13469 ) ;
#7864=EDGE_LOOP ( 'NONE', ( #16740, #18227, #26639, #30780, #17643, #11113, #27, #30840 ) ) ;
#7870=DIRECTION ( 'NONE',  ( 8.574039729943018344E-17, 1.000000000000000000, 0.000000000000000000 ) ) ;
#7878=CARTESIAN_POINT ( 'NONE',  ( 22.11000000273118715, 1.573300977624590313, -1.942864903642426144 ) ) ;
#7883=CARTESIAN_POINT ( 'NONE',  ( 21.11000000136559152, -2.892927487894331406, 1.570731468192932301 ) ) ;
#7884=FACE_OUTER_BOUND ( 'NONE', #20592, .T. ) ;
#7887=CARTESIAN_POINT ( 'NONE',  ( 10.55147673363119232, 2.285372942704952504, 4.458382051008201508 ) ) ;
#7890=CARTESIAN_POINT ( 'NONE',  ( 20.98500000136559862, -2.892927487894331406, 1.570731468192932301 ) ) ;
#7907=ORIENTED_EDGE ( 'NONE', *, *, #28687, .T. ) ;
#7909=CARTESIAN_POINT ( 'NONE',  ( 25.75999999999999801, -2.208672634433321348E-15, 0.000000000000000000 ) ) ;
#7913=LINE ( 'NONE', #22952, #25157 ) ;
#7924=CARTESIAN_POINT ( 'NONE',  ( 10.00000000000000000, 4.116875700062115229, -2.376879293651021019 ) ) ;
#7930=EDGE_CURVE ( 'NONE', #32468, #3987, #4038, .T. ) ;
#7931=DIRECTION ( 'NONE',  ( -1.000000000000000000, 8.574039729943015878E-17, 1.232595164407830946E-32 ) ) ;
#7937=CARTESIAN_POINT ( 'NONE',  ( 10.57125986779756843, -0.8254815157535575487, 4.681538312723514395 ) ) ;
#7940=CARTESIAN_POINT ( 'NONE',  ( 25.24521618911088794, -7.644457093038323125E-15, 2.510216189110891172 ) ) ;
#7945=ORIENTED_EDGE ( 'NONE', *, *, #14443, .T. ) ;
#7953=LINE ( 'NONE', #31034, #16037 ) ;
#7954=CARTESIAN_POINT ( 'NONE',  ( 10.56870887191539587, -4.467071865485484850, 1.625881193364682620 ) ) ;
#7960=EDGE_CURVE ( 'NONE', #3234, #12922, #21899, .T. ) ;
#7970=CARTESIAN_POINT ( 'NONE',  ( 23.75111450864416440, -1.283275288181523244E-15, -2.499999999999998668 ) ) ;
#7993=LINE ( 'NONE', #27904, #29962 ) ;
#8002=CARTESIAN_POINT ( 'NONE',  ( 10.00000000000000000, -2.285372942704986254, 4.458382051008184632 ) ) ;
#8009=CARTESIAN_POINT ( 'NONE',  ( 22.92250000136559862, 0.3178988483021036315, 3.024605502323848949 ) ) ;
#8032=LINE ( 'NONE', #26258, #21505 ) ;
#8038=ADVANCED_FACE ( 'NONE', ( #8797 ), #11303, .F. ) ;
#8041=CARTESIAN_POINT ( 'NONE',  ( 21.29750000136559507, -0.3178988483021076838, -3.024605502323848949 ) ) ;
#8042=AXIS2_PLACEMENT_3D ( 'NONE', #14298, #8956, #29359 ) ;
#8048=DIRECTION ( 'NONE',  ( -8.541412920197223512E-17, -0.9961946980917464334, 0.08715574274764813223 ) ) ;
#8049=CARTESIAN_POINT ( 'NONE',  ( 25.36000000273118715, 1.942864903642424146, 1.573300977624592534 ) ) ;
#8059=LINE ( 'NONE', #5871, #2908 ) ;
#8065=AXIS2_PLACEMENT_3D ( 'NONE', #31905, #1142, #19032 ) ;
#8067=AXIS2_PLACEMENT_3D ( 'NONE', #2297, #25364, #24851 ) ;
#8071=ORIENTED_EDGE ( 'NONE', *, *, #30179, .F. ) ;
#8074=EDGE_CURVE ( 'NONE', #14366, #7526, #7860, .T. ) ;
#8079=ORIENTED_EDGE ( 'NONE', *, *, #14330, .T. ) ;
#8095=VECTOR ( 'NONE', #23863, 1000.000000000000000 ) ;
#8097=LINE ( 'NONE', #20500, #25755 ) ;
#8100=AXIS2_PLACEMENT_3D ( 'NONE', #15839, #18026, #8160 ) ;
#8101=AXIS2_PLACEMENT_3D ( 'NONE', #738, #26615, #3719 ) ;
#8107=EDGE_CURVE ( 'NONE', #14569, #10511, #3481, .T. ) ;
#8111=AXIS2_PLACEMENT_3D ( 'NONE', #16812, #16460, #24333 ) ;
#8112=CARTESIAN_POINT ( 'NONE',  ( 24.75111450864415730, -6.623356326098185375E-16, -2.499999999999998224 ) ) ;
#8114=VERTEX_POINT ( 'NONE', #13638 ) ;
#8120=CARTESIAN_POINT ( 'NONE',  ( 25.75999999999999446, 1.024942698525265428, 2.863353032229740691 ) ) ;
#8126=EDGE_CURVE ( 'NONE', #16126, #17282, #1107, .T. ) ;
#8134=EDGE_CURVE ( 'NONE', #17346, #17030, #20416, .T. ) ;
#8138=AXIS2_PLACEMENT_3D ( 'NONE', #13993, #19370, #18877 ) ;
#8160=DIRECTION ( 'NONE',  ( 0.000000000000000000, 0.000000000000000000, -1.000000000000000000 ) ) ;
#8166=VECTOR ( 'NONE', #2987, 1000.000000000000114 ) ;
#8176=CARTESIAN_POINT ( 'NONE',  ( 21.17250000136559507, -3.024605502323851169, 0.3178988483021052969 ) ) ;
#8177=VECTOR ( 'NONE', #11057, 1000.000000000000114 ) ;
#8189=DIRECTION ( 'NONE',  ( 7.472768010110560055E-18, 0.08715574274765119922, 0.9961946980917462113 ) ) ;
#8193=VECTOR ( 'NONE', #753, 1000.000000000000114 ) ;
#8202=AXIS2_PLACEMENT_3D ( 'NONE', #7172, #17365, #6980 ) ;
#8216=ORIENTED_EDGE ( 'NONE', *, *, #17739, .T. ) ;
#8219=CARTESIAN_POINT ( 'NONE',  ( -2.619932554246580731E-16, -3.055657119358825557, 3.641590349731918863 ) ) ;
#8222=ORIENTED_EDGE ( 'NONE', *, *, #26956, .F. ) ;
#8228=CARTESIAN_POINT ( 'NONE',  ( 10.00000000000000000, 4.458382051008192626, 2.285372942704970267 ) ) ;
#8229=DIRECTION ( 'NONE',  ( -2.219124775574845909E-17, -0.2588190451025115246, -0.9659258262890707547 ) ) ;
#8236=CARTESIAN_POINT ( 'NONE',  ( 24.48500000273118715, 0.2613211581691317065, 2.486304738420681559 ) ) ;
#8246=PLANE ( 'NONE',  #7060 ) ;
#8250=CARTESIAN_POINT ( 'NONE',  ( 10.00000000000000000, -5.003758587302151284, 0.2499999999999993061 ) ) ;
#8252=VERTEX_POINT ( 'NONE', #27827 ) ;
#8254=ORIENTED_EDGE ( 'NONE', *, *, #4870, .T. ) ;
#8259=CARTESIAN_POINT ( 'NONE',  ( 4.013969549054193054E-16, 4.681538312723529494, -0.8254815157534771686 ) ) ;
#8264=EDGE_LOOP ( 'NONE', ( #20214, #3360, #31210, #19907, #17443 ) ) ;
#8277=CARTESIAN_POINT ( 'NONE',  ( 10.00000000000000000, 4.116875700062115229, -2.376879293651021019 ) ) ;
#8282=CARTESIAN_POINT ( 'NONE',  ( 23.42250000136559862, -0.3178988483021076838, -3.024605502323848949 ) ) ;
#8286=EDGE_LOOP ( 'NONE', ( #402, #14170, #11483, #13552 ) ) ;
#8293=CARTESIAN_POINT ( 'NONE',  ( 24.67250000136559507, 2.363507492473148286, 1.913930629741525058 ) ) ;
#8328=FACE_OUTER_BOUND ( 'NONE', #12968, .T. ) ;
#8340=ORIENTED_EDGE ( 'NONE', *, *, #10429, .T. ) ;
#8344=ORIENTED_EDGE ( 'NONE', *, *, #13399, .F. ) ;
#8345=EDGE_CURVE ( 'NONE', #16032, #25766, #8097, .T. ) ;
#8352=EDGE_LOOP ( 'NONE', ( #14794, #30637, #28128, #18619 ) ) ;
#8360=EDGE_LOOP ( 'NONE', ( #2077, #21605, #17278, #20810 ) ) ;
#8361=LINE ( 'NONE', #3369, #29517 ) ;
#8364=DIRECTION ( 'NONE',  ( 8.574039729943018344E-17, 1.000000000000000000, 0.000000000000000000 ) ) ;
#8377=DIRECTION ( 'NONE',  ( 8.574039729943018344E-17, 1.000000000000000000, 0.000000000000000000 ) ) ;
#8381=CARTESIAN_POINT ( 'NONE',  ( 24.29750000273118715, 2.594547506269380133, 0.7685399846772031918 ) ) ;
#8394=DIRECTION ( 'NONE',  ( 1.000000000000000000, -8.574039729943018344E-17, -0.000000000000000000 ) ) ;
#8397=ADVANCED_FACE ( 'NONE', ( #29303 ), #11586, .F. ) ;
#8402=LINE ( 'NONE', #23929, #23506 ) ;
#8408=ORIENTED_EDGE ( 'NONE', *, *, #1396, .F. ) ;
#8414=FACE_OUTER_BOUND ( 'NONE', #20122, .T. ) ;
#8427=CARTESIAN_POINT ( 'NONE',  ( 24.79750000136559507, 2.363507492473148286, 1.913930629741525058 ) ) ;
#8428=CARTESIAN_POINT ( 'NONE',  ( 25.41500598742548434, -2.668779812802359430, -0.3011795608359353338 ) ) ;
#8430=EDGE_LOOP ( 'NONE', ( #16683, #21150, #29510, #21298 ) ) ;
#8436=CARTESIAN_POINT ( 'NONE',  ( 22.75111450864416085, -1.241879311143409511E-16, -2.499999999999998668 ) ) ;
#8442=DIRECTION ( 'NONE',  ( 2.219124775574847758E-17, 0.2588190451025115246, 0.9659258262890707547 ) ) ;
#8443=ORIENTED_EDGE ( 'NONE', *, *, #26832, .F. ) ;
#8448=LINE ( 'NONE', #12790, #22055 ) ;
#8461=ORIENTED_EDGE ( 'NONE', *, *, #587, .T. ) ;
#8466=VERTEX_POINT ( 'NONE', #21464 ) ;
#8474=LINE ( 'NONE', #329, #27793 ) ;
#8478=FACE_OUTER_BOUND ( 'NONE', #26912, .T. ) ;
#8489=CARTESIAN_POINT ( 'NONE',  ( 10.57125986779756843, 0.6226916219172030642, 4.971152295393303611 ) ) ;
#8494=CARTESIAN_POINT ( 'NONE',  ( 10.55147673363118876, 2.376879293651121383, -4.116875700062057497 ) ) ;
#8509=ORIENTED_EDGE ( 'NONE', *, *, #25687, .T. ) ;
#8514=EDGE_CURVE ( 'NONE', #32756, #14180, #26332, .T. ) ;
#8517=VECTOR ( 'NONE', #16615, 1000.000000000000000 ) ;
#8523=CARTESIAN_POINT ( 'NONE',  ( 22.29750000136559507, -0.3178988483021076838, -3.024605502323848949 ) ) ;
#8525=ORIENTED_EDGE ( 'NONE', *, *, #24787, .F. ) ;
#8528=CARTESIAN_POINT ( 'NONE',  ( 21.92250000273118715, -1.291182301015472378, -2.378061970571982098 ) ) ;
#8530=ADVANCED_FACE ( 'NONE', ( #32171 ), #7075, .F. ) ;
#8531=VECTOR ( 'NONE', #25641, 1000.000000000000000 ) ;
#8535=VECTOR ( 'NONE', #20475, 1000.000000000000000 ) ;
#8538=ORIENTED_EDGE ( 'NONE', *, *, #10765, .T. ) ;
#8543=DIRECTION ( 'NONE',  ( 1.000000000000000000, -8.574039729943018344E-17, -0.000000000000000000 ) ) ;
#8553=ADVANCED_FACE ( 'NONE', ( #19468 ), #29659, .T. ) ;
#8558=VERTEX_POINT ( 'NONE', #9742 ) ;
#8562=DIRECTION ( 'NONE',  ( 1.000000000000000000, -8.574039729943018344E-17, -0.000000000000000000 ) ) ;
#8563=VECTOR ( 'NONE', #17486, 1000.000000000000114 ) ;
#8569=CARTESIAN_POINT ( 'NONE',  ( 24.73500000273118715, -2.486304738420683780, 0.2613211581691335383 ) ) ;
#8574=ORIENTED_EDGE ( 'NONE', *, *, #13233, .F. ) ;
#8577=AXIS2_PLACEMENT_3D ( 'NONE', #19842, #14961, #17833 ) ;
#8584=CARTESIAN_POINT ( 'NONE',  ( 25.45498872556016678, -2.391612775111189748, -1.307231450088218949 ) ) ;
#8595=CARTESIAN_POINT ( 'NONE',  ( 10.52034268205830614, 3.641590349731970822, -3.055657119358763829 ) ) ;
#8601=CARTESIAN_POINT ( 'NONE',  ( 21.73500000273118715, -2.486304738420683780, 0.2613211581691335383 ) ) ;
#8605=CARTESIAN_POINT ( 'NONE',  ( -9.560873106162357428E-17, -1.115095498423342990, 4.884328206559833241 ) ) ;
#8614=VECTOR ( 'NONE', #16075, 1000.000000000000000 ) ;
#8618=FACE_OUTER_BOUND ( 'NONE', #3722, .T. ) ;
#8619=CARTESIAN_POINT ( 'NONE',  ( 24.23499999999999943, 0.2613211581691317065, 2.486304738420681559 ) ) ;
#8642=DIRECTION ( 'NONE',  ( 3.623545766764168400E-17, 0.4226182617406938902, 0.9063077870366526012 ) ) ;
#8643=DIRECTION ( 'NONE',  ( 1.000000000000000000, -8.574039729943018344E-17, -0.000000000000000000 ) ) ;
#8650=EDGE_LOOP ( 'NONE', ( #5394, #16760, #31690, #28180 ) ) ;
#8661=CARTESIAN_POINT ( 'NONE',  ( 10.52034268205830259, 3.407865132560229604, -3.672404558090004212 ) ) ;
#8665=CLOSED_SHELL ( 'NONE', ( #27434, #2624, #2261, #1945, #24011, #6892, #14143, #24472, #9747, #8038, #24909, #16781, #5086, #4727, #25621, #15928, #27626, #20218, #10308, #31341, #16582, #25484, #31403, #10915, #15420, #1163, #2542, #29694, #23982, #17333, #1136, #26943, #21217, #28797, #3250, #19395, #4922, #12368, #17404, #2715, #13817, #20814, #15953, #2003, #32585, #12173, #31013, #8553, #5617, #6989, #30865, #17191, #21203, #12084, #27558, #22941, #2112, #13802, #10459, #18795, #25877, #11028, #13630, #22879, #999, #31312, #14090, #798, #13875, #19775, #17724, #17774, #3624, #4672, #21599, #23855, #8530, #17207, #18396, #15283, #22938, #9959, #20808, #29384, #11720, #22342, #14471, #22668, #26312, #5612, #6770, #18997, #23658, #26181, #25445, #9528, #28967, #1071, #2369, #30256, #30445, #6675, #16910, #14965, #5644, #29006, #20657, #21080, #32583, #25006, #1193, #29312, #26370, #11922, #13167, #15842, #9218, #3216, #27487, #19605, #31446, #6322, #13026, #6463, #24142, #17150, #8397, #22631, #11319, #20240, #5763, #5315, #1974, #13658, #23476 ) ) ;
#8688=ORIENTED_EDGE ( 'NONE', *, *, #26636, .F. ) ;
#8689=ORIENTED_EDGE ( 'NONE', *, *, #3090, .T. ) ;
#8706=AXIS2_PLACEMENT_3D ( 'NONE', #27687, #20034, #2300 ) ;
#8709=CARTESIAN_POINT ( 'NONE',  ( 20.61000000273118715, -1.573300977624594976, 1.942864903642425700 ) ) ;
#8722=CARTESIAN_POINT ( 'NONE',  ( 20.74999999999999645, -1.779113243963175696E-15, 0.000000000000000000 ) ) ;
#8733=CARTESIAN_POINT ( 'NONE',  ( 17.75999999999999801, -2.208672634433321348E-15, 0.000000000000000000 ) ) ;
#8744=CARTESIAN_POINT ( 'NONE',  ( 10.00000000000000178, -8.574039729943018837E-16, 0.000000000000000000 ) ) ;
#8751=EDGE_CURVE ( 'NONE', #22534, #21729, #10234, .T. ) ;
#8752=CARTESIAN_POINT ( 'NONE',  ( -2.037945749704337831E-16, -2.376879293651093406, 4.116875700062075261 ) ) ;
#8755=DIRECTION ( 'NONE',  ( -3.623545766764323707E-17, -0.4226182617407121533, 0.9063077870366440525 ) ) ;
#8760=EDGE_CURVE ( 'NONE', #866, #3400, #13229, .T. ) ;
#8763=CARTESIAN_POINT ( 'NONE',  ( 25.35555344407661593, -2.327875542983621315, 1.215979502681800328 ) ) ;
#8771=LINE ( 'NONE', #29163, #3866 ) ;
#8775=ORIENTED_EDGE ( 'NONE', *, *, #25981, .T. ) ;
#8776=CARTESIAN_POINT ( 'NONE',  ( 25.54750000136559507, 3.024605502323846729, -0.3178988483021056854 ) ) ;
#8781=VECTOR ( 'NONE', #33054, 1000.000000000000000 ) ;
#8783=ORIENTED_EDGE ( 'NONE', *, *, #16072, .T. ) ;
#8789=CARTESIAN_POINT ( 'NONE',  ( 10.00000000000000178, -2.285372942704923638, -4.458382051008218383 ) ) ;
#8792=LINE ( 'NONE', #3620, #12350 ) ;
#8795=CARTESIAN_POINT ( 'NONE',  ( 25.75999999999999801, -2.208672634433321348E-15, 0.000000000000000000 ) ) ;
#8797=FACE_OUTER_BOUND ( 'NONE', #30289, .T. ) ;
#8800=ORIENTED_EDGE ( 'NONE', *, *, #21033, .F. ) ;
#8807=ORIENTED_EDGE ( 'NONE', *, *, #2022, .T. ) ;
#8824=ORIENTED_EDGE ( 'NONE', *, *, #7059, .T. ) ;
#8829=LINE ( 'NONE', #16347, #28943 ) ;
#8842=PLANE ( 'NONE',  #22012 ) ;
#8847=ORIENTED_EDGE ( 'NONE', *, *, #10830, .F. ) ;
#8853=CARTESIAN_POINT ( 'NONE',  ( 22.17249999999999943, 1.291182301015469047, 2.378061970571981654 ) ) ;
#8864=VERTEX_POINT ( 'NONE', #27974 ) ;
#8867=CARTESIAN_POINT ( 'NONE',  ( 23.29750000273119070, 2.594547506269380133, 0.7685399846772031918 ) ) ;
#8875=DIRECTION ( 'NONE',  ( -1.000000000000000000, 8.574039729943017111E-17, -0.000000000000000000 ) ) ;
#8884=EDGE_LOOP ( 'NONE', ( #9832, #10329, #7139, #11497 ) ) ;
#8897=CARTESIAN_POINT ( 'NONE',  ( 10.57125986779756843, -4.884328206559830576, -1.115095498423360310 ) ) ;
#8900=UNCERTAINTY_MEASURE_WITH_UNIT (LENGTH_MEASURE( 1.000000000000000082E-05 ), #18799, 'distance_accuracy_value', 'NONE');
#8904=DIRECTION ( 'NONE',  ( 3.623545766764192436E-17, 0.4226182617406968878, 0.9063077870366511579 ) ) ;
#8920=ORIENTED_EDGE ( 'NONE', *, *, #873, .F. ) ;
#8926=ORIENTED_EDGE ( 'NONE', *, *, #10150, .F. ) ;
#8927=LINE ( 'NONE', #24320, #19919 ) ;
#8930=DIRECTION ( 'NONE',  ( 0.000000000000000000, 1.000000000000000000, 0.000000000000000000 ) ) ;
#8936=CARTESIAN_POINT ( 'NONE',  ( 9.999999999999998224, -4.753758587302148619, 3.462581523170091167E-33 ) ) ;
#8939=DIRECTION ( 'NONE',  ( -8.281886410780533213E-17, -0.9659258262890709767, 0.2588190451025108030 ) ) ;
#8941=DIRECTION ( 'NONE',  ( -7.770718973608944144E-17, -0.9063077870366468280, -0.4226182617407062136 ) ) ;
#8956=DIRECTION ( 'NONE',  ( 1.000000000000000000, -8.574039729943018344E-17, -0.000000000000000000 ) ) ;
#8959=CARTESIAN_POINT ( 'NONE',  ( 4.187842409712549624E-16, 4.884328206559851893, -1.115095498423258391 ) ) ;
#8960=ORIENTED_EDGE ( 'NONE', *, *, #5122, .T. ) ;
#8966=CARTESIAN_POINT ( 'NONE',  ( 25.57055368252914462, 0.2377959888981342196, -2.835553682530281172 ) ) ;
#8967=EDGE_LOOP ( 'NONE', ( #3083, #18302, #659, #16895 ) ) ;
#8976=CARTESIAN_POINT ( 'NONE',  ( 10.00000000000000178, 1.476463073999634723, 4.787500056513374069 ) ) ;
#8979=CARTESIAN_POINT ( 'NONE',  ( 20.79750000273118715, -2.594547506269383685, -0.7685399846772043020 ) ) ;
#8985=CARTESIAN_POINT ( 'NONE',  ( 10.55147673363118876, -4.116875700062067267, -2.376879293651108060 ) ) ;
#8999=CARTESIAN_POINT ( 'NONE',  ( 24.75111450864415730, -6.623356326098185375E-16, -2.499999999999998224 ) ) ;
#9001=CARTESIAN_POINT ( 'NONE',  ( 22.10999999999999943, 1.942864903642424146, 1.573300977624592534 ) ) ;
#9003=CARTESIAN_POINT ( 'NONE',  ( 3.830085165118329002E-16, 4.467071865485494619, -1.625881193364653088 ) ) ;
#9009=ORIENTED_EDGE ( 'NONE', *, *, #15421, .T. ) ;
#9014=CARTESIAN_POINT ( 'NONE',  ( 22.11000000273118715, 1.573300977624590313, -1.942864903642426144 ) ) ;
#9017=LINE ( 'NONE', #19237, #29535 ) ;
#9024=DIRECTION ( 'NONE',  ( 1.000000000000000000, -8.574039729943018344E-17, -0.000000000000000000 ) ) ;
#9027=EDGE_CURVE ( 'NONE', #31957, #1852, #11397, .T. ) ;
#9034=EDGE_CURVE ( 'NONE', #18153, #5447, #16547, .T. ) ;
#9055=AXIS2_PLACEMENT_3D ( 'NONE', #22122, #32334, #29803 ) ;
#9064=ORIENTED_EDGE ( 'NONE', *, *, #1843, .T. ) ;
#9066=EDGE_CURVE ( 'NONE', #10505, #5926, #27249, .T. ) ;
#9067=ORIENTED_EDGE ( 'NONE', *, *, #16290, .T. ) ;
#9075=ORIENTED_EDGE ( 'NONE', *, *, #11395, .F. ) ;
#9076=CARTESIAN_POINT ( 'NONE',  ( 23.86000000136559507, -0.9349337715887247047, 3.156283516753367824 ) ) ;
#9085=FACE_OUTER_BOUND ( 'NONE', #27522, .T. ) ;
#9090=AXIS2_PLACEMENT_3D ( 'NONE', #27180, #16655, #29204 ) ;
#9094=CARTESIAN_POINT ( 'NONE',  ( 20.74999999999999645, -5.000000000000005329, 6.123233995736771213E-16 ) ) ;
#9095=AXIS2_PLACEMENT_3D ( 'NONE', #32976, #7728, #2548 ) ;
#9115=VECTOR ( 'NONE', #11280, 1000.000000000000000 ) ;
#9121=DIRECTION ( 'NONE',  ( -1.000000000000000000, 8.574039729943018344E-17, -0.000000000000000000 ) ) ;
#9124=EDGE_CURVE ( 'NONE', #11002, #17553, #30936, .T. ) ;
#9137=CARTESIAN_POINT ( 'NONE',  ( 3.830085165118310759E-16, 4.467071865485471527, 1.625881193364712596 ) ) ;
#9142=AXIS2_PLACEMENT_3D ( 'NONE', #1103, #19000, #3776 ) ;
#9149=CARTESIAN_POINT ( 'NONE',  ( 25.75999999999999446, 1.747856820561523028, 2.520532175753987580 ) ) ;
#9151=ORIENTED_EDGE ( 'NONE', *, *, #19067, .F. ) ;
#9155=VECTOR ( 'NONE', #3572, 1000.000000000000114 ) ;
#9170=CARTESIAN_POINT ( 'NONE',  ( 25.35999999999999943, -1.573300977624594976, 1.942864903642425700 ) ) ;
#9171=AXIS2_PLACEMENT_3D ( 'NONE', #9476, #6811, #16849 ) ;
#9190=CARTESIAN_POINT ( 'NONE',  ( 25.42250000136559507, -0.3178988483021076838, -3.024605502323848949 ) ) ;
#9191=DIRECTION ( 'NONE',  ( 8.281886410780490073E-17, 0.9659258262890662028, 0.2588190451025284000 ) ) ;
#9193=DIRECTION ( 'NONE',  ( -2.219124775574953145E-17, -0.2588190451025242367, 0.9659258262890673130 ) ) ;
#9212=ORIENTED_EDGE ( 'NONE', *, *, #21813, .F. ) ;
#9218=ADVANCED_FACE ( 'NONE', ( #2879 ), #7862, .F. ) ;
#9219=CARTESIAN_POINT ( 'NONE',  ( 21.07875000068279903, 0.2896100032356176412, 2.755455120372265476 ) ) ;
#9233=DIRECTION ( 'NONE',  ( 8.541412920197208721E-17, 0.9961946980917446570, 0.08715574274766814400 ) ) ;
#9236=EDGE_CURVE ( 'NONE', #7359, #16254, #25748, .T. ) ;
#9240=ORIENTED_EDGE ( 'NONE', *, *, #15460, .T. ) ;
#9242=EDGE_CURVE ( 'NONE', #15936, #28186, #26843, .T. ) ;
#9244=CYLINDRICAL_SURFACE ( 'NONE', #17811, 5.010000000000000675 ) ;
#9251=VECTOR ( 'NONE', #7279, 1000.000000000000000 ) ;
#9254=ORIENTED_EDGE ( 'NONE', *, *, #3666, .T. ) ;
#9260=ORIENTED_EDGE ( 'NONE', *, *, #5001, .F. ) ;
#9261=CARTESIAN_POINT ( 'NONE',  ( 24.11000000136559507, -3.156283516753370488, -0.9349337715887220401 ) ) ;
#9266=CARTESIAN_POINT ( 'NONE',  ( 25.75999999999999801, -2.208672634433321348E-15, 0.000000000000000000 ) ) ;
#9267=ORIENTED_EDGE ( 'NONE', *, *, #19703, .F. ) ;
#9274=DIRECTION ( 'NONE',  ( 8.281886410780508561E-17, 0.9659258262890682012, -0.2588190451025209060 ) ) ;
#9279=EDGE_CURVE ( 'NONE', #29481, #11371, #21223, .T. ) ;
#9281=CARTESIAN_POINT ( 'NONE',  ( 1.668773398854301785E-16, 1.946309384392590935, 4.616489984850538519 ) ) ;
#9288=LINE ( 'NONE', #24658, #23143 ) ;
#9291=ORIENTED_EDGE ( 'NONE', *, *, #11893, .T. ) ;
#9294=VECTOR ( 'NONE', #11616, 1000.000000000000000 ) ;
#9311=CARTESIAN_POINT ( 'NONE',  ( 25.56220348721820201, -1.341958225229829886E-11, -2.827203487218203914 ) ) ;
#9321=CARTESIAN_POINT ( 'NONE',  ( 10.57125986779756843, -4.681538312723523276, 0.8254815157535098091 ) ) ;
#9329=EDGE_CURVE ( 'NONE', #15836, #18404, #31767, .T. ) ;
#9333=LINE ( 'NONE', #6819, #19956 ) ;
#9342=CYLINDRICAL_SURFACE ( 'NONE', #12944, 5.010000000000000675 ) ;
#9345=ORIENTED_EDGE ( 'NONE', *, *, #6160, .F. ) ;
#9346=CARTESIAN_POINT ( 'NONE',  ( 24.25111450864415730, -3.256483526998273983E-15, 2.499999999999998668 ) ) ;
#9348=CARTESIAN_POINT ( 'NONE',  ( 25.10999999999999943, 1.942864903642424146, 1.573300977624592534 ) ) ;
#9351=ORIENTED_EDGE ( 'NONE', *, *, #4743, .F. ) ;
#9353=CARTESIAN_POINT ( 'NONE',  ( 25.75999999999999801, -1.838216977691246972E-15, 3.024999999999999911 ) ) ;
#9355=DIRECTION ( 'NONE',  ( 7.472768010112043792E-18, 0.08715574274766818563, -0.9961946980917447680 ) ) ;
#9362=CARTESIAN_POINT ( 'NONE',  ( 3.529825581556927552E-16, 4.116875700062083254, 2.376879293651078751 ) ) ;
#9384=EDGE_LOOP ( 'NONE', ( #25734, #932, #11183, #27876 ) ) ;
#9389=ORIENTED_EDGE ( 'NONE', *, *, #22705, .F. ) ;
#9390=LINE ( 'NONE', #29800, #18293 ) ;
#9391=CARTESIAN_POINT ( 'NONE',  ( 22.48500000000000298, -2.486304738420683780, 0.2613211581691335383 ) ) ;
#9399=CARTESIAN_POINT ( 'NONE',  ( 23.48500000273119070, 0.2613211581691317065, 2.486304738420681559 ) ) ;
#9400=CARTESIAN_POINT ( 'NONE',  ( 23.42250000136559862, 1.913930629741522838, -2.363507492473150062 ) ) ;
#9420=CARTESIAN_POINT ( 'NONE',  ( 10.00000000000000000, 1.625881193364696831, 4.467071865485476856 ) ) ;
#9429=CARTESIAN_POINT ( 'NONE',  ( 23.29750000136559862, -0.3178988483021076838, -3.024605502323848949 ) ) ;
#9435=FACE_OUTER_BOUND ( 'NONE', #2541, .T. ) ;
#9448=EDGE_LOOP ( 'NONE', ( #10488, #11268, #1170, #19198 ) ) ;
#9460=EDGE_CURVE ( 'NONE', #31644, #15187, #6033, .T. ) ;
#9476=CARTESIAN_POINT ( 'NONE',  ( 25.75999999999999801, -2.208672634433321348E-15, 0.000000000000000000 ) ) ;
#9487=CARTESIAN_POINT ( 'NONE',  ( 10.55147673363119232, -4.116875700062100130, 2.376879293651050329 ) ) ;
#9500=CARTESIAN_POINT ( 'NONE',  ( 22.86000000000000298, 1.573300977624590313, -1.942864903642426144 ) ) ;
#9506=CARTESIAN_POINT ( 'NONE',  ( 10.56870887191539587, 1.625881193364757449, -4.467071865485455540 ) ) ;
#9508=VERTEX_POINT ( 'NONE', #6979 ) ;
#9519=LINE ( 'NONE', #32958, #15106 ) ;
#9522=ORIENTED_EDGE ( 'NONE', *, *, #22371, .T. ) ;
#9524=DIRECTION ( 'NONE',  ( -1.000000000000000000, 8.574039729943017111E-17, -0.000000000000000000 ) ) ;
#9527=CARTESIAN_POINT ( 'NONE',  ( 10.00000000000000000, 2.376879293651121383, -4.116875700062057497 ) ) ;
#9528=ADVANCED_FACE ( 'NONE', ( #11516 ), #31921, .F. ) ;
#9532=ORIENTED_EDGE ( 'NONE', *, *, #26274, .T. ) ;
#9535=EDGE_LOOP ( 'NONE', ( #7284, #27539, #7441, #19358 ) ) ;
#9538=CARTESIAN_POINT ( 'NONE',  ( 23.36000000000000298, -1.573300977624594976, 1.942864903642425700 ) ) ;
#9540=DIRECTION ( 'NONE',  ( 0.000000000000000000, -0.2588190451025251804, 0.9659258262890670910 ) ) ;
#9551=CARTESIAN_POINT ( 'NONE',  ( 25.73500000136559507, 1.570731468192929858, 2.892927487894329186 ) ) ;
#9554=ORIENTED_EDGE ( 'NONE', *, *, #16072, .F. ) ;
#9558=ORIENTED_EDGE ( 'NONE', *, *, #20518, .T. ) ;
#9572=VERTEX_POINT ( 'NONE', #30905 ) ;
#9573=CARTESIAN_POINT ( 'NONE',  ( 23.04750000136559862, -3.024605502323851169, 0.3178988483021052969 ) ) ;
#9579=ORIENTED_EDGE ( 'NONE', *, *, #30965, .F. ) ;
#9580=CIRCLE ( 'NONE', #14926, 5.010000000000000675 ) ;
#9583=CARTESIAN_POINT ( 'NONE',  ( 24.86000000136559862, -0.9349337715887248157, 3.156283516753367824 ) ) ;
#9584=DIRECTION ( 'NONE',  ( -1.000000000000000000, 8.574039729943018344E-17, 0.000000000000000000 ) ) ;
#9609=VECTOR ( 'NONE', #20136, 1000.000000000000000 ) ;
#9613=CARTESIAN_POINT ( 'NONE',  ( -3.122314033877883927E-16, -3.641590349731949505, 3.055657119358789142 ) ) ;
#9614=ORIENTED_EDGE ( 'NONE', *, *, #18500, .F. ) ;
#9619=PLANE ( 'NONE',  #8067 ) ;
#9631=LINE ( 'NONE', #22199, #14951 ) ;
#9643=EDGE_LOOP ( 'NONE', ( #28786, #7364, #11097, #5023 ) ) ;
#9652=ORIENTED_EDGE ( 'NONE', *, *, #587, .F. ) ;
#9656=VECTOR ( 'NONE', #30412, 1000.000000000000114 ) ;
#9664=CARTESIAN_POINT ( 'NONE',  ( 3.122314033877864698E-16, 3.641590349731929965, 3.055657119358814011 ) ) ;
#9668=CARTESIAN_POINT ( 'NONE',  ( 24.92250000136559507, 0.3178988483021036315, 3.024605502323848949 ) ) ;
#9674=DIRECTION ( 'NONE',  ( -1.000000000000000000, 8.574039729943018344E-17, 0.000000000000000000 ) ) ;
#9677=CARTESIAN_POINT ( 'NONE',  ( 21.75111450864415730, -1.283275288181523244E-15, -2.499999999999998668 ) ) ;
#9681=CIRCLE ( 'NONE', #14459, 5.010000000000000675 ) ;
#9682=VECTOR ( 'NONE', #27624, 1000.000000000000114 ) ;
#9692=CARTESIAN_POINT ( 'NONE',  ( -2.037945749704288773E-16, -2.376879293651036118, -4.116875700062107235 ) ) ;
#9699=ORIENTED_EDGE ( 'NONE', *, *, #18466, .F. ) ;
#9708=DIRECTION ( 'NONE',  ( -3.623545766764241739E-17, -0.4226182617407029385, 0.9063077870366482713 ) ) ;
#9709=ORIENTED_EDGE ( 'NONE', *, *, #14889, .T. ) ;
#9712=VERTEX_POINT ( 'NONE', #10990 ) ;
#9718=FACE_OUTER_BOUND ( 'NONE', #26003, .T. ) ;
#9730=CARTESIAN_POINT ( 'NONE',  ( 23.61000000136559507, 3.156283516753366047, 0.9349337715887203748 ) ) ;
#9733=CARTESIAN_POINT ( 'NONE',  ( 10.00000000000000000, 1.625881193364757449, -4.467071865485455540 ) ) ;
#9742=CARTESIAN_POINT ( 'NONE',  ( -3.608283490412316094E-16, -4.208382051008173086, -2.718385644597219208 ) ) ;
#9746=CARTESIAN_POINT ( 'NONE',  ( -4.104821569164996770E-16, -4.787500056513356306, -1.476463073999686015 ) ) ;
#9747=ADVANCED_FACE ( 'NONE', ( #813 ), #21191, .F. ) ;
#9752=VERTEX_POINT ( 'NONE', #13644 ) ;
#9759=CARTESIAN_POINT ( 'NONE',  ( 24.04750000136559507, -3.024605502323851169, 0.3178988483021052969 ) ) ;
#9763=VERTEX_POINT ( 'NONE', #15834 ) ;
#9766=ORIENTED_EDGE ( 'NONE', *, *, #21455, .T. ) ;
#9769=AXIS2_PLACEMENT_3D ( 'NONE', #1977, #1629, #11819 ) ;
#9771=CARTESIAN_POINT ( 'NONE',  ( 25.54750000136559507, 3.024605502323846729, -0.3178988483021056854 ) ) ;
#9780=VECTOR ( 'NONE', #28840, 1000.000000000000114 ) ;
#9790=CIRCLE ( 'NONE', #15675, 5.009999999999999787 ) ;
#9805=VECTOR ( 'NONE', #9584, 1000.000000000000000 ) ;
#9810=( BOUNDED_SURFACE ( )  B_SPLINE_SURFACE ( 1, 2, ( 
 ( #22280, #9551, #12403, #30470, #27287, #32986, #17756, #19766, #25100, #32833, #4404, #27625, #4218, #32651, #24599, #10055, #2217, #7063, #27777, #25291, #7385, #14390, #2404, #24944, #14588, #11927, #32490, #22127, #22624, #2058, #20118, #12229, #22436, #30311, #4889, #9730, #19960, #30164, #9400, #15071, #29809, #7237, #6883, #17426, #4726, #14896, #17074, #27966, #25605, #2718, #233, #26106, #28124, #15753, #18249, #20767, #3066, #15397, #5572, #30967, #380, #28462, #17933, #12891, #3211, #18083, #28623, #10555, #28273, #31307, #5223, #23111, #13078, #10405, #5070, #20615, #30822, #7890, #13373, #5384, #25957 ),
 ( #15574, #13221, #8049, #23421, #528, #25789, #2915, #23589, #23279, #5718, #10716, #710, #12726, #20929, #31149, #10900, #8236, #18432, #10225, #8381, #15898, #21107, #15247, #25451, #2559, #22928, #39, #20447, #30667, #7741, #24250, #14203, #13710, #23762, #14041, #8867, #11543, #28938, #16238, #21741, #1190, #31621, #876, #28768, #5858, #24067, #31949, #18578, #16383, #16044, #13856, #16728, #11388, #21587, #9014, #26932, #19231, #8528, #3550, #26276, #31451, #31793, #19074, #1020, #29115, #29430, #3390, #13555, #23911, #29262, #11053, #11204, #21412, #26749, #11696, #18734, #24400, #21894, #8709, #6348, #1368 ) ),
 .UNSPECIFIED., .F., .F., .F. ) 
 B_SPLINE_SURFACE_WITH_KNOTS ( ( 2, 2 ),
 ( 3, 2, 2, 2, 2, 2, 2, 2, 2, 2, 2, 2, 2, 2, 2, 2, 2, 2, 2, 2, 2, 2, 2, 2, 2, 2, 2, 2, 2, 2, 2, 2, 2, 2, 2, 2, 2, 2, 2, 2, 3 ),
 ( 0.000000000000000000, 1.000000000000000000 ),
 ( 0.000000000000000000, 0.02500000000000000139, 0.05000000000000000278, 0.07499999999999999722, 0.1000000000000000056, 0.1250000000000000000, 0.1499999999999999944, 0.1749999999999999889, 0.2000000000000000111, 0.2250000000000000056, 0.2500000000000000000, 0.2750000000000000222, 0.2999999999999999889, 0.3250000000000000111, 0.3499999999999999778, 0.3750000000000000000, 0.4000000000000000222, 0.4249999999999999889, 0.4500000000000000111, 0.4749999999999999778, 0.5000000000000000000, 0.5250000000000000222, 0.5500000000000000444, 0.5749999999999999556, 0.5999999999999999778, 0.6250000000000000000, 0.6500000000000000222, 0.6750000000000000444, 0.6999999999999999556, 0.7249999999999999778, 0.7500000000000000000, 0.7750000000000000222, 0.8000000000000000444, 0.8249999999999999556, 0.8499999999999999778, 0.8750000000000000000, 0.9000000000000000222, 0.9250000000000000444, 0.9499999999999999556, 0.9749999999999999778, 1.000000000000000000 ),
 .UNSPECIFIED. ) 
 GEOMETRIC_REPRESENTATION_ITEM ( )  RATIONAL_B_SPLINE_SURFACE ( (
 ( 1.000000000000000000, 0.9238795325112867385, 1.000000000000000000, 0.9238795325112867385, 1.000000000000000000, 0.9238795325112867385, 1.000000000000000000, 0.9238795325112867385, 1.000000000000000000, 0.9238795325112867385, 1.000000000000000000, 0.9238795325112867385, 1.000000000000000000, 0.9238795325112867385, 1.000000000000000000, 0.9238795325112867385, 1.000000000000000000, 0.9238795325112867385, 1.000000000000000000, 0.9238795325112867385, 1.000000000000000000, 0.9238795325112867385, 1.000000000000000000, 0.9238795325112867385, 1.000000000000000000, 0.9238795325112867385, 1.000000000000000000, 0.9238795325112867385, 1.000000000000000000, 0.9238795325112867385, 1.000000000000000000, 0.9238795325112867385, 1.000000000000000000, 0.9238795325112867385, 1.000000000000000000, 0.9238795325112867385, 1.000000000000000000, 0.9238795325112867385, 1.000000000000000000, 0.9238795325112867385, 1.000000000000000000, 0.9238795325112867385, 1.000000000000000000, 0.9238795325112867385, 1.000000000000000000, 0.9238795325112867385, 1.000000000000000000, 0.9238795325112867385, 1.000000000000000000, 0.9238795325112867385, 1.000000000000000000, 0.9238795325112867385, 1.000000000000000000, 0.9238795325112867385, 1.000000000000000000, 0.9238795325112867385, 1.000000000000000000, 0.9238795325112867385, 1.000000000000000000, 0.9238795325112867385, 1.000000000000000000, 0.9238795325112867385, 1.000000000000000000, 0.9238795325112867385, 1.000000000000000000, 0.9238795325112867385, 1.000000000000000000, 0.9238795325112867385, 1.000000000000000000, 0.9238795325112867385, 1.000000000000000000, 0.9238795325112867385, 1.000000000000000000, 0.9238795325112867385, 1.000000000000000000, 0.9238795325112867385, 1.000000000000000000, 0.9238795325112867385, 1.000000000000000000, 0.9238795325112867385, 1.000000000000000000),
 ( 1.000000000000000000, 0.9238795325112867385, 1.000000000000000000, 0.9238795325112867385, 1.000000000000000000, 0.9238795325112867385, 1.000000000000000000, 0.9238795325112867385, 1.000000000000000000, 0.9238795325112867385, 1.000000000000000000, 0.9238795325112867385, 1.000000000000000000, 0.9238795325112867385, 1.000000000000000000, 0.9238795325112867385, 1.000000000000000000, 0.9238795325112867385, 1.000000000000000000, 0.9238795325112867385, 1.000000000000000000, 0.9238795325112867385, 1.000000000000000000, 0.9238795325112867385, 1.000000000000000000, 0.9238795325112867385, 1.000000000000000000, 0.9238795325112867385, 1.000000000000000000, 0.9238795325112867385, 1.000000000000000000, 0.9238795325112867385, 1.000000000000000000, 0.9238795325112867385, 1.000000000000000000, 0.9238795325112867385, 1.000000000000000000, 0.9238795325112867385, 1.000000000000000000, 0.9238795325112867385, 1.000000000000000000, 0.9238795325112867385, 1.000000000000000000, 0.9238795325112867385, 1.000000000000000000, 0.9238795325112867385, 1.000000000000000000, 0.9238795325112867385, 1.000000000000000000, 0.9238795325112867385, 1.000000000000000000, 0.9238795325112867385, 1.000000000000000000, 0.9238795325112867385, 1.000000000000000000, 0.9238795325112867385, 1.000000000000000000, 0.9238795325112867385, 1.000000000000000000, 0.9238795325112867385, 1.000000000000000000, 0.9238795325112867385, 1.000000000000000000, 0.9238795325112867385, 1.000000000000000000, 0.9238795325112867385, 1.000000000000000000, 0.9238795325112867385, 1.000000000000000000, 0.9238795325112867385, 1.000000000000000000, 0.9238795325112867385, 1.000000000000000000, 0.9238795325112867385, 1.000000000000000000, 0.9238795325112867385, 1.000000000000000000, 0.9238795325112867385, 1.000000000000000000, 0.9238795325112867385, 1.000000000000000000) ) ) 
 REPRESENTATION_ITEM ( '' )  SURFACE ( )  );
#9812=VECTOR ( 'NONE', #32880, 999.9999999999998863 ) ;
#9819=CARTESIAN_POINT ( 'NONE',  ( 21.42250000273118715, 1.291182301015469047, 2.378061970571981654 ) ) ;
#9827=FACE_OUTER_BOUND ( 'NONE', #13202, .T. ) ;
#9832=ORIENTED_EDGE ( 'NONE', *, *, #6571, .T. ) ;
#9839=VERTEX_POINT ( 'NONE', #22789 ) ;
#9853=PLANE ( 'NONE',  #16725 ) ;
#9856=CARTESIAN_POINT ( 'NONE',  ( 24.23500000136559507, -3.156283516753370044, -0.9349337715887220401 ) ) ;
#9870=CARTESIAN_POINT ( 'NONE',  ( 20.92250000136559507, 0.3178988483021036315, 3.024605502323848949 ) ) ;
#9887=VERTEX_POINT ( 'NONE', #21995 ) ;
#9892=CARTESIAN_POINT ( 'NONE',  ( 10.52034268205830614, 3.672404558090085480, -3.407865132560142563 ) ) ;
#9894=DIRECTION ( 'NONE',  ( -8.541412920197212419E-17, -0.9961946980917449901, -0.08715574274766552110 ) ) ;
#9895=ORIENTED_EDGE ( 'NONE', *, *, #30148, .F. ) ;
#9902=ORIENTED_EDGE ( 'NONE', *, *, #10674, .T. ) ;
#9904=CARTESIAN_POINT ( 'NONE',  ( 10.52034268205830259, 3.055657119358849094, -3.641590349731898879 ) ) ;
#9915=CARTESIAN_POINT ( 'NONE',  ( 10.52034268205830614, -3.641590349731950393, 3.055657119358789142 ) ) ;
#9933=CARTESIAN_POINT ( 'NONE',  ( 21.00111451137534146, -1.283275288181523244E-15, -2.499999999999998668 ) ) ;
#9937=DIRECTION ( 'NONE',  ( 1.000000000000000000, -8.574039729943018344E-17, -0.000000000000000000 ) ) ;
#9940=CARTESIAN_POINT ( 'NONE',  ( 25.75999999999999801, -2.208672634433321348E-15, 0.000000000000000000 ) ) ;
#9945=ORIENTED_EDGE ( 'NONE', *, *, #10674, .F. ) ;
#9947=EDGE_CURVE ( 'NONE', #2193, #20203, #15406, .T. ) ;
#9951=CARTESIAN_POINT ( 'NONE',  ( 10.56870887191539587, -4.467071865485484850, 1.625881193364682620 ) ) ;
#9958=VERTEX_POINT ( 'NONE', #13380 ) ;
#9959=ADVANCED_FACE ( 'NONE', ( #5232 ), #8246, .F. ) ;
#9969=CARTESIAN_POINT ( 'NONE',  ( 10.00000000000000000, 4.681538312723528605, -0.8254815157534771686 ) ) ;
#9971=EDGE_CURVE ( 'NONE', #22295, #32366, #28935, .T. ) ;
#9974=CARTESIAN_POINT ( 'NONE',  ( 21.17250000273118715, 2.378061970571979433, -1.291182301015470602 ) ) ;
#9978=EDGE_CURVE ( 'NONE', #30423, #6480, #5583, .T. ) ;
#9987=CARTESIAN_POINT ( 'NONE',  ( 21.98500000136559507, -0.9349337715887248157, 3.156283516753367824 ) ) ;
#10002=DIRECTION ( 'NONE',  ( -1.000000000000000000, 8.574039729943019576E-17, -0.000000000000000000 ) ) ;
#10004=EDGE_CURVE ( 'NONE', #24556, #3406, #12735, .T. ) ;
#10006=DIRECTION ( 'NONE',  ( 2.219124775574961157E-17, 0.2588190451025251249, -0.9659258262890670910 ) ) ;
#10007=CARTESIAN_POINT ( 'NONE',  ( 23.11000000136559507, -2.892927487894331406, 1.570731468192932301 ) ) ;
#10022=DIRECTION ( 'NONE',  ( -1.000000000000000000, 8.574039729943022041E-17, 1.232595164407830946E-32 ) ) ;
#10025=CARTESIAN_POINT ( 'NONE',  ( 10.52034268205830259, -3.641590349731909537, -3.055657119358837992 ) ) ;
#10033=ORIENTED_EDGE ( 'NONE', *, *, #7356, .T. ) ;
#10035=ORIENTED_EDGE ( 'NONE', *, *, #12115, .T. ) ;
#10038=ORIENTED_EDGE ( 'NONE', *, *, #10765, .F. ) ;
#10044=LINE ( 'NONE', #20257, #19787 ) ;
#10047=DIRECTION ( 'NONE',  ( 1.000000000000000000, -8.574039729943018344E-17, -0.000000000000000000 ) ) ;
#10054=CARTESIAN_POINT ( 'NONE',  ( 23.36000000273119070, 1.942864903642424146, 1.573300977624592534 ) ) ;
#10055=CARTESIAN_POINT ( 'NONE',  ( 24.86000000136559862, -0.9349337715887248157, 3.156283516753367824 ) ) ;
#10057=LINE ( 'NONE', #15399, #25168 ) ;
#10060=ORIENTED_EDGE ( 'NONE', *, *, #4138, .T. ) ;
#10064=ORIENTED_EDGE ( 'NONE', *, *, #26957, .T. ) ;
#10065=EDGE_CURVE ( 'NONE', #2638, #10880, #31159, .T. ) ;
#10080=ORIENTED_EDGE ( 'NONE', *, *, #4648, .F. ) ;
#10102=CARTESIAN_POINT ( 'NONE',  ( -3.830085165118321606E-16, -4.467071865485483961, 1.625881193364682620 ) ) ;
#10116=FACE_OUTER_BOUND ( 'NONE', #8967, .T. ) ;
#10131=DIRECTION ( 'NONE',  ( 0.000000000000000000, 0.4226182617407029385, -0.9063077870366482713 ) ) ;
#10139=CARTESIAN_POINT ( 'NONE',  ( 21.54750000136559507, 1.913930629741522838, -2.363507492473150062 ) ) ;
#10140=EDGE_CURVE ( 'NONE', #9712, #10425, #3411, .T. ) ;
#10150=EDGE_CURVE ( 'NONE', #13056, #18479, #19244, .T. ) ;
#10158=VERTEX_POINT ( 'NONE', #11400 ) ;
#10162=CARTESIAN_POINT ( 'NONE',  ( 23.23500000136559862, -3.156283516753370044, -0.9349337715887220401 ) ) ;
#10165=DIRECTION ( 'NONE',  ( 0.000000000000000000, -0.9961946980917444350, -0.08715574274767159957 ) ) ;
#10169=EDGE_CURVE ( 'NONE', #10511, #32781, #132, .T. ) ;
#10177=AXIS2_PLACEMENT_3D ( 'NONE', #24550, #4028, #14196 ) ;
#10178=EDGE_CURVE ( 'NONE', #7714, #15085, #11896, .T. ) ;
#10180=CARTESIAN_POINT ( 'NONE',  ( 23.36000000136559507, -1.570731468192933633, -2.892927487894330962 ) ) ;
#10203=ORIENTED_EDGE ( 'NONE', *, *, #15715, .F. ) ;
#10205=DIRECTION ( 'NONE',  ( 0.000000000000000000, -0.5735764363510447161, -0.8191520442889927978 ) ) ;
#10210=LINE ( 'NONE', #25775, #32617 ) ;
#10225=CARTESIAN_POINT ( 'NONE',  ( 24.36000000273118715, 1.942864903642424146, 1.573300977624592534 ) ) ;
#10234=LINE ( 'NONE', #25457, #27900 ) ;
#10239=CIRCLE ( 'NONE', #10793, 5.009999999999999787 ) ;
#10243=VECTOR ( 'NONE', #17883, 999.9999999999998863 ) ;
#10251=CARTESIAN_POINT ( 'NONE',  ( -3.958196854299262826E-16, -4.616489984850546513, 1.946309384392575392 ) ) ;
#10256=VERTEX_POINT ( 'NONE', #27256 ) ;
#10269=VECTOR ( 'NONE', #9274, 1000.000000000000000 ) ;
#10277=DIRECTION ( 'NONE',  ( 1.000000000000000000, -8.574039729943018344E-17, -0.000000000000000000 ) ) ;
#10292=VECTOR ( 'NONE', #6889, 1000.000000000000000 ) ;
#10303=DIRECTION ( 'NONE',  ( -7.472768010110281180E-18, -0.08715574274764853469, -0.9961946980917464334 ) ) ;
#10308=ADVANCED_FACE ( 'NONE', ( #24920 ), #12205, .T. ) ;
#10318=CARTESIAN_POINT ( 'NONE',  ( 9.999999999999998224, -4.681538312723512618, -0.8254815157535732029 ) ) ;
#10320=CIRCLE ( 'NONE', #23144, 3.024999999999999911 ) ;
#10326=ORIENTED_EDGE ( 'NONE', *, *, #31797, .F. ) ;
#10329=ORIENTED_EDGE ( 'NONE', *, *, #29608, .T. ) ;
#10351=FACE_BOUND ( 'NONE', #16593, .T. ) ;
#10353=CARTESIAN_POINT ( 'NONE',  ( 25.11000000136559507, -2.892927487894331406, 1.570731468192932301 ) ) ;
#10356=EDGE_LOOP ( 'NONE', ( #27096, #7547, #9945, #25389 ) ) ;
#10359=LINE ( 'NONE', #13178, #7037 ) ;
#10368=CARTESIAN_POINT ( 'NONE',  ( 22.67250000136559507, 3.024605502323846729, -0.3178988483021056854 ) ) ;
#10382=CARTESIAN_POINT ( 'NONE',  ( 10.00000000000000178, -3.407865132560208288, 3.672404558090027304 ) ) ;
#10389=EDGE_CURVE ( 'NONE', #9572, #3790, #8829, .T. ) ;
#10392=DIRECTION ( 'NONE',  ( -8.541412920197221047E-17, -0.9961946980917455452, -0.08715574274765869323 ) ) ;
#10399=CARTESIAN_POINT ( 'NONE',  ( 21.36000000136559507, -1.570731468192933633, -2.892927487894330074 ) ) ;
#10405=CARTESIAN_POINT ( 'NONE',  ( 21.23500000136559507, -1.570731468192933633, -2.892927487894330074 ) ) ;
#10417=CARTESIAN_POINT ( 'NONE',  ( 10.55147673363119232, 4.116875700062115229, -2.376879293651021019 ) ) ;
#10425=VERTEX_POINT ( 'NONE', #23873 ) ;
#10428=EDGE_CURVE ( 'NONE', #32816, #16296, #6655, .T. ) ;
#10429=EDGE_CURVE ( 'NONE', #8252, #5204, #16191, .T. ) ;
#10443=LINE ( 'NONE', #5754, #26415 ) ;
#10448=CYLINDRICAL_SURFACE ( 'NONE', #12935, 5.010000000000000675 ) ;
#10452=ORIENTED_EDGE ( 'NONE', *, *, #4648, .T. ) ;
#10459=ADVANCED_FACE ( 'NONE', ( #3816 ), #12954, .F. ) ;
#10460=EDGE_LOOP ( 'NONE', ( #26057, #21837, #22147, #11138 ) ) ;
#10468=ORIENTED_EDGE ( 'NONE', *, *, #10004, .F. ) ;
#10470=DIRECTION ( 'NONE',  ( 3.623545766764135120E-17, 0.4226182617406906705, 0.9063077870366539335 ) ) ;
#10476=ORIENTED_EDGE ( 'NONE', *, *, #19494, .F. ) ;
#10477=CARTESIAN_POINT ( 'NONE',  ( 21.00111451137534146, -1.283275288181523244E-15, -2.499999999999998668 ) ) ;
#10488=ORIENTED_EDGE ( 'NONE', *, *, #21878, .T. ) ;
#10502=FACE_OUTER_BOUND ( 'NONE', #13913, .T. ) ;
#10505=VERTEX_POINT ( 'NONE', #20189 ) ;
#10508=CARTESIAN_POINT ( 'NONE',  ( 21.86000000136559507, 1.570731468192929858, 2.892927487894329186 ) ) ;
#10511=VERTEX_POINT ( 'NONE', #27196 ) ;
#10513=DIRECTION ( 'NONE',  ( 1.000000000000000000, -8.574039729943018344E-17, -0.000000000000000000 ) ) ;
#10520=CARTESIAN_POINT ( 'NONE',  ( 22.23500000136559507, -3.156283516753370488, -0.9349337715887220401 ) ) ;
#10522=LINE ( 'NONE', #10860, #3912 ) ;
#10526=EDGE_CURVE ( 'NONE', #14136, #30361, #26811, .T. ) ;
#10528=EDGE_CURVE ( 'NONE', #3046, #25477, #22037, .T. ) ;
#10548=CARTESIAN_POINT ( 'NONE',  ( 25.48500000136559862, 2.892927487894327410, -1.570731468192931635 ) ) ;
#10552=CARTESIAN_POINT ( 'NONE',  ( 10.00000000000000178, 0.6226916219172025091, 4.971152295393305387 ) ) ;
#10555=CARTESIAN_POINT ( 'NONE',  ( 21.61000000136559507, 3.156283516753366047, 0.9349337715887203748 ) ) ;
#10560=EDGE_LOOP ( 'NONE', ( #8216, #10064, #14982, #16908 ) ) ;
#10562=EDGE_CURVE ( 'NONE', #26729, #23098, #17171, .T. ) ;
#10566=EDGE_LOOP ( 'NONE', ( #13137, #13100, #377, #13180 ) ) ;
#10573=ORIENTED_EDGE ( 'NONE', *, *, #1440, .T. ) ;
#10575=ORIENTED_EDGE ( 'NONE', *, *, #8751, .T. ) ;
#10583=CARTESIAN_POINT ( 'NONE',  ( 10.00000000000000000, -3.024842911000719781, 3.993798362933299373 ) ) ;
#10586=CARTESIAN_POINT ( 'NONE',  ( 10.55147673363118876, -2.376879293651094294, 4.116875700062075261 ) ) ;
#10590=LINE ( 'NONE', #7151, #22953 ) ;
#10600=LINE ( 'NONE', #8277, #19897 ) ;
#10605=ORIENTED_EDGE ( 'NONE', *, *, #1838, .F. ) ;
#10606=CARTESIAN_POINT ( 'NONE',  ( 25.47393414918137466, -2.112935325431762656, -1.751578099123880516 ) ) ;
#10629=EDGE_LOOP ( 'NONE', ( #26560, #11116, #13099, #4469 ) ) ;
#10649=( BOUNDED_CURVE ( )  B_SPLINE_CURVE ( 2, ( #24367, #24704, #4501, #12160, #16682, #8979, #14489, #19190, #12014, #22358, #29385 ),
 .UNSPECIFIED., .F., .F. ) 
 B_SPLINE_CURVE_WITH_KNOTS ( ( 3, 2, 2, 2, 2, 3 ),
 ( 0.8966116191895003862, 0.9000000000000000222, 0.9250000000000000444, 0.9499999999999999556, 0.9749999999999999778, 0.9966116191895003640 ),
 .UNSPECIFIED. ) 
 CURVE ( )  GEOMETRIC_REPRESENTATION_ITEM ( )  RATIONAL_B_SPLINE_CURVE ( ( 0.9821626249036858880, 0.9896829947469992783, 1.000000000000000000, 0.9238795325112867385, 1.000000000000000000, 0.9238795325112867385, 1.000000000000000000, 0.9238795325112867385, 1.000000000000000000, 0.9341965377642874602, 0.9821626249036858880 ) ) 
 REPRESENTATION_ITEM ( '' )  );
#10660=DIRECTION ( 'NONE',  ( 7.023442172597802627E-17, 0.8191520442889853593, 0.5735764363510552633 ) ) ;
#10661=CARTESIAN_POINT ( 'NONE',  ( 21.42250000136559507, -0.3178988483021076838, -3.024605502323848949 ) ) ;
#10662=AXIS2_PLACEMENT_3D ( 'NONE', #27671, #4774, #17326 ) ;
#10670=ORIENTED_EDGE ( 'NONE', *, *, #16290, .F. ) ;
#10673=DIRECTION ( 'NONE',  ( 1.000000000000000000, -8.574039729943018344E-17, -0.000000000000000000 ) ) ;
#10674=EDGE_CURVE ( 'NONE', #26855, #7281, #24937, .T. ) ;
#10700=ORIENTED_EDGE ( 'NONE', *, *, #28548, .T. ) ;
#10703=AXIS2_PLACEMENT_3D ( 'NONE', #12719, #221, #32823 ) ;
#10705=CARTESIAN_POINT ( 'NONE',  ( 21.11000000136559152, -3.156283516753370044, -0.9349337715887220401 ) ) ;
#10706=AXIS2_PLACEMENT_3D ( 'NONE', #28391, #8642, #5809 ) ;
#10707=DIRECTION ( 'NONE',  ( 0.000000000000000000, 1.000000000000000000, 0.000000000000000000 ) ) ;
#10709=CARTESIAN_POINT ( 'NONE',  ( 10.57125986779756843, -0.8254815157534942660, -4.681538312723525053 ) ) ;
#10710=ORIENTED_EDGE ( 'NONE', *, *, #29647, .F. ) ;
#10711=DIRECTION ( 'NONE',  ( -1.000000000000000000, 8.574039729943018344E-17, -0.000000000000000000 ) ) ;
#10716=CARTESIAN_POINT ( 'NONE',  ( 24.86000000273118715, -1.942864903642428587, -1.573300977624592756 ) ) ;
#10722=DIRECTION ( 'NONE',  ( -7.472768010111999110E-18, -0.08715574274766814400, 0.9961946980917446570 ) ) ;
#10725=CARTESIAN_POINT ( 'NONE',  ( 25.23500000000000654, 2.486304733690583912, -0.2613212031729839624 ) ) ;
#10736=CIRCLE ( 'NONE', #32084, 5.010000000000000675 ) ;
#10742=DIRECTION ( 'NONE',  ( 8.574039729943018344E-17, 1.000000000000000000, 0.000000000000000000 ) ) ;
#10744=VECTOR ( 'NONE', #1081, 1000.000000000000000 ) ;
#10752=LINE ( 'NONE', #13408, #21925 ) ;
#10756=DIRECTION ( 'NONE',  ( -7.770718973608981122E-17, -0.9063077870366509359, 0.4226182617406975539 ) ) ;
#10758=AXIS2_PLACEMENT_3D ( 'NONE', #32750, #32413, #29572 ) ;
#10765=EDGE_CURVE ( 'NONE', #3987, #18549, #11458, .T. ) ;
#10769=CARTESIAN_POINT ( 'NONE',  ( 22.11000000136559507, -2.892927487894331406, 1.570731468192932301 ) ) ;
#10774=EDGE_CURVE ( 'NONE', #21855, #30672, #8927, .T. ) ;
#10786=CARTESIAN_POINT ( 'NONE',  ( 24.86000000136559507, -0.9349337715887247047, 3.156283516753367824 ) ) ;
#10793=AXIS2_PLACEMENT_3D ( 'NONE', #20725, #28404, #5520 ) ;
#10800=ORIENTED_EDGE ( 'NONE', *, *, #28298, .F. ) ;
#10811=VECTOR ( 'NONE', #12727, 1000.000000000000114 ) ;
#10826=ORIENTED_EDGE ( 'NONE', *, *, #28752, .T. ) ;
#10830=EDGE_CURVE ( 'NONE', #14757, #24556, #12562, .T. ) ;
#10839=EDGE_CURVE ( 'NONE', #14366, #26855, #20106, .T. ) ;
#10851=VERTEX_POINT ( 'NONE', #15553 ) ;
#10854=LINE ( 'NONE', #8489, #14605 ) ;
#10860=CARTESIAN_POINT ( 'NONE',  ( 10.00000000000000000, 4.753758587302147731, 3.462581523170085693E-33 ) ) ;
#10868=ORIENTED_EDGE ( 'NONE', *, *, #16741, .T. ) ;
#10873=EDGE_CURVE ( 'NONE', #29889, #32584, #2701, .T. ) ;
#10877=CARTESIAN_POINT ( 'NONE',  ( 4.075891499408641642E-16, 4.753758587302147731, 0.000000000000000000 ) ) ;
#10880=VERTEX_POINT ( 'NONE', #11768 ) ;
#10884=CARTESIAN_POINT ( 'NONE',  ( 25.79749999999999943, 0.7685399846772009713, -2.594547506269381909 ) ) ;
#10896=DIRECTION ( 'NONE',  ( -4.917867153433062508E-17, -0.5735764363510531538, 0.8191520442889869136 ) ) ;
#10897=ORIENTED_EDGE ( 'NONE', *, *, #24060, .T. ) ;
#10900=CARTESIAN_POINT ( 'NONE',  ( 24.54750000273118715, -0.7685399846772070775, 2.594547506269381465 ) ) ;
#10902=EDGE_CURVE ( 'NONE', #10851, #8114, #21970, .T. ) ;
#10905=DIRECTION ( 'NONE',  ( -1.000000000000000000, 8.574039729943018344E-17, -0.000000000000000000 ) ) ;
#10906=CARTESIAN_POINT ( 'NONE',  ( 10.00000000000000000, -4.616489984850546513, 1.946309384392575392 ) ) ;
#10913=CARTESIAN_POINT ( 'NONE',  ( 10.56183597391177464, -5.003758587302149508, -0.2500000000000008882 ) ) ;
#10915=ADVANCED_FACE ( 'NONE', ( #20253 ), #19490, .T. ) ;
#10917=EDGE_CURVE ( 'NONE', #18770, #18479, #32197, .T. ) ;
#10920=PLANE ( 'NONE',  #1188 ) ;
#10924=ORIENTED_EDGE ( 'NONE', *, *, #27238, .T. ) ;
#10925=LINE ( 'NONE', #11229, #28936 ) ;
#10948=VERTEX_POINT ( 'NONE', #4874 ) ;
#10949=CARTESIAN_POINT ( 'NONE',  ( 23.36000000136559507, -1.570731468192933633, -2.892927487894330074 ) ) ;
#10951=CARTESIAN_POINT ( 'NONE',  ( 25.46140505637537643, -2.308950792538006613, -1.460408169760519792 ) ) ;
#10960=CARTESIAN_POINT ( 'NONE',  ( 23.04750000000000654, 2.594547506269380133, 0.7685399846772031918 ) ) ;
#10963=CARTESIAN_POINT ( 'NONE',  ( 25.48500000136559507, 2.892927487894327410, -1.570731468192931635 ) ) ;
#10970=DIRECTION ( 'NONE',  ( 1.000000000000000000, -8.574039729943018344E-17, -0.000000000000000000 ) ) ;
#10990=CARTESIAN_POINT ( 'NONE',  ( 20.74999999999999645, 5.999999999999999112, 0.000000000000000000 ) ) ;
#10992=ORIENTED_EDGE ( 'NONE', *, *, #10873, .T. ) ;
#10994=EDGE_CURVE ( 'NONE', #16940, #9839, #8032, .T. ) ;
#11002=VERTEX_POINT ( 'NONE', #8219 ) ;
#11015=CARTESIAN_POINT ( 'NONE',  ( 20.74999999999999645, -1.779113243963176091E-15, 0.000000000000000000 ) ) ;
#11026=EDGE_LOOP ( 'NONE', ( #14877, #208, #1895, #14250 ) ) ;
#11028=ADVANCED_FACE ( 'NONE', ( #13205 ), #21533, .T. ) ;
#11038=CARTESIAN_POINT ( 'NONE',  ( 2.037945749704362236E-16, 2.376879293651122271, -4.116875700062057497 ) ) ;
#11051=ORIENTED_EDGE ( 'NONE', *, *, #13508, .F. ) ;
#11053=CARTESIAN_POINT ( 'NONE',  ( 21.11000000273118715, 1.573300977624590313, -1.942864903642426144 ) ) ;
#11057=DIRECTION ( 'NONE',  ( -8.541412920197225978E-17, -0.9961946980917466554, 0.08715574274764535667 ) ) ;
#11059=CARTESIAN_POINT ( 'NONE',  ( 10.57125986779756843, 4.884328206559851004, -1.115095498423258391 ) ) ;
#11063=CARTESIAN_POINT ( 'NONE',  ( 0.000000000000000000, 0.000000000000000000, 0.000000000000000000 ) ) ;
#11088=CARTESIAN_POINT ( 'NONE',  ( 10.00000000000000000, 4.893557421779793832E-14, -4.753758587302147731 ) ) ;
#11097=ORIENTED_EDGE ( 'NONE', *, *, #10774, .T. ) ;
#11098=CARTESIAN_POINT ( 'NONE',  ( 24.29750000136559507, -2.363507492473152283, -1.913930629741525280 ) ) ;
#11112=CARTESIAN_POINT ( 'NONE',  ( 1.265925305626668392E-16, 1.476463073999636277, 4.787500056513372293 ) ) ;
#11113=ORIENTED_EDGE ( 'NONE', *, *, #1396, .T. ) ;
#11116=ORIENTED_EDGE ( 'NONE', *, *, #30216, .T. ) ;
#11124=DIRECTION ( 'NONE',  ( -7.023442172597837140E-17, -0.8191520442889893561, -0.5735764363510496011 ) ) ;
#11138=ORIENTED_EDGE ( 'NONE', *, *, #28600, .F. ) ;
#11140=ADVANCED_BREP_SHAPE_REPRESENTATION ( '', ( #21237, #2865 ), #13509 ) ;
#11153=CARTESIAN_POINT ( 'NONE',  ( -4.013969549054180728E-16, -4.681538312723511730, -0.8254815157535732029 ) ) ;
#11159=ORIENTED_EDGE ( 'NONE', *, *, #5741, .F. ) ;
#11174=DIRECTION ( 'NONE',  ( 0.000000000000000000, 0.1045284632676536235, 0.9945218953682734009 ) ) ;
#11177=ORIENTED_EDGE ( 'NONE', *, *, #6, .T. ) ;
#11183=ORIENTED_EDGE ( 'NONE', *, *, #171, .T. ) ;
#11198=CARTESIAN_POINT ( 'NONE',  ( 21.48500000136559507, 2.892927487894327410, -1.570731468192931635 ) ) ;
#11200=LINE ( 'NONE', #18573, #20863 ) ;
#11204=CARTESIAN_POINT ( 'NONE',  ( 21.04750000273118715, 0.7685399846772009713, -2.594547506269381909 ) ) ;
#11220=DIRECTION ( 'NONE',  ( 8.574039729943018344E-17, 1.000000000000000000, 0.000000000000000000 ) ) ;
#11229=CARTESIAN_POINT ( 'NONE',  ( 10.00000000000000000, 4.467071865485493731, -1.625881193364653088 ) ) ;
#11238=DIRECTION ( 'NONE',  ( 0.000000000000000000, 1.000000000000000000, 0.000000000000000000 ) ) ;
#11241=VECTOR ( 'NONE', #4631, 1000.000000000000000 ) ;
#11245=CYLINDRICAL_SURFACE ( 'NONE', #16724, 5.010000000000000675 ) ;
#11251=ORIENTED_EDGE ( 'NONE', *, *, #32353, .F. ) ;
#11255=CARTESIAN_POINT ( 'NONE',  ( 10.55147673363119232, 2.376879293651063652, 4.116875700062091248 ) ) ;
#11256=CARTESIAN_POINT ( 'NONE',  ( 25.75999999999999801, -2.208672634433321348E-15, 0.000000000000000000 ) ) ;
#11262=( BOUNDED_CURVE ( )  B_SPLINE_CURVE ( 2, ( #8999, #19400, #32285, #19215, #27414, #27066, #14517, #11528, #21724, #21879, #9346 ),
 .UNSPECIFIED., .F., .F. ) 
 B_SPLINE_CURVE_WITH_KNOTS ( ( 3, 2, 2, 2, 2, 3 ),
 ( 0.2966116191895003529, 0.2999999999999999889, 0.3250000000000000111, 0.3499999999999999778, 0.3750000000000000000, 0.3966116191895003862 ),
 .UNSPECIFIED. ) 
 CURVE ( )  GEOMETRIC_REPRESENTATION_ITEM ( )  RATIONAL_B_SPLINE_CURVE ( ( 0.9821626249036858880, 0.9896829947469992783, 1.000000000000000000, 0.9238795325112867385, 1.000000000000000000, 0.9238795325112867385, 1.000000000000000000, 0.9238795325112867385, 1.000000000000000000, 0.9341965377642874602, 0.9821626249036858880 ) ) 
 REPRESENTATION_ITEM ( '' )  );
#11265=ORIENTED_EDGE ( 'NONE', *, *, #11610, .F. ) ;
#11268=ORIENTED_EDGE ( 'NONE', *, *, #431, .T. ) ;
#11272=CARTESIAN_POINT ( 'NONE',  ( 23.24290772321994325, 0.1310194482076003919, 2.499999999999998668 ) ) ;
#11280=DIRECTION ( 'NONE',  ( -3.623545766764295357E-17, -0.4226182617407088782, 0.9063077870366454958 ) ) ;
#11285=EDGE_CURVE ( 'NONE', #5334, #17030, #4634, .T. ) ;
#11286=CIRCLE ( 'NONE', #4866, 5.009999999999999787 ) ;
#11289=FACE_OUTER_BOUND ( 'NONE', #25885, .T. ) ;
#11292=VECTOR ( 'NONE', #2956, 1000.000000000000000 ) ;
#11299=CARTESIAN_POINT ( 'NONE',  ( 25.75999999999999801, -5.000000000000005329, 6.123233995736771213E-16 ) ) ;
#11303=CYLINDRICAL_SURFACE ( 'NONE', #8111, 2.499999999999997780 ) ;
#11319=ADVANCED_FACE ( 'NONE', ( #20341 ), #12146, .F. ) ;
#11322=FACE_OUTER_BOUND ( 'NONE', #31996, .T. ) ;
#11323=LINE ( 'NONE', #26399, #3801 ) ;
#11341=CYLINDRICAL_SURFACE ( 'NONE', #1175, 2.499999999999997780 ) ;
#11345=ORIENTED_EDGE ( 'NONE', *, *, #23486, .F. ) ;
#11349=CIRCLE ( 'NONE', #1769, 5.009999999999999787 ) ;
#11366=DIRECTION ( 'NONE',  ( -7.023442172597800162E-17, -0.8191520442889850262, -0.5735764363510558184 ) ) ;
#11367=EDGE_LOOP ( 'NONE', ( #10573, #25410, #24183, #28602 ) ) ;
#11369=VECTOR ( 'NONE', #207, 1000.000000000000000 ) ;
#11371=VERTEX_POINT ( 'NONE', #27859 ) ;
#11373=CARTESIAN_POINT ( 'NONE',  ( -4.013969549054187630E-16, -4.681538312723522388, 0.8254815157535098091 ) ) ;
#11375=CARTESIAN_POINT ( 'NONE',  ( 22.73500000000000298, -0.2613211581691358698, -2.486304738420681559 ) ) ;
#11379=ORIENTED_EDGE ( 'NONE', *, *, #14282, .F. ) ;
#11384=LINE ( 'NONE', #13216, #24586 ) ;
#11387=AXIS2_PLACEMENT_3D ( 'NONE', #3488, #18661, #5960 ) ;
#11388=CARTESIAN_POINT ( 'NONE',  ( 22.23500000273118715, 2.486304738420679783, -0.2613211581691337604 ) ) ;
#11395=EDGE_CURVE ( 'NONE', #6345, #32276, #28999, .T. ) ;
#11397=LINE ( 'NONE', #21594, #2307 ) ;
#11399=EDGE_LOOP ( 'NONE', ( #12867, #33062, #8775, #27301 ) ) ;
#11400=CARTESIAN_POINT ( 'NONE',  ( 20.92250000136559507, 0.3178988483021036315, 3.024605502323848949 ) ) ;
#11403=CARTESIAN_POINT ( 'NONE',  ( 25.75999999999999801, -2.208672634433321348E-15, 0.000000000000000000 ) ) ;
#11416=AXIS2_PLACEMENT_3D ( 'NONE', #19245, #888, #24079 ) ;
#11434=DIRECTION ( 'NONE',  ( -1.000000000000000000, 8.574039729943019576E-17, -0.000000000000000000 ) ) ;
#11436=FACE_BOUND ( 'NONE', #21295, .T. ) ;
#11443=FACE_OUTER_BOUND ( 'NONE', #23328, .T. ) ;
#11444=EDGE_CURVE ( 'NONE', #16406, #22729, #27537, .T. ) ;
#11452=ORIENTED_EDGE ( 'NONE', *, *, #21954, .T. ) ;
#11458=LINE ( 'NONE', #16614, #19887 ) ;
#11468=PLANE ( 'NONE',  #5455 ) ;
#11472=CARTESIAN_POINT ( 'NONE',  ( 21.35999999999999943, -1.573300977624594976, 1.942864903642425700 ) ) ;
#11483=ORIENTED_EDGE ( 'NONE', *, *, #20651, .T. ) ;
#11486=ORIENTED_EDGE ( 'NONE', *, *, #2650, .T. ) ;
#11496=CARTESIAN_POINT ( 'NONE',  ( 25.64588685331300510, 2.156159481431626279, -1.970234872520904901 ) ) ;
#11497=ORIENTED_EDGE ( 'NONE', *, *, #1517, .F. ) ;
#11501=DIRECTION ( 'NONE',  ( 3.623545766764117864E-17, 0.4226182617406882835, 0.9063077870366551547 ) ) ;
#11505=CARTESIAN_POINT ( 'NONE',  ( 24.49290772595112742, 0.1310194482076003919, 2.499999999999998668 ) ) ;
#11507=ORIENTED_EDGE ( 'NONE', *, *, #6571, .F. ) ;
#11513=CARTESIAN_POINT ( 'NONE',  ( 0.000000000000000000, 0.000000000000000000, 0.000000000000000000 ) ) ;
#11516=FACE_OUTER_BOUND ( 'NONE', #7721, .T. ) ;
#11523=CARTESIAN_POINT ( 'NONE',  ( 10.57125986779756843, 4.681538312723528605, -0.8254815157534771686 ) ) ;
#11528=CARTESIAN_POINT ( 'NONE',  ( 24.42249999999999943, -2.378061970571983430, 1.291182301015471490 ) ) ;
#11530=CARTESIAN_POINT ( 'NONE',  ( 22.23500000000000298, 0.2613211581691317065, 2.486304738420681559 ) ) ;
#11531=DIRECTION ( 'NONE',  ( -1.000000000000000000, 8.574039729943018344E-17, -0.000000000000000000 ) ) ;
#11543=CARTESIAN_POINT ( 'NONE',  ( 23.23500000273119070, 2.486304738420679783, -0.2613211581691337604 ) ) ;
#11546=EDGE_CURVE ( 'NONE', #20076, #6604, #792, .T. ) ;
#11568=LINE ( 'NONE', #32482, #32549 ) ;
#11577=DIRECTION ( 'NONE',  ( 8.574039729943018344E-17, 1.000000000000000000, 0.000000000000000000 ) ) ;
#11578=EDGE_CURVE ( 'NONE', #4101, #9572, #8448, .T. ) ;
#11586=PLANE ( 'NONE',  #25197 ) ;
#11587=DIRECTION ( 'NONE',  ( -1.000000000000000000, 8.574039729943018344E-17, 0.000000000000000000 ) ) ;
#11589=CARTESIAN_POINT ( 'NONE',  ( 25.05656763645044904, 0.8852964313267434049, -2.499999999999997780 ) ) ;
#11592=ORIENTED_EDGE ( 'NONE', *, *, #28848, .F. ) ;
#11599=ORIENTED_EDGE ( 'NONE', *, *, #15508, .F. ) ;
#11601=CARTESIAN_POINT ( 'NONE',  ( 23.23500000136559862, -1.570731468192933633, -2.892927487894330962 ) ) ;
#11602=EDGE_CURVE ( 'NONE', #4019, #15085, #20832, .T. ) ;
#11603=ORIENTED_EDGE ( 'NONE', *, *, #13508, .T. ) ;
#11608=CARTESIAN_POINT ( 'NONE',  ( 21.67250000273118715, -2.378061970571983430, 1.291182301015471490 ) ) ;
#11610=EDGE_CURVE ( 'NONE', #17346, #27475, #26027, .T. ) ;
#11616=DIRECTION ( 'NONE',  ( 1.000000000000000000, -0.000000000000000000, -0.000000000000000000 ) ) ;
#11625=ORIENTED_EDGE ( 'NONE', *, *, #32353, .T. ) ;
#11630=ORIENTED_EDGE ( 'NONE', *, *, #11578, .F. ) ;
#11636=DIRECTION ( 'NONE',  ( 7.472768010111188679E-18, 0.08715574274765867935, -0.9961946980917455452 ) ) ;
#11637=EDGE_LOOP ( 'NONE', ( #17904, #8509, #31405, #7747 ) ) ;
#11641=DIRECTION ( 'NONE',  ( 1.000000000000000000, -8.574039729943018344E-17, -0.000000000000000000 ) ) ;
#11658=CARTESIAN_POINT ( 'NONE',  ( 10.00000000000000178, -4.884328206559832353, -1.115095498423360754 ) ) ;
#11667=CARTESIAN_POINT ( 'NONE',  ( 20.86000000136559507, 0.3178988483021036315, 3.024605502323848949 ) ) ;
#11672=VERTEX_POINT ( 'NONE', #8605 ) ;
#11680=CARTESIAN_POINT ( 'NONE',  ( 25.75999999999999801, -2.208672634433321348E-15, 0.000000000000000000 ) ) ;
#11683=CARTESIAN_POINT ( 'NONE',  ( 21.60999999999999943, -1.942864903642428587, -1.573300977624592756 ) ) ;
#11685=DIRECTION ( 'NONE',  ( -7.472768010112310340E-18, -0.08715574274767159957, 0.9961946980917444350 ) ) ;
#11696=CARTESIAN_POINT ( 'NONE',  ( 20.86000000273118715, -1.942864903642428587, -1.573300977624592756 ) ) ;
#11700=DIRECTION ( 'NONE',  ( 1.000000000000000000, -8.574039729943018344E-17, -0.000000000000000000 ) ) ;
#11712=VECTOR ( 'NONE', #30006, 1000.000000000000114 ) ;
#11718=ORIENTED_EDGE ( 'NONE', *, *, #25443, .F. ) ;
#11720=ADVANCED_FACE ( 'NONE', ( #11289 ), #11771, .F. ) ;
#11721=CARTESIAN_POINT ( 'NONE',  ( 23.54750000000000654, -2.594547506269383685, -0.7685399846772043020 ) ) ;
#11732=CARTESIAN_POINT ( 'NONE',  ( 10.00000000000000000, 4.467071865485470639, 1.625881193364712596 ) ) ;
#11735=FACE_OUTER_BOUND ( 'NONE', #11399, .T. ) ;
#11736=CARTESIAN_POINT ( 'NONE',  ( 0.000000000000000000, 0.000000000000000000, 0.000000000000000000 ) ) ;
#11759=ORIENTED_EDGE ( 'NONE', *, *, #4999, .F. ) ;
#11761=CARTESIAN_POINT ( 'NONE',  ( 21.17250000136559507, -2.363507492473152283, -1.913930629741525280 ) ) ;
#11763=PLANE ( 'NONE',  #27390 ) ;
#11766=LINE ( 'NONE', #30004, #30997 ) ;
#11768=CARTESIAN_POINT ( 'NONE',  ( 10.00000000000000000, -3.641590349731949505, 3.055657119358789142 ) ) ;
#11771=PLANE ( 'NONE',  #28508 ) ;
#11779=DIRECTION ( 'NONE',  ( 1.000000000000000000, -8.574039729943018344E-17, -0.000000000000000000 ) ) ;
#11794=DIRECTION ( 'NONE',  ( -6.062761635205610267E-17, -0.7071067811865509034, 0.7071067811865441310 ) ) ;
#11806=AXIS2_PLACEMENT_3D ( 'NONE', #18874, #21212, #23380 ) ;
#11811=CARTESIAN_POINT ( 'NONE',  ( 10.57125986779756843, -4.681538312723523276, 0.8254815157535098091 ) ) ;
#11813=DIRECTION ( 'NONE',  ( 1.000000000000000000, -8.574039729943018344E-17, -0.000000000000000000 ) ) ;
#11816=VECTOR ( 'NONE', #27528, 999.9999999999998863 ) ;
#11818=ORIENTED_EDGE ( 'NONE', *, *, #18827, .T. ) ;
#11819=DIRECTION ( 'NONE',  ( 8.574039729943018344E-17, 1.000000000000000000, 0.000000000000000000 ) ) ;
#11825=CARTESIAN_POINT ( 'NONE',  ( 10.57125986779756843, 4.681538312723516171, 0.8254815157535410064 ) ) ;
#11827=LINE ( 'NONE', #9321, #5989 ) ;
#11846=ORIENTED_EDGE ( 'NONE', *, *, #27024, .T. ) ;
#11853=CARTESIAN_POINT ( 'NONE',  ( 10.00000000000000000, -2.376879293651093406, 4.116875700062075261 ) ) ;
#11861=CARTESIAN_POINT ( 'NONE',  ( 24.85999999999999943, 1.573300977624590313, -1.942864903642426144 ) ) ;
#11871=AXIS2_PLACEMENT_3D ( 'NONE', #5195, #17722, #25259 ) ;
#11873=LINE ( 'NONE', #16536, #25656 ) ;
#11876=EDGE_CURVE ( 'NONE', #18235, #30423, #27815, .T. ) ;
#11879=CARTESIAN_POINT ( 'NONE',  ( 10.56870887191539587, 4.467071865485470639, 1.625881193364712596 ) ) ;
#11880=CARTESIAN_POINT ( 'NONE',  ( 24.73500000136559507, 3.156283516753366047, 0.9349337715887203748 ) ) ;
#11885=CARTESIAN_POINT ( 'NONE',  ( 10.00000000000000000, -0.8254815157534942660, -4.681538312723525053 ) ) ;
#11891=CARTESIAN_POINT ( 'NONE',  ( -2.921917104085828724E-16, -3.407865132560154997, -3.672404558090073490 ) ) ;
#11893=EDGE_CURVE ( 'NONE', #26782, #25696, #30510, .T. ) ;
#11895=VECTOR ( 'NONE', #3739, 1000.000000000000227 ) ;
#11896=LINE ( 'NONE', #27600, #25753 ) ;
#11901=ORIENTED_EDGE ( 'NONE', *, *, #23455, .F. ) ;
#11910=VECTOR ( 'NONE', #16870, 1000.000000000000000 ) ;
#11922=ADVANCED_FACE ( 'NONE', ( #24822 ), #16955, .F. ) ;
#11927=CARTESIAN_POINT ( 'NONE',  ( 24.23500000136559507, -1.570731468192933633, -2.892927487894330074 ) ) ;
#11946=VECTOR ( 'NONE', #27556, 1000.000000000000000 ) ;
#11952=CARTESIAN_POINT ( 'NONE',  ( 21.54750000136559507, 3.024605502323846729, -0.3178988483021056854 ) ) ;
#11959=DIRECTION ( 'NONE',  ( -1.000000000000000000, -0.000000000000000000, -0.000000000000000000 ) ) ;
#11962=CARTESIAN_POINT ( 'NONE',  ( 25.36000000136559862, 0.9349337715887185984, -3.156283516753368268 ) ) ;
#11967=DIRECTION ( 'NONE',  ( -2.219124775574878265E-17, -0.2588190451025149663, -0.9659258262890698665 ) ) ;
#11980=ORIENTED_EDGE ( 'NONE', *, *, #5999, .F. ) ;
#11981=CARTESIAN_POINT ( 'NONE',  ( 10.56183597391177464, 0.2499999999999808209, 5.003758587302149508 ) ) ;
#11995=DIRECTION ( 'NONE',  ( 8.574039729943018344E-17, 1.000000000000000000, 0.000000000000000000 ) ) ;
#11997=CARTESIAN_POINT ( 'NONE',  ( 25.62966469407293602, 1.793355229293301489, -2.284851768092018176 ) ) ;
#12002=LINE ( 'NONE', #4639, #21493 ) ;
#12006=CARTESIAN_POINT ( 'NONE',  ( 0.000000000000000000, 0.000000000000000000, 0.000000000000000000 ) ) ;
#12013=EDGE_CURVE ( 'NONE', #545, #2120, #28655, .T. ) ;
#12014=CARTESIAN_POINT ( 'NONE',  ( 20.61000000273118715, -1.573300977624594976, 1.942864903642425700 ) ) ;
#12032=DIRECTION ( 'NONE',  ( 0.000000000000000000, -0.2588190451025184080, -0.9659258262890689783 ) ) ;
#12034=CARTESIAN_POINT ( 'NONE',  ( 25.42249999999999943, -2.378061970571983430, 1.291182301015471712 ) ) ;
#12061=CARTESIAN_POINT ( 'NONE',  ( 10.00000000000000000, -4.467071865485483961, 1.625881193364682842 ) ) ;
#12084=ADVANCED_FACE ( 'NONE', ( #8414 ), #31665, .T. ) ;
#12087=PLANE ( 'NONE',  #25229 ) ;
#12092=EDGE_LOOP ( 'NONE', ( #14237, #20173, #12477, #9151 ) ) ;
#12093=DIRECTION ( 'NONE',  ( 1.000000000000000000, -8.574039729943018344E-17, -0.000000000000000000 ) ) ;
#12105=CARTESIAN_POINT ( 'NONE',  ( 23.79750000136559507, 0.3178988483021036315, 3.024605502323848949 ) ) ;
#12107=DIRECTION ( 'NONE',  ( 1.000000000000000000, -8.574039729943018344E-17, -0.000000000000000000 ) ) ;
#12113=CARTESIAN_POINT ( 'NONE',  ( 22.54750000136559507, 3.024605502323846729, -0.3178988483021056854 ) ) ;
#12115=EDGE_CURVE ( 'NONE', #26383, #22729, #3581, .T. ) ;
#12132=ORIENTED_EDGE ( 'NONE', *, *, #29979, .T. ) ;
#12141=CARTESIAN_POINT ( 'NONE',  ( 10.57125986779756843, 0.8254815157535241310, 4.681538312723519724 ) ) ;
#12146=PLANE ( 'NONE',  #2875 ) ;
#12149=EDGE_LOOP ( 'NONE', ( #836, #26040, #7315, #23333 ) ) ;
#12160=CARTESIAN_POINT ( 'NONE',  ( 20.92250000273118715, -1.291182301015472600, -2.378061970571982098 ) ) ;
#12161=VERTEX_POINT ( 'NONE', #11732 ) ;
#12163=CARTESIAN_POINT ( 'NONE',  ( 24.98500000136559507, -0.9349337715887248157, 3.156283516753367824 ) ) ;
#12173=ADVANCED_FACE ( 'NONE', ( #21772 ), #11245, .T. ) ;
#12176=FACE_OUTER_BOUND ( 'NONE', #21680, .T. ) ;
#12179=CARTESIAN_POINT ( 'NONE',  ( 25.75999999999999801, -2.208672634433321348E-15, 0.000000000000000000 ) ) ;
#12180=CARTESIAN_POINT ( 'NONE',  ( 25.61000000136559507, 2.892927487894327410, -1.570731468192931635 ) ) ;
#12195=CARTESIAN_POINT ( 'NONE',  ( 24.29750000136559507, -2.363507492473152283, -1.913930629741525280 ) ) ;
#12198=DIRECTION ( 'NONE',  ( -1.000000000000000000, 8.574039729943018344E-17, -0.000000000000000000 ) ) ;
#12205=CYLINDRICAL_SURFACE ( 'NONE', #20414, 5.010000000000000675 ) ;
#12228=CARTESIAN_POINT ( 'NONE',  ( 23.05656763645045615, 0.8852964313267427388, -2.499999999999999112 ) ) ;
#12229=CARTESIAN_POINT ( 'NONE',  ( 23.86000000136559507, -0.9349337715887248157, 3.156283516753367824 ) ) ;
#12240=EDGE_CURVE ( 'NONE', #14180, #4101, #22619, .T. ) ;
#12248=CARTESIAN_POINT ( 'NONE',  ( 10.57125986779756843, -4.681538312723512618, -0.8254815157535732029 ) ) ;
#12249=LINE ( 'NONE', #30334, #8535 ) ;
#12250=ORIENTED_EDGE ( 'NONE', *, *, #19952, .T. ) ;
#12252=CARTESIAN_POINT ( 'NONE',  ( 22.29750000136559507, -0.3178988483021076838, -3.024605502323848949 ) ) ;
#12253=EDGE_CURVE ( 'NONE', #20952, #3262, #32268, .T. ) ;
#12262=CARTESIAN_POINT ( 'NONE',  ( 25.79750000136559507, 0.3178988483021036315, 3.024605502323848949 ) ) ;
#12263=CARTESIAN_POINT ( 'NONE',  ( 10.56870887191539587, -1.625881193364669297, -4.467071865485488402 ) ) ;
#12266=CARTESIAN_POINT ( 'NONE',  ( 3.424298583717193057E-16, 3.993798362933351775, -3.024842911000649615 ) ) ;
#12271=CARTESIAN_POINT ( 'NONE',  ( 10.52034268205830259, -3.055657119358826446, 3.641590349731918863 ) ) ;
#12283=ORIENTED_EDGE ( 'NONE', *, *, #2050, .T. ) ;
#12289=DIRECTION ( 'NONE',  ( 1.000000000000000000, -8.574039729943018344E-17, -0.000000000000000000 ) ) ;
#12291=DIRECTION ( 'NONE',  ( 0.000000000000000000, 0.9961946980917454342, 0.08715574274765866547 ) ) ;
#12322=CIRCLE ( 'NONE', #8577, 5.000000000000003553 ) ;
#12329=AXIS2_PLACEMENT_3D ( 'NONE', #32744, #4492, #7647 ) ;
#12342=CARTESIAN_POINT ( 'NONE',  ( 20.74999999999999645, 5.999999999999998224, 0.000000000000000000 ) ) ;
#12344=CARTESIAN_POINT ( 'NONE',  ( 23.36000000136559507, -1.570731468192933633, -2.892927487894330074 ) ) ;
#12350=VECTOR ( 'NONE', #13465, 1000.000000000000114 ) ;
#12352=DIRECTION ( 'NONE',  ( -3.623545766764274403E-17, -0.4226182617407064912, 0.9063077870366467170 ) ) ;
#12360=CARTESIAN_POINT ( 'NONE',  ( 25.75999999999999801, -2.208672634433321348E-15, 0.000000000000000000 ) ) ;
#12364=CIRCLE ( 'NONE', #32697, 5.009999999999999787 ) ;
#12368=ADVANCED_FACE ( 'NONE', ( #4215 ), #22431, .T. ) ;
#12369=CARTESIAN_POINT ( 'NONE',  ( 25.04749999999999943, 2.594547506269380133, 0.7685399846772031918 ) ) ;
#12372=ORIENTED_EDGE ( 'NONE', *, *, #2650, .F. ) ;
#12376=ORIENTED_EDGE ( 'NONE', *, *, #1514, .F. ) ;
#12387=CARTESIAN_POINT ( 'NONE',  ( 23.42250000000000298, -2.378061970571983430, 1.291182301015471490 ) ) ;
#12389=LINE ( 'NONE', #9219, #28931 ) ;
#12398=CARTESIAN_POINT ( 'NONE',  ( 25.75999999999999801, -2.208672634433321348E-15, 0.000000000000000000 ) ) ;
#12403=CARTESIAN_POINT ( 'NONE',  ( 25.67250000136559507, 2.363507492473148286, 1.913930629741525058 ) ) ;
#12407=CIRCLE ( 'NONE', #15642, 5.010000000000000675 ) ;
#12412=EDGE_CURVE ( 'NONE', #3558, #14852, #23418, .T. ) ;
#12426=CONICAL_SURFACE ( 'NONE', #14009, 3.024999999999999911, 0.7853981633974520538 ) ;
#12432=AXIS2_PLACEMENT_3D ( 'NONE', #7516, #25420, #23389 ) ;
#12433=CYLINDRICAL_SURFACE ( 'NONE', #2154, 5.010000000000000675 ) ;
#12434=ORIENTED_EDGE ( 'NONE', *, *, #6276, .T. ) ;
#12439=AXIS2_PLACEMENT_3D ( 'NONE', #31800, #11700, #19078 ) ;
#12477=ORIENTED_EDGE ( 'NONE', *, *, #27272, .F. ) ;
#12479=EDGE_CURVE ( 'NONE', #24378, #7137, #18430, .T. ) ;
#12484=VECTOR ( 'NONE', #24500, 1000.000000000000000 ) ;
#12485=DIRECTION ( 'NONE',  ( 1.000000000000000000, -8.574039729943018344E-17, -0.000000000000000000 ) ) ;
#12501=CARTESIAN_POINT ( 'NONE',  ( 24.29750000273118715, 2.594547506269380133, 0.7685399846772031918 ) ) ;
#12524=CARTESIAN_POINT ( 'NONE',  ( 10.00000000000000000, 0.8254815157535864145, -4.681538312723508177 ) ) ;
#12526=CARTESIAN_POINT ( 'NONE',  ( 24.67250000136559507, 3.024605502323846729, -0.3178988483021056854 ) ) ;
#12542=CARTESIAN_POINT ( 'NONE',  ( 21.42250000136559507, -0.3178988483021076838, -3.024605502323848949 ) ) ;
#12555=VERTEX_POINT ( 'NONE', #10552 ) ;
#12562=LINE ( 'NONE', #7726, #7084 ) ;
#12565=ORIENTED_EDGE ( 'NONE', *, *, #25836, .F. ) ;
#12569=EDGE_CURVE ( 'NONE', #3086, #18770, #20763, .T. ) ;
#12597=ORIENTED_EDGE ( 'NONE', *, *, #26446, .T. ) ;
#12603=ORIENTED_EDGE ( 'NONE', *, *, #8514, .T. ) ;
#12623=ORIENTED_EDGE ( 'NONE', *, *, #90, .F. ) ;
#12631=ORIENTED_EDGE ( 'NONE', *, *, #19067, .T. ) ;
#12632=ORIENTED_EDGE ( 'NONE', *, *, #23778, .F. ) ;
#12644=ORIENTED_EDGE ( 'NONE', *, *, #14113, .F. ) ;
#12653=CARTESIAN_POINT ( 'NONE',  ( 10.56870887191539587, 1.625881193364696831, 4.467071865485476856 ) ) ;
#12659=CARTESIAN_POINT ( 'NONE',  ( 24.73500000136559507, 3.156283516753366047, 0.9349337715887203748 ) ) ;
#12677=CARTESIAN_POINT ( 'NONE',  ( 3.529825581556955655E-16, 4.116875700062116117, -2.376879293651021019 ) ) ;
#12678=CARTESIAN_POINT ( 'NONE',  ( 25.23500000136559507, -3.156283516753370044, -0.9349337715887220401 ) ) ;
#12685=CARTESIAN_POINT ( 'NONE',  ( 22.10999999999999943, 1.942864903642424146, 1.573300977624592534 ) ) ;
#12689=FACE_OUTER_BOUND ( 'NONE', #30801, .T. ) ;
#12691=CARTESIAN_POINT ( 'NONE',  ( 21.67250000136559507, 3.024605502323846729, -0.3178988483021056854 ) ) ;
#12699=ORIENTED_EDGE ( 'NONE', *, *, #3684, .T. ) ;
#12702=CARTESIAN_POINT ( 'NONE',  ( 3.830085165118310759E-16, 4.467071865485471527, 1.625881193364712596 ) ) ;
#12713=CARTESIAN_POINT ( 'NONE',  ( 10.00000000000000000, 2.376879293651121383, -4.116875700062057497 ) ) ;
#12715=LINE ( 'NONE', #20913, #7573 ) ;
#12716=DIRECTION ( 'NONE',  ( 1.000000000000000000, -8.574039729943018344E-17, -0.000000000000000000 ) ) ;
#12717=ORIENTED_EDGE ( 'NONE', *, *, #16698, .F. ) ;
#12719=CARTESIAN_POINT ( 'NONE',  ( 10.56870887191539587, 1.625881193364696831, 4.467071865485476856 ) ) ;
#12726=CARTESIAN_POINT ( 'NONE',  ( 24.73500000273118715, -2.486304738420683780, 0.2613211581691335383 ) ) ;
#12727=DIRECTION ( 'NONE',  ( -8.541412920197208721E-17, -0.9961946980917449901, -0.08715574274766461904 ) ) ;
#12735=LINE ( 'NONE', #7753, #651 ) ;
#12746=VERTEX_POINT ( 'NONE', #30563 ) ;
#12748=FACE_OUTER_BOUND ( 'NONE', #15704, .T. ) ;
#12765=LINE ( 'NONE', #93, #29530 ) ;
#12776=CARTESIAN_POINT ( 'NONE',  ( 0.000000000000000000, 0.000000000000000000, 0.000000000000000000 ) ) ;
#12778=EDGE_LOOP ( 'NONE', ( #6669, #9009, #21572, #20425 ) ) ;
#12781=ORIENTED_EDGE ( 'NONE', *, *, #15421, .F. ) ;
#12783=( BOUNDED_CURVE ( )  B_SPLINE_CURVE ( 2, ( #778, #11272, #3455, #29165, #28529, #10960, #13439, #6253, #23660, #592, #8436 ),
 .UNSPECIFIED., .F., .F. ) 
 B_SPLINE_CURVE_WITH_KNOTS ( ( 3, 2, 2, 2, 2, 3 ),
 ( 0.5966116191895003418, 0.5999999999999999778, 0.6250000000000000000, 0.6500000000000000222, 0.6750000000000000444, 0.6966116191895003196 ),
 .UNSPECIFIED. ) 
 CURVE ( )  GEOMETRIC_REPRESENTATION_ITEM ( )  RATIONAL_B_SPLINE_CURVE ( ( 0.9821626249036858880, 0.9896829947469992783, 1.000000000000000000, 0.9238795325112867385, 1.000000000000000000, 0.9238795325112867385, 1.000000000000000000, 0.9238795325112867385, 1.000000000000000000, 0.9341965377642874602, 0.9821626249036858880 ) ) 
 REPRESENTATION_ITEM ( '' )  );
#12784=LINE ( 'NONE', #2115, #26715 ) ;
#12790=CARTESIAN_POINT ( 'NONE',  ( 10.52034268205830259, -3.993798362933288271, -3.024842911000732215 ) ) ;
#12803=EDGE_CURVE ( 'NONE', #32781, #9763, #23009, .T. ) ;
#12809=EDGE_CURVE ( 'NONE', #31932, #22762, #28048, .T. ) ;
#12822=AXIS2_PLACEMENT_3D ( 'NONE', #15235, #15386, #28262 ) ;
#12828=LINE ( 'NONE', #22561, #15534 ) ;
#12829=CARTESIAN_POINT ( 'NONE',  ( 23.48500000136559862, 0.9349337715887185984, -3.156283516753368268 ) ) ;
#12830=EDGE_CURVE ( 'NONE', #26383, #17238, #5048, .T. ) ;
#12838=CARTESIAN_POINT ( 'NONE',  ( 22.25111450864416085, -3.256483526998273983E-15, 2.499999999999998668 ) ) ;
#12846=CARTESIAN_POINT ( 'NONE',  ( 22.98500000136559862, -0.9349337715887247047, 3.156283516753367824 ) ) ;
#12858=EDGE_CURVE ( 'NONE', #31776, #10511, #15167, .T. ) ;
#12867=ORIENTED_EDGE ( 'NONE', *, *, #8760, .T. ) ;
#12873=CARTESIAN_POINT ( 'NONE',  ( 25.75999999999999801, -2.208672634433321348E-15, 0.000000000000000000 ) ) ;
#12883=CARTESIAN_POINT ( 'NONE',  ( 21.29750000136559507, -2.363507492473152283, -1.913930629741525280 ) ) ;
#12885=CYLINDRICAL_SURFACE ( 'NONE', #26199, 5.010000000000000675 ) ;
#12889=AXIS2_PLACEMENT_3D ( 'NONE', #13914, #23958, #21472 ) ;
#12891=CARTESIAN_POINT ( 'NONE',  ( 21.86000000136559507, -0.9349337715887248157, 3.156283516753367824 ) ) ;
#12904=AXIS2_PLACEMENT_3D ( 'NONE', #12939, #10756, #18118 ) ;
#12906=CARTESIAN_POINT ( 'NONE',  ( 25.46715431016588482, 2.408328468251813348, 1.329981640288168121 ) ) ;
#12908=CARTESIAN_POINT ( 'NONE',  ( 0.000000000000000000, 0.000000000000000000, 0.000000000000000000 ) ) ;
#12915=ORIENTED_EDGE ( 'NONE', *, *, #1094, .F. ) ;
#12917=DIRECTION ( 'NONE',  ( 0.000000000000000000, 1.000000000000000000, 0.000000000000000000 ) ) ;
#12920=CARTESIAN_POINT ( 'NONE',  ( 10.56870887191539587, 4.467071865485470639, 1.625881193364712596 ) ) ;
#12922=VERTEX_POINT ( 'NONE', #26033 ) ;
#12926=AXIS2_PLACEMENT_3D ( 'NONE', #14215, #24572, #16897 ) ;
#12933=CARTESIAN_POINT ( 'NONE',  ( 10.55147673363119232, -2.285372942704923194, -4.458382051008217495 ) ) ;
#12935=AXIS2_PLACEMENT_3D ( 'NONE', #9940, #10277, #20154 ) ;
#12939=CARTESIAN_POINT ( 'NONE',  ( 10.56870887191539587, 4.467071865485470639, 1.625881193364712596 ) ) ;
#12944=AXIS2_PLACEMENT_3D ( 'NONE', #24537, #32432, #1660 ) ;
#12954=CONICAL_SURFACE ( 'NONE', #8138, 2.499999999999996891, 1.029744258676653867 ) ;
#12968=EDGE_LOOP ( 'NONE', ( #8783, #18853, #31651, #30444 ) ) ;
#12974=CARTESIAN_POINT ( 'NONE',  ( 21.24290772321993970, 0.1310194482076003919, 2.499999999999998668 ) ) ;
#12976=ORIENTED_EDGE ( 'NONE', *, *, #5515, .T. ) ;
#12980=CARTESIAN_POINT ( 'NONE',  ( 10.00000000000000000, -1.745506336992504507E-14, 4.753758587302147731 ) ) ;
#12986=CYLINDRICAL_SURFACE ( 'NONE', #15617, 5.010000000000000675 ) ;
#13016=DIRECTION ( 'NONE',  ( 8.541412920197216117E-17, 0.9961946980917455452, -0.08715574274765799934 ) ) ;
#13024=CARTESIAN_POINT ( 'NONE',  ( 20.92250000136559507, 0.3178988483021036315, 3.024605502323848949 ) ) ;
#13026=ADVANCED_FACE ( 'NONE', ( #2810 ), #13632, .F. ) ;
#13027=LINE ( 'NONE', #11153, #29907 ) ;
#13028=ORIENTED_EDGE ( 'NONE', *, *, #30235, .F. ) ;
#13041=CARTESIAN_POINT ( 'NONE',  ( 23.23500000136559862, -3.156283516753370488, -0.9349337715887220401 ) ) ;
#13042=CARTESIAN_POINT ( 'NONE',  ( 10.00000000000000000, 4.681538312723528605, -0.8254815157534769465 ) ) ;
#13052=ORIENTED_EDGE ( 'NONE', *, *, #16111, .T. ) ;
#13056=VERTEX_POINT ( 'NONE', #1439 ) ;
#13070=CARTESIAN_POINT ( 'NONE',  ( 23.17250000136559862, -2.363507492473152283, -1.913930629741525280 ) ) ;
#13078=CARTESIAN_POINT ( 'NONE',  ( 21.29750000136559507, -0.3178988483021076838, -3.024605502323848949 ) ) ;
#13094=ORIENTED_EDGE ( 'NONE', *, *, #5006, .T. ) ;
#13098=CARTESIAN_POINT ( 'NONE',  ( 10.56870887191539587, 4.787500056513365188, 1.476463073999653819 ) ) ;
#13099=ORIENTED_EDGE ( 'NONE', *, *, #18600, .T. ) ;
#13100=ORIENTED_EDGE ( 'NONE', *, *, #6525, .T. ) ;
#13104=ORIENTED_EDGE ( 'NONE', *, *, #10150, .T. ) ;
#13119=LINE ( 'NONE', #16102, #16175 ) ;
#13121=EDGE_CURVE ( 'NONE', #21706, #7070, #29183, .T. ) ;
#13122=CARTESIAN_POINT ( 'NONE',  ( 25.38274187136685356, -2.592012193576345158, 0.5676849011231037689 ) ) ;
#13123=DIRECTION ( 'NONE',  ( 1.000000000000000000, -8.574039729943018344E-17, -0.000000000000000000 ) ) ;
#13133=EDGE_CURVE ( 'NONE', #19939, #7714, #19316, .T. ) ;
#13135=CARTESIAN_POINT ( 'NONE',  ( 21.23499999999999943, 0.2613211581691317065, 2.486304738420681559 ) ) ;
#13136=LINE ( 'NONE', #28185, #1600 ) ;
#13137=ORIENTED_EDGE ( 'NONE', *, *, #24429, .T. ) ;
#13152=ORIENTED_EDGE ( 'NONE', *, *, #30275, .F. ) ;
#13159=VERTEX_POINT ( 'NONE', #6614 ) ;
#13167=ADVANCED_FACE ( 'NONE', ( #16626 ), #29689, .F. ) ;
#13174=CARTESIAN_POINT ( 'NONE',  ( 22.29750000136559507, -2.363507492473152283, -1.913930629741525280 ) ) ;
#13178=CARTESIAN_POINT ( 'NONE',  ( 10.57125986779756843, -4.681538312723512618, -0.8254815157535732029 ) ) ;
#13180=ORIENTED_EDGE ( 'NONE', *, *, #6, .F. ) ;
#13184=CARTESIAN_POINT ( 'NONE',  ( 23.79750000136559507, 2.363507492473148286, 1.913930629741525058 ) ) ;
#13186=CARTESIAN_POINT ( 'NONE',  ( 10.00000000000000178, -8.574039729943018837E-16, 0.000000000000000000 ) ) ;
#13192=ORIENTED_EDGE ( 'NONE', *, *, #22289, .F. ) ;
#13202=EDGE_LOOP ( 'NONE', ( #1545, #21013, #28681, #27582 ) ) ;
#13205=FACE_OUTER_BOUND ( 'NONE', #2255, .T. ) ;
#13207=CARTESIAN_POINT ( 'NONE',  ( 10.00000000000000178, -4.208382051008173086, -2.718385644597221873 ) ) ;
#13214=CARTESIAN_POINT ( 'NONE',  ( 21.23500000136559507, -1.570731468192933633, -2.892927487894330074 ) ) ;
#13216=CARTESIAN_POINT ( 'NONE',  ( 4.075891499408641642E-16, 4.753758587302147731, 0.000000000000000000 ) ) ;
#13217=ORIENTED_EDGE ( 'NONE', *, *, #7722, .F. ) ;
#13221=CARTESIAN_POINT ( 'NONE',  ( 25.42250000273118360, 1.291182301015469047, 2.378061970571981654 ) ) ;
#13223=CARTESIAN_POINT ( 'NONE',  ( -3.122314033877883927E-16, -3.641590349731949505, 3.055657119358789142 ) ) ;
#13226=ORIENTED_EDGE ( 'NONE', *, *, #8134, .F. ) ;
#13228=EDGE_CURVE ( 'NONE', #866, #7332, #2381, .T. ) ;
#13229=LINE ( 'NONE', #17941, #18838 ) ;
#13233=EDGE_CURVE ( 'NONE', #6857, #31196, #24794, .T. ) ;
#13245=CARTESIAN_POINT ( 'NONE',  ( 25.75999999999999801, -1.902510934646483477E-15, 2.499999999999997780 ) ) ;
#13248=ORIENTED_EDGE ( 'NONE', *, *, #25009, .T. ) ;
#13249=ORIENTED_EDGE ( 'NONE', *, *, #13233, .T. ) ;
#13250=CARTESIAN_POINT ( 'NONE',  ( 10.00000000000000178, -8.574039729943018837E-16, 0.000000000000000000 ) ) ;
#13256=CARTESIAN_POINT ( 'NONE',  ( 4.290242492657217039E-16, 5.003758587302148619, 0.2500000000000008882 ) ) ;
#13260=CARTESIAN_POINT ( 'NONE',  ( 10.00000000000000178, 4.458382051008225488, -2.285372942704905430 ) ) ;
#13267=CARTESIAN_POINT ( 'NONE',  ( 22.92250000136559862, 0.3178988483021036315, 3.024605502323848949 ) ) ;
#13277=VERTEX_POINT ( 'NONE', #19808 ) ;
#13281=DIRECTION ( 'NONE',  ( 7.472768010112066903E-18, 0.08715574274766894891, -0.9961946980917446570 ) ) ;
#13297=CARTESIAN_POINT ( 'NONE',  ( 22.98500000273118715, -0.2613211581691358698, -2.486304738420681559 ) ) ;
#13309=AXIS2_PLACEMENT_3D ( 'NONE', #19602, #29963, #6726 ) ;
#13324=AXIS2_PLACEMENT_3D ( 'NONE', #9266, #19488, #29680 ) ;
#13343=AXIS2_PLACEMENT_3D ( 'NONE', #24547, #1859, #32099 ) ;
#13352=LINE ( 'NONE', #10877, #3888 ) ;
#13354=VERTEX_POINT ( 'NONE', #5426 ) ;
#13355=ORIENTED_EDGE ( 'NONE', *, *, #4938, .F. ) ;
#13368=VERTEX_POINT ( 'NONE', #5262 ) ;
#13371=EDGE_CURVE ( 'NONE', #3931, #8864, #10443, .T. ) ;
#13373=CARTESIAN_POINT ( 'NONE',  ( 20.92250000136559507, -1.913930629741527500, 2.363507492473149618 ) ) ;
#13376=CARTESIAN_POINT ( 'NONE',  ( 10.55147673363119232, 4.458382051008223712, -2.285372942704906762 ) ) ;
#13377=CARTESIAN_POINT ( 'NONE',  ( 10.00000000000000178, -8.574039729943018837E-16, 0.000000000000000000 ) ) ;
#13380=CARTESIAN_POINT ( 'NONE',  ( 10.00000000000000000, 4.753758587302147731, 2.969445807578340325E-16 ) ) ;
#13385=CYLINDRICAL_SURFACE ( 'NONE', #5947, 5.010000000000000675 ) ;
#13394=DIRECTION ( 'NONE',  ( 1.000000000000000000, -8.574039729943018344E-17, -0.000000000000000000 ) ) ;
#13399=EDGE_CURVE ( 'NONE', #29918, #5334, #25646, .T. ) ;
#13405=EDGE_CURVE ( 'NONE', #13354, #13368, #2761, .T. ) ;
#13408=CARTESIAN_POINT ( 'NONE',  ( 10.00000000000000000, 4.116875700062082366, 2.376879293651078751 ) ) ;
#13410=CIRCLE ( 'NONE', #26792, 3.024999999999999911 ) ;
#13422=EDGE_CURVE ( 'NONE', #32470, #29481, #13742, .T. ) ;
#13425=CARTESIAN_POINT ( 'NONE',  ( 23.17250000136559862, -3.024605502323851169, 0.3178988483021052969 ) ) ;
#13434=AXIS2_PLACEMENT_3D ( 'NONE', #8722, #31804, #18745 ) ;
#13439=CARTESIAN_POINT ( 'NONE',  ( 22.98500000000000298, 2.486304738420679783, -0.2613211581691337604 ) ) ;
#13442=CARTESIAN_POINT ( 'NONE',  ( 25.61000000136559507, 3.156283516753366047, 0.9349337715887203748 ) ) ;
#13455=DIRECTION ( 'NONE',  ( 0.000000000000000000, 1.000000000000000000, 0.000000000000000000 ) ) ;
#13465=DIRECTION ( 'NONE',  ( 3.623545766764298439E-17, 0.4226182617407088782, -0.9063077870366454958 ) ) ;
#13469=AXIS2_PLACEMENT_3D ( 'NONE', #28241, #30435, #15535 ) ;
#13476=VECTOR ( 'NONE', #26150, 1000.000000000000000 ) ;
#13492=FACE_OUTER_BOUND ( 'NONE', #21225, .T. ) ;
#13493=VECTOR ( 'NONE', #22699, 1000.000000000000114 ) ;
#13501=CARTESIAN_POINT ( 'NONE',  ( 21.92250000136559507, 0.3178988483021036315, 3.024605502323848949 ) ) ;
#13508=EDGE_CURVE ( 'NONE', #115, #12922, #28026, .T. ) ;
#13509=( GEOMETRIC_REPRESENTATION_CONTEXT ( 3 ) GLOBAL_UNCERTAINTY_ASSIGNED_CONTEXT ( ( #8900 ) ) GLOBAL_UNIT_ASSIGNED_CONTEXT ( ( #18799, #32315, #4550 ) ) REPRESENTATION_CONTEXT ( 'NONE', 'WORKASPACE' ) );
#13512=DIRECTION ( 'NONE',  ( -3.623545766764303986E-17, -0.4226182617407096553, 0.9063077870366452737 ) ) ;
#13541=CARTESIAN_POINT ( 'NONE',  ( 10.57125986779756843, -0.6226916219172400346, 4.971152295393299170 ) ) ;
#13544=AXIS2_PLACEMENT_3D ( 'NONE', #12398, #14385, #32647 ) ;
#13549=CARTESIAN_POINT ( 'NONE',  ( 21.61000000136559507, 3.156283516753366047, 0.9349337715887203748 ) ) ;
#13552=ORIENTED_EDGE ( 'NONE', *, *, #22410, .F. ) ;
#13554=LINE ( 'NONE', #4149, #2825 ) ;
#13555=CARTESIAN_POINT ( 'NONE',  ( 21.29750000273119070, 2.594547506269380133, 0.7685399846772031918 ) ) ;
#13569=ORIENTED_EDGE ( 'NONE', *, *, #20385, .F. ) ;
#13575=ORIENTED_EDGE ( 'NONE', *, *, #27526, .F. ) ;
#13591=LINE ( 'NONE', #28313, #20367 ) ;
#13592=CARTESIAN_POINT ( 'NONE',  ( 25.00111451137534146, -4.139597703811366476E-17, -2.499999999999998668 ) ) ;
#13601=CARTESIAN_POINT ( 'NONE',  ( 22.29750000136559507, -2.363507492473152283, -1.913930629741525280 ) ) ;
#13602=CARTESIAN_POINT ( 'NONE',  ( 25.55028516831285756, -0.3470411663994143470, -2.799286153339490379 ) ) ;
#13607=ORIENTED_EDGE ( 'NONE', *, *, #12569, .F. ) ;
#13612=DIRECTION ( 'NONE',  ( -1.000000000000000000, 8.574039729943018344E-17, -0.000000000000000000 ) ) ;
#13625=LINE ( 'NONE', #29024, #23997 ) ;
#13630=ADVANCED_FACE ( 'NONE', ( #1727 ), #9810, .T. ) ;
#13632=PLANE ( 'NONE',  #24262 ) ;
#13635=CARTESIAN_POINT ( 'NONE',  ( 22.67250000273118715, -2.378061970571983430, 1.291182301015471490 ) ) ;
#13638=CARTESIAN_POINT ( 'NONE',  ( 3.148734258548822534E-16, 3.672404558090086368, -3.407865132560142563 ) ) ;
#13644=CARTESIAN_POINT ( 'NONE',  ( 25.24521618911088794, -7.644457093038323125E-15, 2.510216189110891172 ) ) ;
#13658=ADVANCED_FACE ( 'NONE', ( #6696 ), #1683, .F. ) ;
#13661=CARTESIAN_POINT ( 'NONE',  ( 21.61000000136559507, 2.892927487894327410, -1.570731468192931635 ) ) ;
#13672=LINE ( 'NONE', #982, #31066 ) ;
#13674=FACE_OUTER_BOUND ( 'NONE', #2459, .T. ) ;
#13677=DIRECTION ( 'NONE',  ( 1.000000000000000000, -8.574039729943018344E-17, -0.000000000000000000 ) ) ;
#13681=VERTEX_POINT ( 'NONE', #9362 ) ;
#13690=ORIENTED_EDGE ( 'NONE', *, *, #14657, .T. ) ;
#13692=ORIENTED_EDGE ( 'NONE', *, *, #1917, .F. ) ;
#13705=CARTESIAN_POINT ( 'NONE',  ( 21.86000000136559507, -0.9349337715887248157, 3.156283516753367824 ) ) ;
#13710=CARTESIAN_POINT ( 'NONE',  ( 23.48500000273119070, 0.2613211581691317065, 2.486304738420681559 ) ) ;
#13719=EDGE_CURVE ( 'NONE', #9887, #2902, #24907, .T. ) ;
#13723=DIRECTION ( 'NONE',  ( -1.000000000000000000, 8.574039729943019576E-17, -0.000000000000000000 ) ) ;
#13728=CARTESIAN_POINT ( 'NONE',  ( 10.57125986779756843, -4.681538312723512618, -0.8254815157535732029 ) ) ;
#13731=ORIENTED_EDGE ( 'NONE', *, *, #9329, .F. ) ;
#13732=CARTESIAN_POINT ( 'NONE',  ( 0.000000000000000000, 0.000000000000000000, 0.000000000000000000 ) ) ;
#13742=LINE ( 'NONE', #11088, #16270 ) ;
#13748=EDGE_CURVE ( 'NONE', #545, #17553, #4358, .T. ) ;
#13750=VERTEX_POINT ( 'NONE', #20083 ) ;
#13751=EDGE_CURVE ( 'NONE', #27641, #3086, #22243, .T. ) ;
#13755=ORIENTED_EDGE ( 'NONE', *, *, #22697, .F. ) ;
#13762=DIRECTION ( 'NONE',  ( 0.000000000000000000, 1.000000000000000000, 0.000000000000000000 ) ) ;
#13776=CARTESIAN_POINT ( 'NONE',  ( 10.00000000000000000, 4.208382051008230818, -2.718385644597129502 ) ) ;
#13781=FACE_OUTER_BOUND ( 'NONE', #8264, .T. ) ;
#13791=VERTEX_POINT ( 'NONE', #14858 ) ;
#13802=ADVANCED_FACE ( 'NONE', ( #6150 ), #32239, .T. ) ;
#13804=CARTESIAN_POINT ( 'NONE',  ( 10.56870887191539587, 1.476463073999635389, 4.787500056513372293 ) ) ;
#13807=ORIENTED_EDGE ( 'NONE', *, *, #30929, .F. ) ;
#13809=EDGE_CURVE ( 'NONE', #29918, #15750, #2408, .T. ) ;
#13817=ADVANCED_FACE ( 'NONE', ( #19022 ), #16171, .T. ) ;
#13822=AXIS2_PLACEMENT_3D ( 'NONE', #13250, #21134, #11238 ) ;
#13830=EDGE_CURVE ( 'NONE', #25011, #30361, #11323, .T. ) ;
#13837=ORIENTED_EDGE ( 'NONE', *, *, #9242, .T. ) ;
#13843=CARTESIAN_POINT ( 'NONE',  ( 22.48500000000000298, -2.486304738420683780, 0.2613211581691335383 ) ) ;
#13846=( BOUNDED_CURVE ( )  B_SPLINE_CURVE ( 2, ( #13592, #6574, #16771, #26970, #26625, #6384, #8569, #23944, #26483, #26323, #23797 ),
 .UNSPECIFIED., .F., .F. ) 
 B_SPLINE_CURVE_WITH_KNOTS ( ( 3, 2, 2, 2, 2, 3 ),
 ( 0.09661161918950035565, 0.1000000000000000056, 0.1250000000000000000, 0.1499999999999999944, 0.1749999999999999889, 0.1966116191895003751 ),
 .UNSPECIFIED. ) 
 CURVE ( )  GEOMETRIC_REPRESENTATION_ITEM ( )  RATIONAL_B_SPLINE_CURVE ( ( 0.9821626249036858880, 0.9896829947469992783, 1.000000000000000000, 0.9238795325112867385, 1.000000000000000000, 0.9238795325112867385, 1.000000000000000000, 0.9238795325112867385, 1.000000000000000000, 0.9341965377642874602, 0.9821626249036858880 ) ) 
 REPRESENTATION_ITEM ( '' )  );
#13853=CARTESIAN_POINT ( 'NONE',  ( 10.56870887191539587, -1.946309384392561626, -4.616489984850551842 ) ) ;
#13856=CARTESIAN_POINT ( 'NONE',  ( 22.36000000273118715, 1.942864903642424146, 1.573300977624592534 ) ) ;
#13860=VECTOR ( 'NONE', #4025, 1000.000000000000000 ) ;
#13867=CARTESIAN_POINT ( 'NONE',  ( -1.959487840848880017E-16, -2.285372942704922306, -4.458382051008217495 ) ) ;
#13874=ORIENTED_EDGE ( 'NONE', *, *, #2933, .T. ) ;
#13875=ADVANCED_FACE ( 'NONE', ( #25003 ), #9619, .F. ) ;
#13883=CARTESIAN_POINT ( 'NONE',  ( 10.55147673363119232, 2.718385644597172579, 4.208382051008202396 ) ) ;
#13887=EDGE_LOOP ( 'NONE', ( #23305, #23426, #5625, #21132 ) ) ;
#13897=VECTOR ( 'NONE', #19932, 1000.000000000000114 ) ;
#13910=AXIS2_PLACEMENT_3D ( 'NONE', #17524, #7842, #7490 ) ;
#13913=EDGE_LOOP ( 'NONE', ( #18139, #11818, #19626, #12632 ) ) ;
#13914=CARTESIAN_POINT ( 'NONE',  ( 10.52034268205830259, -3.055657119358826446, 3.641590349731918863 ) ) ;
#13922=CARTESIAN_POINT ( 'NONE',  ( 25.23500000136559507, -1.570731468192933633, -2.892927487894330962 ) ) ;
#13923=ORIENTED_EDGE ( 'NONE', *, *, #27133, .F. ) ;
#13927=ORIENTED_EDGE ( 'NONE', *, *, #21218, .T. ) ;
#13931=EDGE_CURVE ( 'NONE', #26262, #3931, #10736, .T. ) ;
#13946=FACE_OUTER_BOUND ( 'NONE', #15315, .T. ) ;
#13947=LINE ( 'NONE', #9733, #7616 ) ;
#13949=CARTESIAN_POINT ( 'NONE',  ( 21.67249999999999943, -1.291182301015472600, -2.378061970571982098 ) ) ;
#13951=ORIENTED_EDGE ( 'NONE', *, *, #26274, .F. ) ;
#13960=CONICAL_SURFACE ( 'NONE', #9171, 3.024999999999999911, 0.7853981633974520538 ) ;
#13967=VECTOR ( 'NONE', #3935, 999.9999999999998863 ) ;
#13986=CARTESIAN_POINT ( 'NONE',  ( 10.56870887191539587, 1.946309384392654218, -4.616489984850511874 ) ) ;
#13993=CARTESIAN_POINT ( 'NONE',  ( 17.75999999999999801, -2.208672634433321348E-15, 0.000000000000000000 ) ) ;
#13994=DIRECTION ( 'NONE',  ( 0.000000000000000000, 0.000000000000000000, -1.000000000000000000 ) ) ;
#13995=CARTESIAN_POINT ( 'NONE',  ( 10.56870887191539587, -1.625881193364669297, -4.467071865485488402 ) ) ;
#14008=DIRECTION ( 'NONE',  ( 1.000000000000000000, -8.574039729943018344E-17, -0.000000000000000000 ) ) ;
#14009=AXIS2_PLACEMENT_3D ( 'NONE', #24386, #1354, #32594 ) ;
#14015=CARTESIAN_POINT ( 'NONE',  ( 2.143509932485593732E-17, 0.2499999999999817368, 5.003758587302149508 ) ) ;
#14019=EDGE_CURVE ( 'NONE', #1268, #228, #7294, .T. ) ;
#14025=FACE_OUTER_BOUND ( 'NONE', #2584, .T. ) ;
#14027=CARTESIAN_POINT ( 'NONE',  ( 24.10999999999999943, 1.942864903642424146, 1.573300977624592534 ) ) ;
#14041=CARTESIAN_POINT ( 'NONE',  ( 23.36000000273119070, 1.942864903642424146, 1.573300977624592534 ) ) ;
#14045=CARTESIAN_POINT ( 'NONE',  ( 25.75999999999999801, -2.208672634433321348E-15, -3.024999999999999911 ) ) ;
#14076=CARTESIAN_POINT ( 'NONE',  ( 10.55147673363119232, -4.116875700062100130, 2.376879293651050329 ) ) ;
#14078=CARTESIAN_POINT ( 'NONE',  ( 23.25111450864416085, -3.256483526998273983E-15, 2.499999999999998668 ) ) ;
#14090=ADVANCED_FACE ( 'NONE', ( #30950 ), #30647, .F. ) ;
#14094=VECTOR ( 'NONE', #10711, 1000.000000000000000 ) ;
#14113=EDGE_CURVE ( 'NONE', #9508, #31957, #15736, .T. ) ;
#14133=DIRECTION ( 'NONE',  ( 1.000000000000000000, -8.574039729943018344E-17, -0.000000000000000000 ) ) ;
#14136=VERTEX_POINT ( 'NONE', #19216 ) ;
#14143=ADVANCED_FACE ( 'NONE', ( #6834 ), #29913, .F. ) ;
#14156=LINE ( 'NONE', #14303, #12484 ) ;
#14162=DIRECTION ( 'NONE',  ( -2.219124775574964855E-17, -0.2588190451025251804, 0.9659258262890670910 ) ) ;
#14169=DIRECTION ( 'NONE',  ( -3.623545766764197982E-17, -0.4226182617406974984, -0.9063077870366508249 ) ) ;
#14170=ORIENTED_EDGE ( 'NONE', *, *, #15116, .T. ) ;
#14171=DIRECTION ( 'NONE',  ( -7.770718973608945377E-17, -0.9063077870366467170, -0.4226182617407064912 ) ) ;
#14175=FACE_OUTER_BOUND ( 'NONE', #15638, .T. ) ;
#14176=ORIENTED_EDGE ( 'NONE', *, *, #14409, .F. ) ;
#14180=VERTEX_POINT ( 'NONE', #24387 ) ;
#14185=CARTESIAN_POINT ( 'NONE',  ( 10.00000000000000000, -2.376879293651094294, 4.116875700062075261 ) ) ;
#14186=ORIENTED_EDGE ( 'NONE', *, *, #26498, .F. ) ;
#14190=CARTESIAN_POINT ( 'NONE',  ( 21.98499999999999943, 2.486304738420679783, -0.2613211581691337604 ) ) ;
#14194=ORIENTED_EDGE ( 'NONE', *, *, #23581, .F. ) ;
#14196=DIRECTION ( 'NONE',  ( 0.000000000000000000, -0.7071067811865465735, 0.7071067811865484609 ) ) ;
#14199=ORIENTED_EDGE ( 'NONE', *, *, #11602, .T. ) ;
#14203=CARTESIAN_POINT ( 'NONE',  ( 23.54750000273119070, -0.7685399846772070775, 2.594547506269381465 ) ) ;
#14204=DIRECTION ( 'NONE',  ( -1.000000000000000000, 8.574039729943019576E-17, -0.000000000000000000 ) ) ;
#14209=CARTESIAN_POINT ( 'NONE',  ( 10.57125986779756843, 4.884328206559835905, 1.115095498423326559 ) ) ;
#14215=CARTESIAN_POINT ( 'NONE',  ( 0.000000000000000000, 0.000000000000000000, 0.000000000000000000 ) ) ;
#14228=CARTESIAN_POINT ( 'NONE',  ( 25.75999999999999446, 1.024942698525265428, 2.863353032229740691 ) ) ;
#14237=ORIENTED_EDGE ( 'NONE', *, *, #32875, .T. ) ;
#14240=PLANE ( 'NONE',  #16092 ) ;
#14250=ORIENTED_EDGE ( 'NONE', *, *, #11893, .F. ) ;
#14255=ORIENTED_EDGE ( 'NONE', *, *, #15500, .F. ) ;
#14257=CARTESIAN_POINT ( 'NONE',  ( -3.148734258548802813E-16, -3.672404558090061943, 3.407865132560167432 ) ) ;
#14261=CARTESIAN_POINT ( 'NONE',  ( 23.61000000136559507, 3.156283516753366047, 0.9349337715887203748 ) ) ;
#14263=VERTEX_POINT ( 'NONE', #15510 ) ;
#14266=DIRECTION ( 'NONE',  ( 0.000000000000000000, -0.8191520442889983489, 0.5735764363510366115 ) ) ;
#14268=CARTESIAN_POINT ( 'NONE',  ( 21.98500000273118715, -0.2613211581691358698, -2.486304738420681559 ) ) ;
#14280=EDGE_CURVE ( 'NONE', #3186, #3463, #12828, .T. ) ;
#14282=EDGE_CURVE ( 'NONE', #11672, #29889, #6985, .T. ) ;
#14296=EDGE_CURVE ( 'NONE', #17299, #19432, #28223, .T. ) ;
#14298=CARTESIAN_POINT ( 'NONE',  ( 25.75999999999999801, -2.208672634433321348E-15, 0.000000000000000000 ) ) ;
#14303=CARTESIAN_POINT ( 'NONE',  ( 10.52034268205830259, -3.672404558090015314, -3.407865132560218946 ) ) ;
#14316=PLANE ( 'NONE',  #14516 ) ;
#14321=DIRECTION ( 'NONE',  ( -1.000000000000000000, 8.574039729943019576E-17, -6.162975822039154730E-33 ) ) ;
#14323=LINE ( 'NONE', #24524, #24750 ) ;
#14330=EDGE_CURVE ( 'NONE', #32682, #23691, #7993, .T. ) ;
#14337=CARTESIAN_POINT ( 'NONE',  ( 24.92249999999999943, 2.378061970571979433, -1.291182301015470824 ) ) ;
#14353=CARTESIAN_POINT ( 'NONE',  ( 25.11000000136559507, -2.892927487894331406, 1.570731468192932523 ) ) ;
#14365=CARTESIAN_POINT ( 'NONE',  ( 2.593512329575687483E-16, 3.024842911000745094, -3.993798362933278057 ) ) ;
#14366=VERTEX_POINT ( 'NONE', #25228 ) ;
#14367=VECTOR ( 'NONE', #26178, 1000.000000000000114 ) ;
#14380=FACE_OUTER_BOUND ( 'NONE', #29248, .T. ) ;
#14385=DIRECTION ( 'NONE',  ( 1.000000000000000000, -8.574039729943018344E-17, -0.000000000000000000 ) ) ;
#14390=CARTESIAN_POINT ( 'NONE',  ( 24.48500000136559507, 2.892927487894327410, -1.570731468192931635 ) ) ;
#14409=EDGE_CURVE ( 'NONE', #6020, #23760, #28355, .T. ) ;
#14414=CARTESIAN_POINT ( 'NONE',  ( 21.29750000136559507, -0.3178988483021076838, -3.024605502323848949 ) ) ;
#14422=EDGE_LOOP ( 'NONE', ( #16334, #11603, #32675, #24966 ) ) ;
#14427=CARTESIAN_POINT ( 'NONE',  ( 22.92250000136559862, -1.913930629741527500, 2.363507492473149618 ) ) ;
#14443=EDGE_CURVE ( 'NONE', #14180, #3790, #23531, .T. ) ;
#14447=LINE ( 'NONE', #6936, #741 ) ;
#14457=VERTEX_POINT ( 'NONE', #23714 ) ;
#14459=AXIS2_PLACEMENT_3D ( 'NONE', #2020, #24557, #1681 ) ;
#14471=ADVANCED_FACE ( 'NONE', ( #8478 ), #1134, .F. ) ;
#14476=CARTESIAN_POINT ( 'NONE',  ( 25.71927239433071222, 2.993516940937198889, -0.04068705237182682760 ) ) ;
#14477=ORIENTED_EDGE ( 'NONE', *, *, #17541, .F. ) ;
#14487=LINE ( 'NONE', #3549, #28953 ) ;
#14489=CARTESIAN_POINT ( 'NONE',  ( 20.73500000273118715, -2.486304738420683780, 0.2613211581691335383 ) ) ;
#14490=ORIENTED_EDGE ( 'NONE', *, *, #9236, .F. ) ;
#14496=CARTESIAN_POINT ( 'NONE',  ( 25.23500000136559507, -3.156283516753370044, -0.9349337715887220401 ) ) ;
#14515=EDGE_CURVE ( 'NONE', #26262, #4614, #24008, .T. ) ;
#14516=AXIS2_PLACEMENT_3D ( 'NONE', #13995, #32414, #19535 ) ;
#14517=CARTESIAN_POINT ( 'NONE',  ( 24.48499999999999943, -2.486304738420683780, 0.2613211581691335383 ) ) ;
#14520=CARTESIAN_POINT ( 'NONE',  ( 23.04750000000000654, 2.594547506269380133, 0.7685399846772031918 ) ) ;
#14527=DIRECTION ( 'NONE',  ( -1.000000000000000000, 8.574039729943015878E-17, 1.232595164407830946E-32 ) ) ;
#14533=CARTESIAN_POINT ( 'NONE',  ( 10.56870887191539587, 1.625881193364757449, -4.467071865485455540 ) ) ;
#14537=CARTESIAN_POINT ( 'NONE',  ( 10.52034268205830259, -3.407865132560206511, 3.672404558090026860 ) ) ;
#14538=CARTESIAN_POINT ( 'NONE',  ( 24.98500000136559507, -0.9349337715887247047, 3.156283516753367824 ) ) ;
#14544=CARTESIAN_POINT ( 'NONE',  ( 24.80656763371926843, 0.8852964313267430718, -2.499999999999998224 ) ) ;
#14553=VECTOR ( 'NONE', #28733, 1000.000000000000000 ) ;
#14569=VERTEX_POINT ( 'NONE', #828 ) ;
#14577=CARTESIAN_POINT ( 'NONE',  ( 22.67250000000000298, -1.291182301015472600, -2.378061970571982098 ) ) ;
#14588=CARTESIAN_POINT ( 'NONE',  ( 24.29750000136559507, -0.3178988483021076838, -3.024605502323848949 ) ) ;
#14589=DIRECTION ( 'NONE',  ( 0.000000000000000000, 1.000000000000000000, 0.000000000000000000 ) ) ;
#14592=DIRECTION ( 'NONE',  ( 0.000000000000000000, -0.9063077870366440525, -0.4226182617407121533 ) ) ;
#14597=ORIENTED_EDGE ( 'NONE', *, *, #14515, .F. ) ;
#14601=DIRECTION ( 'NONE',  ( -6.062761635205638616E-17, -0.7071067811865540120, 0.7071067811865410224 ) ) ;
#14605=VECTOR ( 'NONE', #5997, 1000.000000000000000 ) ;
#14607=ORIENTED_EDGE ( 'NONE', *, *, #7480, .F. ) ;
#14612=CARTESIAN_POINT ( 'NONE',  ( 24.29750000136559507, -0.3178988483021076838, -3.024605502323848949 ) ) ;
#14615=FACE_OUTER_BOUND ( 'NONE', #1147, .T. ) ;
#14620=CARTESIAN_POINT ( 'NONE',  ( 23.98500000136559507, -2.892927487894331406, 1.570731468192932301 ) ) ;
#14623=AXIS2_PLACEMENT_3D ( 'NONE', #1622, #11813, #16836 ) ;
#14628=DIRECTION ( 'NONE',  ( 4.917867153432943562E-17, 0.5735764363510392760, 0.8191520442889966835 ) ) ;
#14635=ORIENTED_EDGE ( 'NONE', *, *, #9124, .F. ) ;
#14639=ORIENTED_EDGE ( 'NONE', *, *, #5664, .F. ) ;
#14643=VECTOR ( 'NONE', #18119, 1000.000000000000000 ) ;
#14655=LINE ( 'NONE', #12141, #11241 ) ;
#14657=EDGE_CURVE ( 'NONE', #17282, #1891, #20300, .T. ) ;
#14658=DIRECTION ( 'NONE',  ( 7.770718973609008239E-17, 0.9063077870366537114, -0.4226182617406915032 ) ) ;
#14680=EDGE_CURVE ( 'NONE', #27411, #15557, #25710, .T. ) ;
#14687=ORIENTED_EDGE ( 'NONE', *, *, #10526, .F. ) ;
#14696=CARTESIAN_POINT ( 'NONE',  ( 25.29750000136559507, -2.363507492473152283, -1.913930629741525280 ) ) ;
#14720=ORIENTED_EDGE ( 'NONE', *, *, #15276, .F. ) ;
#14724=CARTESIAN_POINT ( 'NONE',  ( 0.000000000000000000, 0.000000000000000000, 0.000000000000000000 ) ) ;
#14745=CARTESIAN_POINT ( 'NONE',  ( 23.42250000273119070, 1.291182301015469047, 2.378061970571981654 ) ) ;
#14752=ORIENTED_EDGE ( 'NONE', *, *, #11395, .T. ) ;
#14754=EDGE_CURVE ( 'NONE', #32366, #27630, #29450, .T. ) ;
#14757=VERTEX_POINT ( 'NONE', #30700 ) ;
#14760=ORIENTED_EDGE ( 'NONE', *, *, #7785, .T. ) ;
#14769=CARTESIAN_POINT ( 'NONE',  ( 23.11000000136559862, -3.156283516753370488, -0.9349337715887220401 ) ) ;
#14771=FACE_OUTER_BOUND ( 'NONE', #20193, .T. ) ;
#14776=CARTESIAN_POINT ( 'NONE',  ( 23.67250000136559507, 2.363507492473148286, 1.913930629741525058 ) ) ;
#14793=DIRECTION ( 'NONE',  ( 1.000000000000000000, -8.574039729943018344E-17, -0.000000000000000000 ) ) ;
#14794=ORIENTED_EDGE ( 'NONE', *, *, #9279, .T. ) ;
#14796=CARTESIAN_POINT ( 'NONE',  ( 0.000000000000000000, 0.000000000000000000, 0.000000000000000000 ) ) ;
#14808=ORIENTED_EDGE ( 'NONE', *, *, #22094, .F. ) ;
#14813=ORIENTED_EDGE ( 'NONE', *, *, #5919, .F. ) ;
#14822=EDGE_LOOP ( 'NONE', ( #1249, #21627, #10924, #17763 ) ) ;
#14826=CARTESIAN_POINT ( 'NONE',  ( 25.92250000136559507, 0.3178988483021036315, 3.024605502323848949 ) ) ;
#14838=CARTESIAN_POINT ( 'NONE',  ( 25.75999999999999801, -2.208672634433321348E-15, 0.000000000000000000 ) ) ;
#14840=ORIENTED_EDGE ( 'NONE', *, *, #7553, .F. ) ;
#14843=CARTESIAN_POINT ( 'NONE',  ( 24.86000000136559862, 1.570731468192929858, 2.892927487894329186 ) ) ;
#14852=VERTEX_POINT ( 'NONE', #15428 ) ;
#14858=CARTESIAN_POINT ( 'NONE',  ( 10.00000000000000000, 4.971152295393300946, 0.6226916219172224931 ) ) ;
#14877=ORIENTED_EDGE ( 'NONE', *, *, #18466, .T. ) ;
#14882=CARTESIAN_POINT ( 'NONE',  ( 23.48500000000000298, -2.486304738420683780, 0.2613211581691335383 ) ) ;
#14884=CYLINDRICAL_SURFACE ( 'NONE', #12822, 5.010000000000000675 ) ;
#14889=EDGE_CURVE ( 'NONE', #17028, #3611, #27298, .T. ) ;
#14895=CARTESIAN_POINT ( 'NONE',  ( 10.57125986779756843, -4.971152295393299170, -0.6226916219172566880 ) ) ;
#14896=CARTESIAN_POINT ( 'NONE',  ( 22.98500000136559507, -2.892927487894331406, 1.570731468192932301 ) ) ;
#14909=CYLINDRICAL_SURFACE ( 'NONE', #19420, 5.010000000000000675 ) ;
#14915=LINE ( 'NONE', #1749, #7602 ) ;
#14926=AXIS2_PLACEMENT_3D ( 'NONE', #26014, #3121, #13762 ) ;
#14938=LINE ( 'NONE', #7782, #2824 ) ;
#14947=DIRECTION ( 'NONE',  ( -1.000000000000000000, 8.574039729943019576E-17, 0.000000000000000000 ) ) ;
#14948=EDGE_LOOP ( 'NONE', ( #13104, #31434, #26115, #14840 ) ) ;
#14951=VECTOR ( 'NONE', #19363, 1000.000000000000000 ) ;
#14960=ORIENTED_EDGE ( 'NONE', *, *, #11578, .T. ) ;
#14961=DIRECTION ( 'NONE',  ( 1.000000000000000000, -8.574039729943018344E-17, -0.000000000000000000 ) ) ;
#14965=ADVANCED_FACE ( 'NONE', ( #1548 ), #29467, .F. ) ;
#14977=DIRECTION ( 'NONE',  ( 7.770718973608992215E-17, 0.9063077870366522681, -0.4226182617406944453 ) ) ;
#14982=ORIENTED_EDGE ( 'NONE', *, *, #12803, .T. ) ;
#14984=CARTESIAN_POINT ( 'NONE',  ( 25.73500000136559507, 3.156283516753366047, 0.9349337715887203748 ) ) ;
#14991=CARTESIAN_POINT ( 'NONE',  ( -1.668773398854276148E-16, -1.946309384392560737, -4.616489984850551842 ) ) ;
#14994=AXIS2_PLACEMENT_3D ( 'NONE', #12179, #27225, #1855 ) ;
#15005=CARTESIAN_POINT ( 'NONE',  ( 4.075891499408641642E-16, 4.753758587302147731, 0.000000000000000000 ) ) ;
#15008=DIRECTION ( 'NONE',  ( 1.000000000000000000, -8.574039729943018344E-17, -0.000000000000000000 ) ) ;
#15009=CARTESIAN_POINT ( 'NONE',  ( 22.73500000136559862, 3.156283516753366047, 0.9349337715887203748 ) ) ;
#15022=AXIS2_PLACEMENT_3D ( 'NONE', #7600, #4448, #25485 ) ;
#15027=CARTESIAN_POINT ( 'NONE',  ( 23.48500000136559862, 0.9349337715887185984, -3.156283516753368268 ) ) ;
#15028=VECTOR ( 'NONE', #13723, 1000.000000000000000 ) ;
#15037=EDGE_CURVE ( 'NONE', #19939, #22762, #7568, .T. ) ;
#15061=LINE ( 'NONE', #32979, #29389 ) ;
#15063=CARTESIAN_POINT ( 'NONE',  ( 10.56870887191539587, 1.476463073999701781, -4.787500056513350977 ) ) ;
#15070=LINE ( 'NONE', #30469, #21427 ) ;
#15071=CARTESIAN_POINT ( 'NONE',  ( 23.36000000136559507, 0.9349337715887185984, -3.156283516753368268 ) ) ;
#15078=ORIENTED_EDGE ( 'NONE', *, *, #15037, .T. ) ;
#15081=VECTOR ( 'NONE', #32734, 1000.000000000000000 ) ;
#15085=VERTEX_POINT ( 'NONE', #7231 ) ;
#15106=VECTOR ( 'NONE', #17237, 1000.000000000000114 ) ;
#15107=CIRCLE ( 'NONE', #714, 5.010000000000000675 ) ;
#15109=CARTESIAN_POINT ( 'NONE',  ( 25.75999999999999801, -2.208672634433321348E-15, 0.000000000000000000 ) ) ;
#15112=LINE ( 'NONE', #20299, #27205 ) ;
#15116=EDGE_CURVE ( 'NONE', #4840, #18222, #2049, .T. ) ;
#15121=CARTESIAN_POINT ( 'NONE',  ( 10.56870887191539587, -1.476463073999670916, 4.787500056513361635 ) ) ;
#15132=VECTOR ( 'NONE', #24915, 1000.000000000000000 ) ;
#15133=AXIS2_PLACEMENT_3D ( 'NONE', #31100, #8189, #28585 ) ;
#15135=CARTESIAN_POINT ( 'NONE',  ( 25.75999999999999801, -2.208672634433321348E-15, -3.024999999999999911 ) ) ;
#15143=DIRECTION ( 'NONE',  ( 8.574039729943018344E-17, 1.000000000000000000, 0.000000000000000000 ) ) ;
#15153=VECTOR ( 'NONE', #17351, 1000.000000000000000 ) ;
#15155=ORIENTED_EDGE ( 'NONE', *, *, #13830, .T. ) ;
#15167=LINE ( 'NONE', #4641, #8781 ) ;
#15171=CARTESIAN_POINT ( 'NONE',  ( 24.11000000273118715, 1.573300977624590313, -1.942864903642426144 ) ) ;
#15172=ORIENTED_EDGE ( 'NONE', *, *, #7059, .F. ) ;
#15178=CARTESIAN_POINT ( 'NONE',  ( 23.98500000136559507, -0.9349337715887248157, 3.156283516753367824 ) ) ;
#15183=ORIENTED_EDGE ( 'NONE', *, *, #25491, .T. ) ;
#15186=CARTESIAN_POINT ( 'NONE',  ( 10.00000000000000000, -4.467071865485462645, -1.625881193364742572 ) ) ;
#15187=VERTEX_POINT ( 'NONE', #16533 ) ;
#15195=ORIENTED_EDGE ( 'NONE', *, *, #10562, .T. ) ;
#15198=CARTESIAN_POINT ( 'NONE',  ( 24.36000000136559507, -1.570731468192933633, -2.892927487894330074 ) ) ;
#15199=DIRECTION ( 'NONE',  ( 7.023442172597848233E-17, 0.8191520442889907994, 0.5735764363510474917 ) ) ;
#15205=DIRECTION ( 'NONE',  ( -1.000000000000000000, 8.574039729943022041E-17, 1.232595164407830946E-32 ) ) ;
#15213=CARTESIAN_POINT ( 'NONE',  ( 21.86000000136559507, 1.570731468192929858, 2.892927487894329630 ) ) ;
#15219=DIRECTION ( 'NONE',  ( 1.000000000000000000, -0.000000000000000000, -0.000000000000000000 ) ) ;
#15224=ORIENTED_EDGE ( 'NONE', *, *, #12803, .F. ) ;
#15235=CARTESIAN_POINT ( 'NONE',  ( 25.75999999999999801, -2.208672634433321348E-15, 0.000000000000000000 ) ) ;
#15242=ORIENTED_EDGE ( 'NONE', *, *, #20764, .F. ) ;
#15247=CARTESIAN_POINT ( 'NONE',  ( 24.11000000273118715, 1.573300977624590313, -1.942864903642426144 ) ) ;
#15249=DIRECTION ( 'NONE',  ( -1.000000000000000000, 8.574039729943019576E-17, -0.000000000000000000 ) ) ;
#15267=ORIENTED_EDGE ( 'NONE', *, *, #7184, .F. ) ;
#15274=ORIENTED_EDGE ( 'NONE', *, *, #11285, .F. ) ;
#15276=EDGE_CURVE ( 'NONE', #23760, #6020, #18260, .T. ) ;
#15280=DIRECTION ( 'NONE',  ( 8.574039729943018344E-17, 1.000000000000000000, 0.000000000000000000 ) ) ;
#15283=ADVANCED_FACE ( 'NONE', ( #6690 ), #24394, .F. ) ;
#15311=DIRECTION ( 'NONE',  ( 0.000000000000000000, -0.08715574274765533480, -0.9961946980917457672 ) ) ;
#15315=EDGE_LOOP ( 'NONE', ( #25234, #32310, #6802, #497 ) ) ;
#15330=CARTESIAN_POINT ( 'NONE',  ( 24.17250000136559507, -3.024605502323851169, 0.3178988483021052969 ) ) ;
#15334=VERTEX_POINT ( 'NONE', #22077 ) ;
#15337=( BOUNDED_CURVE ( )  B_SPLINE_CURVE ( 2, ( #1105, #31721, #16811, #27011, #16458, #4113, #24475, #1593, #27337, #24831, #27662 ),
 .UNSPECIFIED., .F., .F. ) 
 B_SPLINE_CURVE_WITH_KNOTS ( ( 3, 2, 2, 2, 2, 3 ),
 ( 0.2966116191895003529, 0.2999999999999999889, 0.3250000000000000111, 0.3499999999999999778, 0.3750000000000000000, 0.3966116191895003862 ),
 .UNSPECIFIED. ) 
 CURVE ( )  GEOMETRIC_REPRESENTATION_ITEM ( )  RATIONAL_B_SPLINE_CURVE ( ( 0.9821626249036858880, 0.9896829947469992783, 1.000000000000000000, 0.9238795325112867385, 1.000000000000000000, 0.9238795325112867385, 1.000000000000000000, 0.9238795325112867385, 1.000000000000000000, 0.9341965377642874602, 0.9821626249036858880 ) ) 
 REPRESENTATION_ITEM ( '' )  );
#15339=ORIENTED_EDGE ( 'NONE', *, *, #18077, .F. ) ;
#15350=CARTESIAN_POINT ( 'NONE',  ( 25.17250000136559507, -3.024605502323851169, 0.3178988483021052969 ) ) ;
#15351=LINE ( 'NONE', #18191, #10243 ) ;
#15355=FACE_OUTER_BOUND ( 'NONE', #26308, .T. ) ;
#15356=CYLINDRICAL_SURFACE ( 'NONE', #22004, 5.010000000000000675 ) ;
#15357=CARTESIAN_POINT ( 'NONE',  ( 10.00000000000000000, -4.116875700062100130, 2.376879293651050329 ) ) ;
#15363=CARTESIAN_POINT ( 'NONE',  ( 23.54750000136559862, 1.913930629741522838, -2.363507492473150062 ) ) ;
#15366=CYLINDRICAL_SURFACE ( 'NONE', #19394, 5.010000000000000675 ) ;
#15386=DIRECTION ( 'NONE',  ( 1.000000000000000000, -8.574039729943018344E-17, -0.000000000000000000 ) ) ;
#15388=CARTESIAN_POINT ( 'NONE',  ( 22.30656763371926843, -0.8852964313267484009, 2.499999999999997780 ) ) ;
#15391=CARTESIAN_POINT ( 'NONE',  ( 24.67250000136559507, 2.363507492473148286, 1.913930629741525058 ) ) ;
#15397=CARTESIAN_POINT ( 'NONE',  ( 22.23500000136559862, -1.570731468192933633, -2.892927487894330074 ) ) ;
#15399=CARTESIAN_POINT ( 'NONE',  ( -2.037945749704337831E-16, -2.376879293651093406, 4.116875700062075261 ) ) ;
#15406=LINE ( 'NONE', #23431, #23676 ) ;
#15416=ORIENTED_EDGE ( 'NONE', *, *, #27056, .T. ) ;
#15420=ADVANCED_FACE ( 'NONE', ( #17889 ), #15356, .T. ) ;
#15421=EDGE_CURVE ( 'NONE', #31932, #16406, #10359, .T. ) ;
#15426=DIRECTION ( 'NONE',  ( -7.472768010111467553E-18, -0.08715574274766195451, 0.9961946980917452121 ) ) ;
#15428=CARTESIAN_POINT ( 'NONE',  ( 1.959487840848906148E-16, 2.285372942704953392, 4.458382051008201508 ) ) ;
#15438=VECTOR ( 'NONE', #19991, 1000.000000000000114 ) ;
#15439=CARTESIAN_POINT ( 'NONE',  ( 23.73500000000000298, -0.2613211581691358698, -2.486304738420681559 ) ) ;
#15451=AXIS2_PLACEMENT_3D ( 'NONE', #9951, #30210, #20015 ) ;
#15453=VECTOR ( 'NONE', #27257, 1000.000000000000000 ) ;
#15459=ORIENTED_EDGE ( 'NONE', *, *, #4285, .F. ) ;
#15460=EDGE_CURVE ( 'NONE', #3262, #20824, #30421, .T. ) ;
#15466=ORIENTED_EDGE ( 'NONE', *, *, #13719, .F. ) ;
#15485=VERTEX_POINT ( 'NONE', #8002 ) ;
#15492=CARTESIAN_POINT ( 'NONE',  ( 10.00000000000000178, -3.672404558090015758, -3.407865132560221166 ) ) ;
#15500=EDGE_CURVE ( 'NONE', #3034, #8114, #16646, .T. ) ;
#15501=AXIS2_PLACEMENT_3D ( 'NONE', #6944, #11636, #12291 ) ;
#15508=EDGE_CURVE ( 'NONE', #5774, #23867, #10239, .T. ) ;
#15510=CARTESIAN_POINT ( 'NONE',  ( 10.00000000000000000, -3.407865132560156329, -3.672404558090074378 ) ) ;
#15517=CARTESIAN_POINT ( 'NONE',  ( 10.00000000000000000, 4.787500056513365188, 1.476463073999653819 ) ) ;
#15529=CARTESIAN_POINT ( 'NONE',  ( 23.86000000136559507, 1.570731468192929858, 2.892927487894329630 ) ) ;
#15534=VECTOR ( 'NONE', #10006, 1000.000000000000000 ) ;
#15535=DIRECTION ( 'NONE',  ( 0.000000000000000000, 0.9063077870366522681, -0.4226182617406944453 ) ) ;
#15537=ORIENTED_EDGE ( 'NONE', *, *, #21198, .F. ) ;
#15553=CARTESIAN_POINT ( 'NONE',  ( 10.00000000000000000, 3.672404558090085036, -3.407865132560141674 ) ) ;
#15556=CARTESIAN_POINT ( 'NONE',  ( 10.00000000000000000, -3.055657119358777152, -3.641590349731960163 ) ) ;
#15557=VERTEX_POINT ( 'NONE', #5818 ) ;
#15558=CARTESIAN_POINT ( 'NONE',  ( 10.00000000000000000, 1.625881193364696609, 4.467071865485476856 ) ) ;
#15559=AXIS2_PLACEMENT_3D ( 'NONE', #26137, #3245, #266 ) ;
#15560=CARTESIAN_POINT ( 'NONE',  ( 22.25111450864416085, -3.256483526998273983E-15, 2.499999999999998668 ) ) ;
#15563=CARTESIAN_POINT ( 'NONE',  ( 23.48500000136559862, 2.892927487894327410, -1.570731468192931635 ) ) ;
#15571=AXIS2_PLACEMENT_3D ( 'NONE', #27061, #31429, #26430 ) ;
#15574=CARTESIAN_POINT ( 'NONE',  ( 25.48500000273118715, 0.2613211581691317065, 2.486304738420681559 ) ) ;
#15586=AXIS2_PLACEMENT_3D ( 'NONE', #9506, #30117, #26926 ) ;
#15588=EDGE_CURVE ( 'NONE', #32584, #5774, #31569, .T. ) ;
#15589=DIRECTION ( 'NONE',  ( 8.574039729943018344E-17, 1.000000000000000000, 0.000000000000000000 ) ) ;
#15592=CARTESIAN_POINT ( 'NONE',  ( 10.00000000000000000, 4.923251879855578162E-14, -4.753758587302147731 ) ) ;
#15598=ORIENTED_EDGE ( 'NONE', *, *, #28515, .F. ) ;
#15603=CARTESIAN_POINT ( 'NONE',  ( 10.00000000000000000, 1.476463073999702225, -4.787500056513350977 ) ) ;
#15617=AXIS2_PLACEMENT_3D ( 'NONE', #25872, #2992, #4795 ) ;
#15630=VERTEX_POINT ( 'NONE', #5987 ) ;
#15635=CARTESIAN_POINT ( 'NONE',  ( 25.27346073696792672, -0.6948329026079288484, 2.447823836836187539 ) ) ;
#15638=EDGE_LOOP ( 'NONE', ( #14477, #10468, #8847, #10326 ) ) ;
#15642=AXIS2_PLACEMENT_3D ( 'NONE', #13377, #25963, #3217 ) ;
#15652=CARTESIAN_POINT ( 'NONE',  ( 25.76000000000000512, 0.9093756521784821523, 2.891331917153146858 ) ) ;
#15654=ORIENTED_EDGE ( 'NONE', *, *, #4999, .T. ) ;
#15668=AXIS2_PLACEMENT_3D ( 'NONE', #22248, #2180, #29934 ) ;
#15671=CARTESIAN_POINT ( 'NONE',  ( 10.00000000000000000, -0.6226916219172395905, 4.971152295393299170 ) ) ;
#15672=CARTESIAN_POINT ( 'NONE',  ( 22.55656763645045615, -0.8852964313267484009, 2.499999999999997780 ) ) ;
#15675=AXIS2_PLACEMENT_3D ( 'NONE', #20744, #23560, #18901 ) ;
#15697=VERTEX_POINT ( 'NONE', #26552 ) ;
#15700=FACE_OUTER_BOUND ( 'NONE', #5288, .T. ) ;
#15704=EDGE_LOOP ( 'NONE', ( #15183, #19761, #15598, #19389 ) ) ;
#15712=DIRECTION ( 'NONE',  ( 0.000000000000000000, 1.000000000000000000, 0.000000000000000000 ) ) ;
#15715=EDGE_CURVE ( 'NONE', #4235, #13159, #27542, .T. ) ;
#15716=CARTESIAN_POINT ( 'NONE',  ( 22.04750000136559507, -1.913930629741527500, 2.363507492473149618 ) ) ;
#15734=EDGE_LOOP ( 'NONE', ( #12603, #7945, #6207, #28594 ) ) ;
#15736=LINE ( 'NONE', #12713, #25684 ) ;
#15737=DIRECTION ( 'NONE',  ( -8.281886410780512259E-17, -0.9659258262890680902, -0.2588190451025216277 ) ) ;
#15742=CARTESIAN_POINT ( 'NONE',  ( 10.00000000000000000, 3.641590349731970822, -3.055657119358763829 ) ) ;
#15746=CARTESIAN_POINT ( 'NONE',  ( 21.79750000136559507, 0.3178988483021036315, 3.024605502323848949 ) ) ;
#15750=VERTEX_POINT ( 'NONE', #27377 ) ;
#15753=CARTESIAN_POINT ( 'NONE',  ( 22.48500000136559507, 2.892927487894327410, -1.570731468192931635 ) ) ;
#15754=EDGE_CURVE ( 'NONE', #2105, #27641, #12002, .T. ) ;
#15756=CARTESIAN_POINT ( 'NONE',  ( 10.00000000000000000, 4.467071865485470639, 1.625881193364712596 ) ) ;
#15778=CARTESIAN_POINT ( 'NONE',  ( 25.75999999999999801, -2.208672634433321348E-15, 0.000000000000000000 ) ) ;
#15789=CARTESIAN_POINT ( 'NONE',  ( 10.57125986779756843, 0.8254815157535864145, -4.681538312723508177 ) ) ;
#15790=DIRECTION ( 'NONE',  ( -7.770718973609018100E-17, -0.9063077870366551547, 0.4226182617406882835 ) ) ;
#15796=FACE_OUTER_BOUND ( 'NONE', #27527, .T. ) ;
#15811=LINE ( 'NONE', #2793, #29953 ) ;
#15813=ORIENTED_EDGE ( 'NONE', *, *, #26791, .F. ) ;
#15834=CARTESIAN_POINT ( 'NONE',  ( -4.013969549054187630E-16, -4.681538312723522388, 0.8254815157535098091 ) ) ;
#15836=VERTEX_POINT ( 'NONE', #5142 ) ;
#15839=CARTESIAN_POINT ( 'NONE',  ( 17.75999999999999801, -2.208672634433321348E-15, 0.000000000000000000 ) ) ;
#15842=ADVANCED_FACE ( 'NONE', ( #7814 ), #32743, .F. ) ;
#15849=CARTESIAN_POINT ( 'NONE',  ( 22.17250000136559507, -3.024605502323851169, 0.3178988483021052969 ) ) ;
#15893=LINE ( 'NONE', #3384, #7511 ) ;
#15898=CARTESIAN_POINT ( 'NONE',  ( 24.23500000273118715, 2.486304738420679783, -0.2613211581691337604 ) ) ;
#15906=CARTESIAN_POINT ( 'NONE',  ( 25.75999999999999801, 0.8512451026088739825, 2.902758476911987628 ) ) ;
#15918=CARTESIAN_POINT ( 'NONE',  ( 10.00000000000000000, -1.946309384392561626, -4.616489984850552730 ) ) ;
#15928=ADVANCED_FACE ( 'NONE', ( #25187 ), #12986, .T. ) ;
#15935=PLANE ( 'NONE',  #6538 ) ;
#15936=VERTEX_POINT ( 'NONE', #32906 ) ;
#15937=CARTESIAN_POINT ( 'NONE',  ( 25.75999999999999801, -1.902510934646483477E-15, 2.499999999999997780 ) ) ;
#15941=CARTESIAN_POINT ( 'NONE',  ( 22.79750000136559862, 2.363507492473148286, 1.913930629741525058 ) ) ;
#15944=VERTEX_POINT ( 'NONE', #31374 ) ;
#15946=VERTEX_POINT ( 'NONE', #8789 ) ;
#15952=CARTESIAN_POINT ( 'NONE',  ( 24.54750000136559507, 3.024605502323846729, -0.3178988483021056854 ) ) ;
#15953=ADVANCED_FACE ( 'NONE', ( #26517 ), #21323, .T. ) ;
#15961=DIRECTION ( 'NONE',  ( -1.000000000000000000, 8.574039729943022041E-17, 1.232595164407830946E-32 ) ) ;
#15970=CARTESIAN_POINT ( 'NONE',  ( 24.24290772321993970, 0.1310194482076003919, 2.499999999999998668 ) ) ;
#15977=CARTESIAN_POINT ( 'NONE',  ( 10.56183597391177464, 5.003758587302147731, -0.2499999999999991951 ) ) ;
#15984=ORIENTED_EDGE ( 'NONE', *, *, #1021, .T. ) ;
#15994=CARTESIAN_POINT ( 'NONE',  ( 21.54750000136559507, 1.913930629741522838, -2.363507492473150062 ) ) ;
#15996=EDGE_LOOP ( 'NONE', ( #20221, #12132, #736, #5745 ) ) ;
#16004=DIRECTION ( 'NONE',  ( 0.000000000000000000, 1.000000000000000000, 0.000000000000000000 ) ) ;
#16010=AXIS2_PLACEMENT_3D ( 'NONE', #11523, #11366, #29908 ) ;
#16013=VERTEX_POINT ( 'NONE', #13776 ) ;
#16024=DIRECTION ( 'NONE',  ( 0.000000000000000000, 0.000000000000000000, -1.000000000000000000 ) ) ;
#16032=VERTEX_POINT ( 'NONE', #3617 ) ;
#16036=CARTESIAN_POINT ( 'NONE',  ( 22.04750000136559507, -3.024605502323851169, 0.3178988483021052969 ) ) ;
#16037=VECTOR ( 'NONE', #23336, 1000.000000000000000 ) ;
#16041=CIRCLE ( 'NONE', #27244, 5.010000000000000675 ) ;
#16044=CARTESIAN_POINT ( 'NONE',  ( 22.42250000273118715, 1.291182301015469047, 2.378061970571981654 ) ) ;
#16063=ORIENTED_EDGE ( 'NONE', *, *, #5555, .T. ) ;
#16065=CIRCLE ( 'NONE', #11806, 5.010000000000000675 ) ;
#16070=DIRECTION ( 'NONE',  ( 0.000000000000000000, 0.000000000000000000, -1.000000000000000000 ) ) ;
#16072=EDGE_CURVE ( 'NONE', #25185, #3234, #26836, .T. ) ;
#16075=DIRECTION ( 'NONE',  ( -1.000000000000000000, 8.574039729943022041E-17, 1.232595164407830946E-32 ) ) ;
#16079=ORIENTED_EDGE ( 'NONE', *, *, #19980, .F. ) ;
#16083=CARTESIAN_POINT ( 'NONE',  ( 0.000000000000000000, 0.000000000000000000, 0.000000000000000000 ) ) ;
#16092=AXIS2_PLACEMENT_3D ( 'NONE', #29474, #9233, #18778 ) ;
#16093=CARTESIAN_POINT ( 'NONE',  ( 25.75999999999999801, -2.208672634433321348E-15, 0.000000000000000000 ) ) ;
#16097=VECTOR ( 'NONE', #6727, 1000.000000000000000 ) ;
#16102=CARTESIAN_POINT ( 'NONE',  ( 25.75999999999999801, -1.902510934646483477E-15, 2.499999999999997780 ) ) ;
#16104=CARTESIAN_POINT ( 'NONE',  ( 22.48500000136559507, 0.9349337715887185984, -3.156283516753368268 ) ) ;
#16107=CARTESIAN_POINT ( 'NONE',  ( 10.00000000000000000, -2.376879293651037006, -4.116875700062107235 ) ) ;
#16111=EDGE_CURVE ( 'NONE', #10948, #3034, #28007, .T. ) ;
#16122=CARTESIAN_POINT ( 'NONE',  ( 10.56870887191539587, 4.787500056513386504, -1.476463073999588538 ) ) ;
#16125=EDGE_CURVE ( 'NONE', #6480, #29275, #19810, .T. ) ;
#16126=VERTEX_POINT ( 'NONE', #30194 ) ;
#16138=CARTESIAN_POINT ( 'NONE',  ( -5.338982705821066855E-17, -0.6226916219172391465, 4.971152295393299170 ) ) ;
#16151=CARTESIAN_POINT ( 'NONE',  ( 21.30656763371926132, -0.8852964313267484009, 2.499999999999997780 ) ) ;
#16171=CYLINDRICAL_SURFACE ( 'NONE', #27276, 5.010000000000000675 ) ;
#16175=VECTOR ( 'NONE', #3440, 1000.000000000000000 ) ;
#16180=VECTOR ( 'NONE', #24406, 1000.000000000000000 ) ;
#16191=LINE ( 'NONE', #32067, #23620 ) ;
#16200=VECTOR ( 'NONE', #5728, 1000.000000000000114 ) ;
#16221=CARTESIAN_POINT ( 'NONE',  ( 26.04750000000000298, 2.594547506269380133, 0.7685399846772031918 ) ) ;
#16225=ORIENTED_EDGE ( 'NONE', *, *, #19577, .F. ) ;
#16227=AXIS2_PLACEMENT_3D ( 'NONE', #2986, #791, #18333 ) ;
#16238=CARTESIAN_POINT ( 'NONE',  ( 23.11000000273118715, 1.573300977624590313, -1.942864903642426144 ) ) ;
#16251=DIRECTION ( 'NONE',  ( -1.000000000000000000, 8.574039729943018344E-17, -0.000000000000000000 ) ) ;
#16252=ORIENTED_EDGE ( 'NONE', *, *, #31726, .T. ) ;
#16254=VERTEX_POINT ( 'NONE', #12266 ) ;
#16259=DIRECTION ( 'NONE',  ( 0.000000000000000000, 1.000000000000000000, 0.000000000000000000 ) ) ;
#16269=DIRECTION ( 'NONE',  ( 1.000000000000000000, -8.574039729943018344E-17, -0.000000000000000000 ) ) ;
#16270=VECTOR ( 'NONE', #29475, 999.9999999999998863 ) ;
#16273=DIRECTION ( 'NONE',  ( 0.000000000000000000, 0.000000000000000000, -1.000000000000000000 ) ) ;
#16280=CARTESIAN_POINT ( 'NONE',  ( 25.44184412664977657, -2.526879277147909164, -0.9860087766846566959 ) ) ;
#16284=ORIENTED_EDGE ( 'NONE', *, *, #27024, .F. ) ;
#16288=EDGE_LOOP ( 'NONE', ( #4440, #24905, #2581, #8926 ) ) ;
#16290=EDGE_CURVE ( 'NONE', #19663, #25011, #13591, .T. ) ;
#16293=ORIENTED_EDGE ( 'NONE', *, *, #17517, .F. ) ;
#16294=ORIENTED_EDGE ( 'NONE', *, *, #9279, .F. ) ;
#16295=LINE ( 'NONE', #16122, #10744 ) ;
#16296=VERTEX_POINT ( 'NONE', #13256 ) ;
#16297=DIRECTION ( 'NONE',  ( 0.000000000000000000, 1.000000000000000000, 0.000000000000000000 ) ) ;
#16299=EDGE_LOOP ( 'NONE', ( #29719, #18896, #18366, #18422 ) ) ;
#16312=PLANE ( 'NONE',  #19279 ) ;
#16334=ORIENTED_EDGE ( 'NONE', *, *, #7146, .T. ) ;
#16343=DIRECTION ( 'NONE',  ( -7.770718973608988517E-17, -0.9063077870366522681, 0.4226182617406944453 ) ) ;
#16347=CARTESIAN_POINT ( 'NONE',  ( -3.122314033877847442E-16, -3.641590349731908649, -3.055657119358837992 ) ) ;
#16354=CARTESIAN_POINT ( 'NONE',  ( 10.56870887191539587, 4.616489984850558059, -1.946309384392544972 ) ) ;
#16359=CARTESIAN_POINT ( 'NONE',  ( 7.077711312404847644E-17, 0.8254815157535873027, -4.681538312723508177 ) ) ;
#16373=CARTESIAN_POINT ( 'NONE',  ( 22.79750000000000654, 0.7685399846772009713, -2.594547506269381909 ) ) ;
#16381=PLANE ( 'NONE',  #581 ) ;
#16383=CARTESIAN_POINT ( 'NONE',  ( 22.48500000273118715, 0.2613211581691317065, 2.486304738420681559 ) ) ;
#16385=CYLINDRICAL_SURFACE ( 'NONE', #5483, 5.010000000000000675 ) ;
#16405=ORIENTED_EDGE ( 'NONE', *, *, #32875, .F. ) ;
#16406=VERTEX_POINT ( 'NONE', #4841 ) ;
#16407=DIRECTION ( 'NONE',  ( 1.000000000000000000, -8.574039729943018344E-17, -0.000000000000000000 ) ) ;
#16408=CARTESIAN_POINT ( 'NONE',  ( 10.52034268205830259, 3.672404558090037963, 3.407865132560194077 ) ) ;
#16413=B_SPLINE_CURVE_WITH_KNOTS ( 'NONE', 3,
 ( #25720, #7678, #5506, #7330 ),
 .UNSPECIFIED., .F., .F.,
 ( 4, 4 ),
 ( 3.740497495074990297E-18, 0.0002608162019139872436 ),
 .UNSPECIFIED. ) ;
#16438=CARTESIAN_POINT ( 'NONE',  ( 10.57125986779756843, 4.971152295393300946, 0.6226916219172224931 ) ) ;
#16444=CARTESIAN_POINT ( 'NONE',  ( 10.00000000000000178, -8.574039729943018837E-16, 0.000000000000000000 ) ) ;
#16458=CARTESIAN_POINT ( 'NONE',  ( 23.86000000273118715, -1.942864903642428587, -1.573300977624592756 ) ) ;
#16460=DIRECTION ( 'NONE',  ( 1.000000000000000000, -0.000000000000000000, -0.000000000000000000 ) ) ;
#16464=EDGE_CURVE ( 'NONE', #20076, #15630, #9681, .T. ) ;
#16480=DIRECTION ( 'NONE',  ( 0.000000000000000000, 1.000000000000000000, 0.000000000000000000 ) ) ;
#16484=CARTESIAN_POINT ( 'NONE',  ( 10.56870887191539587, -4.467071865485462645, -1.625881193364742572 ) ) ;
#16502=DIRECTION ( 'NONE',  ( 0.000000000000000000, -0.9659258262890716429, 0.2588190451025081940 ) ) ;
#16507=DIRECTION ( 'NONE',  ( 0.000000000000000000, 0.9945218953682734009, -0.1045284632676536235 ) ) ;
#16521=ORIENTED_EDGE ( 'NONE', *, *, #27133, .T. ) ;
#16522=DIRECTION ( 'NONE',  ( 0.000000000000000000, 1.000000000000000000, 0.000000000000000000 ) ) ;
#16524=CARTESIAN_POINT ( 'NONE',  ( 24.73499999999999943, -0.2613211581691358698, -2.486304738420681559 ) ) ;
#16533=CARTESIAN_POINT ( 'NONE',  ( 25.76000000000000512, 2.749440278475487442, 1.299952413566024756 ) ) ;
#16536=CARTESIAN_POINT ( 'NONE',  ( 10.56183597391177464, 4.753758587302147731, 0.000000000000000000 ) ) ;
#16540=CARTESIAN_POINT ( 'NONE',  ( -4.075891499408641642E-16, -4.753758587302147731, 0.000000000000000000 ) ) ;
#16547=LINE ( 'NONE', #11059, #22588 ) ;
#16550=VERTEX_POINT ( 'NONE', #344 ) ;
#16551=VECTOR ( 'NONE', #19855, 1000.000000000000000 ) ;
#16555=CARTESIAN_POINT ( 'NONE',  ( 25.75999999999999801, -2.208672634433321348E-15, 0.000000000000000000 ) ) ;
#16561=EDGE_LOOP ( 'NONE', ( #23338, #23135, #30811, #12597, #20482, #29696, #28571, #13927, #9902, #2964, #24735, #24172, #5317, #18524, #16943 ) ) ;
#16563=ORIENTED_EDGE ( 'NONE', *, *, #21227, .F. ) ;
#16564=LINE ( 'NONE', #32433, #122 ) ;
#16569=CARTESIAN_POINT ( 'NONE',  ( -3.424298583717175800E-16, -3.993798362933329127, 3.024842911000676704 ) ) ;
#16582=ADVANCED_FACE ( 'NONE', ( #12689 ), #3170, .T. ) ;
#16589=VECTOR ( 'NONE', #14628, 999.9999999999998863 ) ;
#16593=EDGE_LOOP ( 'NONE', ( #31026, #12717 ) ) ;
#16597=CARTESIAN_POINT ( 'NONE',  ( 25.17250000273118715, 2.378061970571979433, -1.291182301015470602 ) ) ;
#16614=CARTESIAN_POINT ( 'NONE',  ( -2.037945749704288773E-16, -2.376879293651036118, -4.116875700062107235 ) ) ;
#16615=DIRECTION ( 'NONE',  ( 0.5150380749100547106, 1.049727191138618326E-16, 0.8571673007021120005 ) ) ;
#16617=CYLINDRICAL_SURFACE ( 'NONE', #2139, 5.010000000000000675 ) ;
#16626=FACE_OUTER_BOUND ( 'NONE', #2788, .T. ) ;
#16631=VECTOR ( 'NONE', #21435, 1000.000000000000000 ) ;
#16632=LINE ( 'NONE', #26839, #1673 ) ;
#16646=CIRCLE ( 'NONE', #4379, 5.009999999999999787 ) ;
#16653=CIRCLE ( 'NONE', #18787, 5.009999999999999787 ) ;
#16655=DIRECTION ( 'NONE',  ( 1.000000000000000000, -8.574039729943018344E-17, -0.000000000000000000 ) ) ;
#16661=CARTESIAN_POINT ( 'NONE',  ( 0.000000000000000000, 0.000000000000000000, 0.000000000000000000 ) ) ;
#16669=CARTESIAN_POINT ( 'NONE',  ( 10.00000000000000000, -3.055657119358777152, -3.641590349731960163 ) ) ;
#16671=DIRECTION ( 'NONE',  ( 1.000000000000000000, -8.574039729943018344E-17, -0.000000000000000000 ) ) ;
#16678=ORIENTED_EDGE ( 'NONE', *, *, #30235, .T. ) ;
#16680=EDGE_CURVE ( 'NONE', #28186, #21430, #13672, .T. ) ;
#16682=CARTESIAN_POINT ( 'NONE',  ( 20.86000000273118715, -1.942864903642428587, -1.573300977624592756 ) ) ;
#16683=ORIENTED_EDGE ( 'NONE', *, *, #25449, .T. ) ;
#16690=DIRECTION ( 'NONE',  ( 0.000000000000000000, -0.9659258262890700886, 0.2588190451025141336 ) ) ;
#16693=CYLINDRICAL_SURFACE ( 'NONE', #3349, 5.010000000000000675 ) ;
#16698=EDGE_CURVE ( 'NONE', #24378, #5341, #29983, .T. ) ;
#16704=ORIENTED_EDGE ( 'NONE', *, *, #16680, .F. ) ;
#16707=ORIENTED_EDGE ( 'NONE', *, *, #18600, .F. ) ;
#16709=FACE_OUTER_BOUND ( 'NONE', #10629, .T. ) ;
#16711=CARTESIAN_POINT ( 'NONE',  ( 23.54750000000000654, -2.594547506269383685, -0.7685399846772043020 ) ) ;
#16713=PLANE ( 'NONE',  #29368 ) ;
#16724=AXIS2_PLACEMENT_3D ( 'NONE', #1235, #18609, #28799 ) ;
#16725=AXIS2_PLACEMENT_3D ( 'NONE', #12342, #30262, #28222 ) ;
#16728=CARTESIAN_POINT ( 'NONE',  ( 22.29750000273118715, 2.594547506269380133, 0.7685399846772031918 ) ) ;
#16739=CARTESIAN_POINT ( 'NONE',  ( 5.338982705820766102E-17, 0.6226916219172039524, 4.971152295393303611 ) ) ;
#16740=ORIENTED_EDGE ( 'NONE', *, *, #24719, .F. ) ;
#16741=EDGE_CURVE ( 'NONE', #2976, #3034, #26557, .T. ) ;
#16754=ORIENTED_EDGE ( 'NONE', *, *, #26240, .F. ) ;
#16757=LINE ( 'NONE', #24930, #18291 ) ;
#16760=ORIENTED_EDGE ( 'NONE', *, *, #4184, .T. ) ;
#16762=CARTESIAN_POINT ( 'NONE',  ( 22.75111450864416085, -1.241879311143409511E-16, -2.499999999999998668 ) ) ;
#16771=CARTESIAN_POINT ( 'NONE',  ( 24.98500000273118715, -0.2613211581691358698, -2.486304738420681559 ) ) ;
#16773=DIRECTION ( 'NONE',  ( 1.000000000000000000, -8.574039729943018344E-17, -0.000000000000000000 ) ) ;
#16779=FACE_OUTER_BOUND ( 'NONE', #22932, .T. ) ;
#16781=ADVANCED_FACE ( 'NONE', ( #1144 ), #11341, .F. ) ;
#16794=ORIENTED_EDGE ( 'NONE', *, *, #6263, .F. ) ;
#16795=CARTESIAN_POINT ( 'NONE',  ( 22.73500000136559862, 1.570731468192929858, 2.892927487894329630 ) ) ;
#16799=CARTESIAN_POINT ( 'NONE',  ( 10.00000000000000000, -1.625881193364669297, -4.467071865485488402 ) ) ;
#16811=CARTESIAN_POINT ( 'NONE',  ( 23.98500000273118715, -0.2613211581691358698, -2.486304738420681559 ) ) ;
#16812=CARTESIAN_POINT ( 'NONE',  ( 25.75999999999999801, -2.208672634433321348E-15, 0.000000000000000000 ) ) ;
#16829=LINE ( 'NONE', #3643, #26188 ) ;
#16836=DIRECTION ( 'NONE',  ( 0.000000000000000000, 1.000000000000000000, 0.000000000000000000 ) ) ;
#16849=DIRECTION ( 'NONE',  ( 0.000000000000000000, 0.000000000000000000, -1.000000000000000000 ) ) ;
#16850=ORIENTED_EDGE ( 'NONE', *, *, #25657, .T. ) ;
#16854=LINE ( 'NONE', #1486, #17758 ) ;
#16866=FACE_OUTER_BOUND ( 'NONE', #21214, .T. ) ;
#16870=DIRECTION ( 'NONE',  ( -1.000000000000000000, 8.574039729943019576E-17, 1.232595164407830946E-32 ) ) ;
#16872=CARTESIAN_POINT ( 'NONE',  ( 23.73500000000000298, -0.2613211581691358698, -2.486304738420681559 ) ) ;
#16874=CARTESIAN_POINT ( 'NONE',  ( 10.00000000000000000, 0.8254815157535241310, 4.681538312723519724 ) ) ;
#16878=DIRECTION ( 'NONE',  ( 0.000000000000000000, 1.000000000000000000, 0.000000000000000000 ) ) ;
#16882=ORIENTED_EDGE ( 'NONE', *, *, #17071, .F. ) ;
#16884=DIRECTION ( 'NONE',  ( -1.000000000000000000, 8.574039729943018344E-17, -0.000000000000000000 ) ) ;
#16891=CARTESIAN_POINT ( 'NONE',  ( 10.00000000000000000, 3.055657119358849094, -3.641590349731898879 ) ) ;
#16895=ORIENTED_EDGE ( 'NONE', *, *, #12858, .F. ) ;
#16897=DIRECTION ( 'NONE',  ( 8.574039729943018344E-17, 1.000000000000000000, 0.000000000000000000 ) ) ;
#16908=ORIENTED_EDGE ( 'NONE', *, *, #26372, .F. ) ;
#16910=ADVANCED_FACE ( 'NONE', ( #9827 ), #2131, .F. ) ;
#16915=LINE ( 'NONE', #27108, #31637 ) ;
#16931=CARTESIAN_POINT ( 'NONE',  ( 10.00000000000000000, 5.009999999999999787, 0.000000000000000000 ) ) ;
#16940=VERTEX_POINT ( 'NONE', #311 ) ;
#16941=CARTESIAN_POINT ( 'NONE',  ( 10.55147673363119232, -4.208382051008212166, 2.718385644597158812 ) ) ;
#16943=ORIENTED_EDGE ( 'NONE', *, *, #1372, .F. ) ;
#16945=CARTESIAN_POINT ( 'NONE',  ( 22.23500000136559507, -1.570731468192933633, -2.892927487894330962 ) ) ;
#16948=FACE_OUTER_BOUND ( 'NONE', #182, .T. ) ;
#16954=CARTESIAN_POINT ( 'NONE',  ( 24.23500000136559507, -1.570731468192933633, -2.892927487894330074 ) ) ;
#16955=PLANE ( 'NONE',  #22082 ) ;
#16962=LINE ( 'NONE', #29188, #662 ) ;
#16968=EDGE_CURVE ( 'NONE', #2120, #31503, #25374, .T. ) ;
#16979=LINE ( 'NONE', #22334, #11816 ) ;
#16980=DIRECTION ( 'NONE',  ( 7.472768010111698665E-18, 0.08715574274766461904, -0.9961946980917449901 ) ) ;
#16989=CARTESIAN_POINT ( 'NONE',  ( 25.67945691304631595, 2.703519047173982948, -1.190363068855617712 ) ) ;
#16990=ORIENTED_EDGE ( 'NONE', *, *, #2823, .T. ) ;
#16997=CARTESIAN_POINT ( 'NONE',  ( 24.50111451137534146, -3.256483526998273983E-15, 2.499999999999998668 ) ) ;
#16999=ORIENTED_EDGE ( 'NONE', *, *, #7167, .T. ) ;
#17000=DIRECTION ( 'NONE',  ( 7.023442172597814953E-17, 0.8191520442889869136, 0.5735764363510531538 ) ) ;
#17004=CARTESIAN_POINT ( 'NONE',  ( 25.61000000136559507, 2.892927487894327410, -1.570731468192931635 ) ) ;
#17005=EDGE_CURVE ( 'NONE', #18235, #18153, #17852, .T. ) ;
#17016=ORIENTED_EDGE ( 'NONE', *, *, #28298, .T. ) ;
#17020=CARTESIAN_POINT ( 'NONE',  ( 24.98499999999999943, 2.486304738420679783, -0.2613211581691337604 ) ) ;
#17028=VERTEX_POINT ( 'NONE', #2635 ) ;
#17030=VERTEX_POINT ( 'NONE', #15671 ) ;
#17034=CARTESIAN_POINT ( 'NONE',  ( 25.76000000000000512, 2.749440278475487442, 1.299952413566024756 ) ) ;
#17049=DIRECTION ( 'NONE',  ( 1.000000000000000000, -8.574039729943018344E-17, -0.000000000000000000 ) ) ;
#17054=EDGE_LOOP ( 'NONE', ( #9212, #27169, #7121 ) ) ;
#17059=CARTESIAN_POINT ( 'NONE',  ( 23.25111450864416085, -3.256483526998273983E-15, 2.499999999999998668 ) ) ;
#17064=CARTESIAN_POINT ( 'NONE',  ( 22.36000000000000298, -1.573300977624594976, 1.942864903642425700 ) ) ;
#17068=ORIENTED_EDGE ( 'NONE', *, *, #10774, .F. ) ;
#17071=EDGE_CURVE ( 'NONE', #5453, #1564, #28365, .T. ) ;
#17072=AXIS2_PLACEMENT_3D ( 'NONE', #7954, #18145, #30547 ) ;
#17074=CARTESIAN_POINT ( 'NONE',  ( 22.92250000136559862, -1.913930629741527500, 2.363507492473149618 ) ) ;
#17077=CARTESIAN_POINT ( 'NONE',  ( 21.25111450864416085, -3.256483526998273983E-15, 2.499999999999998668 ) ) ;
#17091=VERTEX_POINT ( 'NONE', #28699 ) ;
#17100=VERTEX_POINT ( 'NONE', #21663 ) ;
#17103=CARTESIAN_POINT ( 'NONE',  ( 21.98500000136559507, -2.892927487894331406, 1.570731468192932523 ) ) ;
#17104=ORIENTED_EDGE ( 'NONE', *, *, #18267, .F. ) ;
#17105=PLANE ( 'NONE',  #19318 ) ;
#17113=CARTESIAN_POINT ( 'NONE',  ( 22.79750000136559862, 0.3178988483021036315, 3.024605502323848949 ) ) ;
#17150=ADVANCED_FACE ( 'NONE', ( #8618 ), #18505, .F. ) ;
#17154=CARTESIAN_POINT ( 'NONE',  ( 10.55147673363119232, -2.376879293651037006, -4.116875700062107235 ) ) ;
#17162=CARTESIAN_POINT ( 'NONE',  ( 10.00000000000000000, -1.115095498423275933, -4.884328206559848340 ) ) ;
#17171=LINE ( 'NONE', #11825, #31657 ) ;
#17180=VECTOR ( 'NONE', #7062, 1000.000000000000000 ) ;
#17182=CARTESIAN_POINT ( 'NONE',  ( 25.11000000136559507, -2.892927487894331406, 1.570731468192932301 ) ) ;
#17191=ADVANCED_FACE ( 'NONE', ( #13781 ), #23568, .F. ) ;
#17203=ORIENTED_EDGE ( 'NONE', *, *, #25449, .F. ) ;
#17207=ADVANCED_FACE ( 'NONE', ( #13946 ), #11468, .F. ) ;
#17209=CARTESIAN_POINT ( 'NONE',  ( 25.86000000136559862, 1.570731468192929858, 2.892927487894329186 ) ) ;
#17235=AXIS2_PLACEMENT_3D ( 'NONE', #7937, #5436, #5760 ) ;
#17237=DIRECTION ( 'NONE',  ( 2.219124775574910312E-17, 0.2588190451025183525, 0.9659258262890689783 ) ) ;
#17238=VERTEX_POINT ( 'NONE', #22485 ) ;
#17241=AXIS2_PLACEMENT_3D ( 'NONE', #8494, #6482, #16502 ) ;
#17278=ORIENTED_EDGE ( 'NONE', *, *, #10528, .T. ) ;
#17280=DIRECTION ( 'NONE',  ( 0.000000000000000000, 1.000000000000000000, 0.000000000000000000 ) ) ;
#17282=VERTEX_POINT ( 'NONE', #9281 ) ;
#17286=AXIS2_PLACEMENT_3D ( 'NONE', #19621, #12093, #19289 ) ;
#17295=ORIENTED_EDGE ( 'NONE', *, *, #15588, .F. ) ;
#17297=CARTESIAN_POINT ( 'NONE',  ( 21.23500000136559507, -1.570731468192933633, -2.892927487894330962 ) ) ;
#17299=VERTEX_POINT ( 'NONE', #32378 ) ;
#17304=DIRECTION ( 'NONE',  ( -7.023442172597859327E-17, -0.8191520442889911324, 0.5735764363510470476 ) ) ;
#17305=CARTESIAN_POINT ( 'NONE',  ( 24.04750000136559507, -3.024605502323851169, 0.3178988483021052969 ) ) ;
#17315=DIRECTION ( 'NONE',  ( 0.000000000000000000, -0.2588190451025108030, -0.9659258262890709767 ) ) ;
#17326=DIRECTION ( 'NONE',  ( 0.000000000000000000, 0.2588190451025115246, 0.9659258262890707547 ) ) ;
#17333=ADVANCED_FACE ( 'NONE', ( #9435 ), #24474, .T. ) ;
#17341=VERTEX_POINT ( 'NONE', #1592 ) ;
#17346=VERTEX_POINT ( 'NONE', #32530 ) ;
#17351=DIRECTION ( 'NONE',  ( -7.023442172597887676E-17, -0.8191520442889951292, 0.5735764363510412744 ) ) ;
#17359=CARTESIAN_POINT ( 'NONE',  ( -7.077711312404032898E-17, -0.8254815157534933778, -4.681538312723525053 ) ) ;
#17365=DIRECTION ( 'NONE',  ( -7.472768010111758754E-18, -0.08715574274766552110, 0.9961946980917449901 ) ) ;
#17380=CARTESIAN_POINT ( 'NONE',  ( 23.61000000136559507, 2.892927487894327410, -1.570731468192931635 ) ) ;
#17398=FACE_OUTER_BOUND ( 'NONE', #17893, .T. ) ;
#17403=ORIENTED_EDGE ( 'NONE', *, *, #26446, .F. ) ;
#17404=ADVANCED_FACE ( 'NONE', ( #30521 ), #10448, .T. ) ;
#17426=CARTESIAN_POINT ( 'NONE',  ( 23.11000000136559507, -3.156283516753370044, -0.9349337715887220401 ) ) ;
#17443=ORIENTED_EDGE ( 'NONE', *, *, #7480, .T. ) ;
#17448=DIRECTION ( 'NONE',  ( 7.770718973608968796E-17, 0.9063077870366493816, 0.4226182617407006070 ) ) ;
#17449=ORIENTED_EDGE ( 'NONE', *, *, #24960, .T. ) ;
#17454=DIRECTION ( 'NONE',  ( -1.000000000000000000, 8.574039729943018344E-17, -0.000000000000000000 ) ) ;
#17479=EDGE_LOOP ( 'NONE', ( #30928, #9291, #8824, #11507 ) ) ;
#17480=CARTESIAN_POINT ( 'NONE',  ( 10.00000000000000000, 4.116875700062115229, -2.376879293651021019 ) ) ;
#17485=CARTESIAN_POINT ( 'NONE',  ( 10.00000000000000000, 3.641590349731970822, -3.055657119358763829 ) ) ;
#17486=DIRECTION ( 'NONE',  ( -7.023442172597786603E-17, -0.8191520442889833609, -0.5735764363510580388 ) ) ;
#17508=EDGE_CURVE ( 'NONE', #28583, #32678, #14938, .T. ) ;
#17512=ORIENTED_EDGE ( 'NONE', *, *, #27240, .F. ) ;
#17517=EDGE_CURVE ( 'NONE', #21706, #61, #4706, .T. ) ;
#17524=CARTESIAN_POINT ( 'NONE',  ( 0.000000000000000000, 0.000000000000000000, 0.000000000000000000 ) ) ;
#17526=CARTESIAN_POINT ( 'NONE',  ( 21.54750000000000654, -2.594547506269383685, -0.7685399846772043020 ) ) ;
#17541=EDGE_CURVE ( 'NONE', #3406, #10158, #16757, .T. ) ;
#17542=CARTESIAN_POINT ( 'NONE',  ( 24.23500000136559507, -3.156283516753370488, -0.9349337715887220401 ) ) ;
#17545=DIRECTION ( 'NONE',  ( -4.917867153433080997E-17, -0.5735764363510552633, 0.8191520442889853593 ) ) ;
#17552=DIRECTION ( 'NONE',  ( 8.574039729943018344E-17, 1.000000000000000000, 0.000000000000000000 ) ) ;
#17553=VERTEX_POINT ( 'NONE', #1712 ) ;
#17556=EDGE_LOOP ( 'NONE', ( #26226, #27808, #25447, #8574 ) ) ;
#17562=CARTESIAN_POINT ( 'NONE',  ( 7.077711312404847644E-17, 0.8254815157535873027, -4.681538312723508177 ) ) ;
#17564=CARTESIAN_POINT ( 'NONE',  ( 22.49290772595112387, 0.1310194482076003919, 2.499999999999998668 ) ) ;
#17574=CARTESIAN_POINT ( 'NONE',  ( 23.50111451137534857, -3.256483526998273983E-15, 2.499999999999998668 ) ) ;
#17580=DIRECTION ( 'NONE',  ( 1.000000000000000000, -0.000000000000000000, -0.000000000000000000 ) ) ;
#17593=ORIENTED_EDGE ( 'NONE', *, *, #13422, .F. ) ;
#17597=FACE_OUTER_BOUND ( 'NONE', #26015, .T. ) ;
#17615=DIRECTION ( 'NONE',  ( -1.000000000000000000, 8.574039729943018344E-17, -0.000000000000000000 ) ) ;
#17621=VECTOR ( 'NONE', #13016, 1000.000000000000000 ) ;
#17632=CIRCLE ( 'NONE', #24571, 5.010000000000000675 ) ;
#17640=VERTEX_POINT ( 'NONE', #13260 ) ;
#17643=ORIENTED_EDGE ( 'NONE', *, *, #28090, .F. ) ;
#17645=DIRECTION ( 'NONE',  ( -6.062761635205572056E-17, -0.7071067811865460184, -0.7071067811865490160 ) ) ;
#17652=CIRCLE ( 'NONE', #31530, 5.009999999999999787 ) ;
#17655=DIRECTION ( 'NONE',  ( 7.770718973608983587E-17, 0.9063077870366511579, -0.4226182617406968878 ) ) ;
#17668=CARTESIAN_POINT ( 'NONE',  ( 22.23500000136559862, -3.156283516753370044, -0.9349337715887220401 ) ) ;
#17674=ORIENTED_EDGE ( 'NONE', *, *, #28600, .T. ) ;
#17677=AXIS2_PLACEMENT_3D ( 'NONE', #22033, #11501, #6466 ) ;
#17690=LINE ( 'NONE', #25040, #1251 ) ;
#17692=CARTESIAN_POINT ( 'NONE',  ( 21.35999999999999943, -1.573300977624594976, 1.942864903642425700 ) ) ;
#17698=AXIS2_PLACEMENT_3D ( 'NONE', #24792, #16773, #30166 ) ;
#17703=ORIENTED_EDGE ( 'NONE', *, *, #29080, .F. ) ;
#17712=CARTESIAN_POINT ( 'NONE',  ( 21.54750000136559507, 1.913930629741522838, -2.363507492473150062 ) ) ;
#17716=AXIS2_PLACEMENT_3D ( 'NONE', #15778, #16407, #31652 ) ;
#17720=LINE ( 'NONE', #2529, #15132 ) ;
#17722=DIRECTION ( 'NONE',  ( 1.000000000000000000, -8.574039729943018344E-17, -0.000000000000000000 ) ) ;
#17724=ADVANCED_FACE ( 'NONE', ( #18301 ), #15935, .F. ) ;
#17725=AXIS2_PLACEMENT_3D ( 'NONE', #19149, #29338, #21330 ) ;
#17728=EDGE_LOOP ( 'NONE', ( #28023, #239, #22605, #1738 ) ) ;
#17739=EDGE_CURVE ( 'NONE', #24462, #19352, #24793, .T. ) ;
#17744=DIRECTION ( 'NONE',  ( -8.281886410780513492E-17, -0.9659258262890682012, 0.2588190451025209060 ) ) ;
#17756=CARTESIAN_POINT ( 'NONE',  ( 25.42250000136559507, 1.913930629741522838, -2.363507492473150062 ) ) ;
#17758=VECTOR ( 'NONE', #21707, 1000.000000000000000 ) ;
#17760=EDGE_CURVE ( 'NONE', #20952, #19944, #27121, .T. ) ;
#17763=ORIENTED_EDGE ( 'NONE', *, *, #14330, .F. ) ;
#17769=CARTESIAN_POINT ( 'NONE',  ( 25.32825331906372668, 2.585664297775035259, 0.3776202052181991675 ) ) ;
#17774=ADVANCED_FACE ( 'NONE', ( #26974 ), #12087, .F. ) ;
#17791=ORIENTED_EDGE ( 'NONE', *, *, #22705, .T. ) ;
#17811=AXIS2_PLACEMENT_3D ( 'NONE', #11256, #24444, #31680 ) ;
#17824=EDGE_CURVE ( 'NONE', #26609, #32336, #27290, .T. ) ;
#17833=DIRECTION ( 'NONE',  ( 0.000000000000000000, 1.000000000000000000, 0.000000000000000000 ) ) ;
#17835=DIRECTION ( 'NONE',  ( -1.000000000000000000, 8.574039729943022041E-17, -0.000000000000000000 ) ) ;
#17845=CARTESIAN_POINT ( 'NONE',  ( 10.00000000000000178, 2.285372942704952060, 4.458382051008203284 ) ) ;
#17852=LINE ( 'NONE', #30747, #2229 ) ;
#17860=CARTESIAN_POINT ( 'NONE',  ( 24.42250000136559507, -0.3178988483021076838, -3.024605502323848949 ) ) ;
#17882=CARTESIAN_POINT ( 'NONE',  ( 23.42250000136559862, -0.3178988483021076838, -3.024605502323848949 ) ) ;
#17883=DIRECTION ( 'NONE',  ( 4.917867153432994099E-17, 0.5735764363510447161, 0.8191520442889927978 ) ) ;
#17889=FACE_OUTER_BOUND ( 'NONE', #8430, .T. ) ;
#17893=EDGE_LOOP ( 'NONE', ( #26205, #23559, #17703, #13028 ) ) ;
#17895=DIRECTION ( 'NONE',  ( 1.000000000000000000, -8.574039729943018344E-17, -0.000000000000000000 ) ) ;
#17896=CARTESIAN_POINT ( 'NONE',  ( 21.23500000136559507, -3.156283516753370488, -0.9349337715887220401 ) ) ;
#17904=ORIENTED_EDGE ( 'NONE', *, *, #29612, .T. ) ;
#17926=CARTESIAN_POINT ( 'NONE',  ( 21.17250000136559507, -3.024605502323851169, 0.3178988483021052969 ) ) ;
#17933=CARTESIAN_POINT ( 'NONE',  ( 21.92250000136559507, -1.913930629741527500, 2.363507492473149618 ) ) ;
#17941=CARTESIAN_POINT ( 'NONE',  ( 10.00000000000000000, -3.055657119358777152, -3.641590349731960163 ) ) ;
#17944=ORIENTED_EDGE ( 'NONE', *, *, #30836, .T. ) ;
#17946=LINE ( 'NONE', #10417, #23705 ) ;
#17966=LINE ( 'NONE', #12933, #18157 ) ;
#17973=DIRECTION ( 'NONE',  ( 7.770718973608992215E-17, 0.9063077870366524902, -0.4226182617406938347 ) ) ;
#17984=ORIENTED_EDGE ( 'NONE', *, *, #4868, .F. ) ;
#18026=DIRECTION ( 'NONE',  ( 1.000000000000000000, -0.000000000000000000, -0.000000000000000000 ) ) ;
#18036=CARTESIAN_POINT ( 'NONE',  ( 20.98500000136559862, -0.9349337715887248157, 3.156283516753367824 ) ) ;
#18037=LINE ( 'NONE', #23231, #119 ) ;
#18043=CARTESIAN_POINT ( 'NONE',  ( 22.23500000000000298, 0.2613211581691317065, 2.486304738420681559 ) ) ;
#18050=CARTESIAN_POINT ( 'NONE',  ( 21.98500000136559507, -0.9349337715887247047, 3.156283516753367824 ) ) ;
#18064=ORIENTED_EDGE ( 'NONE', *, *, #4938, .T. ) ;
#18070=FACE_OUTER_BOUND ( 'NONE', #22421, .T. ) ;
#18075=CARTESIAN_POINT ( 'NONE',  ( 24.98500000136559507, -2.892927487894331406, 1.570731468192932301 ) ) ;
#18076=CARTESIAN_POINT ( 'NONE',  ( 25.75999999999999801, -2.208672634433321348E-15, 0.000000000000000000 ) ) ;
#18077=EDGE_CURVE ( 'NONE', #17640, #15936, #26455, .T. ) ;
#18083=CARTESIAN_POINT ( 'NONE',  ( 21.73500000136559507, 1.570731468192929858, 2.892927487894329186 ) ) ;
#18084=LINE ( 'NONE', #13223, #10811 ) ;
#18096=ORIENTED_EDGE ( 'NONE', *, *, #21455, .F. ) ;
#18102=EDGE_LOOP ( 'NONE', ( #10868, #4964, #4588, #16794 ) ) ;
#18118=DIRECTION ( 'NONE',  ( 0.000000000000000000, -0.4226182617406974984, -0.9063077870366508249 ) ) ;
#18119=DIRECTION ( 'NONE',  ( 7.023442172597882746E-17, 0.8191520442889946851, -0.5735764363510419406 ) ) ;
#18129=CARTESIAN_POINT ( 'NONE',  ( 25.25210947164438124, -0.1742962440539902735, 2.517109471644361385 ) ) ;
#18139=ORIENTED_EDGE ( 'NONE', *, *, #19703, .T. ) ;
#18140=ORIENTED_EDGE ( 'NONE', *, *, #2933, .F. ) ;
#18144=DIRECTION ( 'NONE',  ( 7.023442172597854396E-17, 0.8191520442889912434, -0.5735764363510469366 ) ) ;
#18145=DIRECTION ( 'NONE',  ( 3.623545766764271938E-17, 0.4226182617407062136, -0.9063077870366468280 ) ) ;
#18153=VERTEX_POINT ( 'NONE', #4039 ) ;
#18157=VECTOR ( 'NONE', #32737, 1000.000000000000000 ) ;
#18162=VECTOR ( 'NONE', #10470, 1000.000000000000227 ) ;
#18165=ORIENTED_EDGE ( 'NONE', *, *, #19153, .F. ) ;
#18172=ORIENTED_EDGE ( 'NONE', *, *, #21954, .F. ) ;
#18189=CARTESIAN_POINT ( 'NONE',  ( 10.00000000000000178, -8.574039729943018837E-16, 0.000000000000000000 ) ) ;
#18191=CARTESIAN_POINT ( 'NONE',  ( 4.013969549054183686E-16, 4.681538312723517059, 0.8254815157535410064 ) ) ;
#18194=ORIENTED_EDGE ( 'NONE', *, *, #1517, .T. ) ;
#18196=DIRECTION ( 'NONE',  ( 8.574039729943018344E-17, 1.000000000000000000, 0.000000000000000000 ) ) ;
#18216=VECTOR ( 'NONE', #17448, 1000.000000000000114 ) ;
#18222=VERTEX_POINT ( 'NONE', #669 ) ;
#18227=ORIENTED_EDGE ( 'NONE', *, *, #29823, .F. ) ;
#18229=DIRECTION ( 'NONE',  ( -8.281886410780538144E-17, -0.9659258262890716429, 0.2588190451025081940 ) ) ;
#18235=VERTEX_POINT ( 'NONE', #13042 ) ;
#18249=CARTESIAN_POINT ( 'NONE',  ( 22.42250000136559507, 1.913930629741522838, -2.363507492473150062 ) ) ;
#18258=VECTOR ( 'NONE', #14977, 1000.000000000000114 ) ;
#18260=CIRCLE ( 'NONE', #32170, 5.999999999999999112 ) ;
#18261=CARTESIAN_POINT ( 'NONE',  ( 25.71953681024719174, 1.150786689167072163, 2.772749569664193725 ) ) ;
#18267=EDGE_CURVE ( 'NONE', #19049, #26729, #5189, .T. ) ;
#18273=CARTESIAN_POINT ( 'NONE',  ( 4.013969549054193054E-16, 4.681538312723529494, -0.8254815157534771686 ) ) ;
#18277=ORIENTED_EDGE ( 'NONE', *, *, #10562, .F. ) ;
#18291=VECTOR ( 'NONE', #4559, 1000.000000000000000 ) ;
#18293=VECTOR ( 'NONE', #32481, 1000.000000000000000 ) ;
#18301=FACE_OUTER_BOUND ( 'NONE', #19253, .T. ) ;
#18302=ORIENTED_EDGE ( 'NONE', *, *, #23455, .T. ) ;
#18311=CARTESIAN_POINT ( 'NONE',  ( 25.33479043841976974, -2.021976348156035108, 1.643476287762689170 ) ) ;
#18313=VECTOR ( 'NONE', #7165, 1000.000000000000000 ) ;
#18317=CIRCLE ( 'NONE', #12439, 5.009999999999999787 ) ;
#18325=LINE ( 'NONE', #33039, #97 ) ;
#18333=DIRECTION ( 'NONE',  ( 0.000000000000000000, 1.000000000000000000, 0.000000000000000000 ) ) ;
#18341=DIRECTION ( 'NONE',  ( 1.000000000000000000, -8.574039729943018344E-17, -0.000000000000000000 ) ) ;
#18356=ORIENTED_EDGE ( 'NONE', *, *, #26158, .T. ) ;
#18362=ORIENTED_EDGE ( 'NONE', *, *, #3980, .F. ) ;
#18365=VECTOR ( 'NONE', #30162, 999.9999999999998863 ) ;
#18366=ORIENTED_EDGE ( 'NONE', *, *, #24487, .F. ) ;
#18386=ORIENTED_EDGE ( 'NONE', *, *, #25491, .F. ) ;
#18396=ADVANCED_FACE ( 'NONE', ( #19192 ), #4154, .F. ) ;
#18400=ORIENTED_EDGE ( 'NONE', *, *, #9027, .T. ) ;
#18404=VERTEX_POINT ( 'NONE', #1337 ) ;
#18407=EDGE_CURVE ( 'NONE', #26134, #28186, #6168, .T. ) ;
#18411=ORIENTED_EDGE ( 'NONE', *, *, #32065, .F. ) ;
#18414=ORIENTED_EDGE ( 'NONE', *, *, #171, .F. ) ;
#18416=CARTESIAN_POINT ( 'NONE',  ( 0.000000000000000000, 0.000000000000000000, 0.000000000000000000 ) ) ;
#18422=ORIENTED_EDGE ( 'NONE', *, *, #13121, .F. ) ;
#18427=FACE_OUTER_BOUND ( 'NONE', #23653, .T. ) ;
#18430=LINE ( 'NONE', #20613, #24242 ) ;
#18432=CARTESIAN_POINT ( 'NONE',  ( 24.42250000273118715, 1.291182301015469047, 2.378061970571981654 ) ) ;
#18434=CARTESIAN_POINT ( 'NONE',  ( 10.00000000000000000, -1.625881193364669075, -4.467071865485488402 ) ) ;
#18440=DIRECTION ( 'NONE',  ( -7.023442172597900002E-17, -0.8191520442889969056, 0.5735764363510388320 ) ) ;
#18466=EDGE_CURVE ( 'NONE', #26782, #5049, #26894, .T. ) ;
#18475=CARTESIAN_POINT ( 'NONE',  ( 23.23500000136559862, -3.156283516753370044, -0.9349337715887220401 ) ) ;
#18477=CARTESIAN_POINT ( 'NONE',  ( 25.39550262306211792, -2.656620010619367811, 0.2256117632562368858 ) ) ;
#18479=VERTEX_POINT ( 'NONE', #23878 ) ;
#18487=CARTESIAN_POINT ( 'NONE',  ( 25.11000000136559507, -3.156283516753370488, -0.9349337715887220401 ) ) ;
#18500=EDGE_CURVE ( 'NONE', #23437, #13750, #16854, .T. ) ;
#18505=PLANE ( 'NONE',  #4900 ) ;
#18524=ORIENTED_EDGE ( 'NONE', *, *, #4689, .F. ) ;
#18538=DIRECTION ( 'NONE',  ( -1.000000000000000000, 8.574039729943018344E-17, -0.000000000000000000 ) ) ;
#18549=VERTEX_POINT ( 'NONE', #13867 ) ;
#18559=VERTEX_POINT ( 'NONE', #31802 ) ;
#18570=CARTESIAN_POINT ( 'NONE',  ( 21.54750000136559507, 3.024605502323846729, -0.3178988483021056854 ) ) ;
#18571=EDGE_CURVE ( 'NONE', #26955, #16550, #10320, .T. ) ;
#18572=PLANE ( 'NONE',  #28833 ) ;
#18573=CARTESIAN_POINT ( 'NONE',  ( 10.00000000000000000, 4.753758587302147731, -3.462581523170085693E-33 ) ) ;
#18575=EDGE_CURVE ( 'NONE', #6678, #26955, #26344, .T. ) ;
#18578=CARTESIAN_POINT ( 'NONE',  ( 22.54750000273119070, -0.7685399846772070775, 2.594547506269381465 ) ) ;
#18599=DIRECTION ( 'NONE',  ( 1.000000000000000000, -8.574039729943018344E-17, -0.000000000000000000 ) ) ;
#18600=EDGE_CURVE ( 'NONE', #13681, #19944, #9519, .T. ) ;
#18609=DIRECTION ( 'NONE',  ( 1.000000000000000000, -8.574039729943018344E-17, -0.000000000000000000 ) ) ;
#18619=ORIENTED_EDGE ( 'NONE', *, *, #2050, .F. ) ;
#18620=CARTESIAN_POINT ( 'NONE',  ( 24.48500000136559507, 0.9349337715887185984, -3.156283516753368268 ) ) ;
#18621=EDGE_CURVE ( 'NONE', #228, #7359, #17720, .T. ) ;
#18623=CARTESIAN_POINT ( 'NONE',  ( 25.56220348721820201, -1.341958225229829886E-11, -2.827203487218203914 ) ) ;
#18630=CARTESIAN_POINT ( 'NONE',  ( 10.55147673363118876, 2.285372942705016452, -4.458382051008168645 ) ) ;
#18639=CARTESIAN_POINT ( 'NONE',  ( 21.86000000273118715, -1.942864903642428587, -1.573300977624592756 ) ) ;
#18653=CARTESIAN_POINT ( 'NONE',  ( 21.73499999999999943, -0.2613211581691358698, -2.486304738420681559 ) ) ;
#18657=AXIS2_PLACEMENT_3D ( 'NONE', #11063, #31462, #15589 ) ;
#18661=DIRECTION ( 'NONE',  ( 1.000000000000000000, -0.000000000000000000, -0.000000000000000000 ) ) ;
#18666=ORIENTED_EDGE ( 'NONE', *, *, #12253, .T. ) ;
#18678=AXIS2_PLACEMENT_3D ( 'NONE', #12360, #17895, #22579 ) ;
#18698=DIRECTION ( 'NONE',  ( -6.062761635205527683E-17, -0.7071067811865410224, -0.7071067811865540120 ) ) ;
#18713=ORIENTED_EDGE ( 'NONE', *, *, #11285, .T. ) ;
#18726=CARTESIAN_POINT ( 'NONE',  ( 22.17250000136559507, -2.363507492473152283, -1.913930629741525280 ) ) ;
#18733=FACE_OUTER_BOUND ( 'NONE', #17054, .T. ) ;
#18734=CARTESIAN_POINT ( 'NONE',  ( 20.79750000273119070, -2.594547506269383685, -0.7685399846772043020 ) ) ;
#18745=DIRECTION ( 'NONE',  ( 0.000000000000000000, 1.000000000000000000, 0.000000000000000000 ) ) ;
#18757=AXIS2_PLACEMENT_3D ( 'NONE', #1049, #3725, #19103 ) ;
#18770=VERTEX_POINT ( 'NONE', #16359 ) ;
#18778=DIRECTION ( 'NONE',  ( 0.000000000000000000, -0.08715574274766814400, 0.9961946980917446570 ) ) ;
#18787=AXIS2_PLACEMENT_3D ( 'NONE', #7492, #2661, #336 ) ;
#18795=ADVANCED_FACE ( 'NONE', ( #14175 ), #19044, .F. ) ;
#18799=( LENGTH_UNIT ( ) NAMED_UNIT ( * ) SI_UNIT ( .MILLI., .METRE. ) );
#18801=EDGE_LOOP ( 'NONE', ( #26079, #14960, #1716, #20516 ) ) ;
#18811=DIRECTION ( 'NONE',  ( -8.541412920197209954E-17, -0.9961946980917446570, -0.08715574274766894891 ) ) ;
#18812=AXIS2_PLACEMENT_3D ( 'NONE', #6471, #24513, #1639 ) ;
#18813=VECTOR ( 'NONE', #1244, 1000.000000000000000 ) ;
#18822=AXIS2_PLACEMENT_3D ( 'NONE', #23868, #975, #3653 ) ;
#18824=CYLINDRICAL_SURFACE ( 'NONE', #31515, 5.000000000000002665 ) ;
#18827=EDGE_CURVE ( 'NONE', #17238, #28583, #9333, .T. ) ;
#18833=DIRECTION ( 'NONE',  ( -1.000000000000000000, 8.574039729943018344E-17, -0.000000000000000000 ) ) ;
#18838=VECTOR ( 'NONE', #10722, 1000.000000000000114 ) ;
#18839=CARTESIAN_POINT ( 'NONE',  ( 10.56870887191539587, 1.946309384392590047, 4.616489984850538519 ) ) ;
#18847=DIRECTION ( 'NONE',  ( -1.000000000000000000, 8.574039729943017111E-17, -0.000000000000000000 ) ) ;
#18852=AXIS2_PLACEMENT_3D ( 'NONE', #3015, #31079, #23370 ) ;
#18853=ORIENTED_EDGE ( 'NONE', *, *, #7960, .T. ) ;
#18859=CARTESIAN_POINT ( 'NONE',  ( 25.75999999999999801, -2.208672634433321348E-15, 0.000000000000000000 ) ) ;
#18863=AXIS2_PLACEMENT_3D ( 'NONE', #16931, #11587, #19115 ) ;
#18874=CARTESIAN_POINT ( 'NONE',  ( 10.00000000000000178, -8.574039729943018837E-16, 0.000000000000000000 ) ) ;
#18877=DIRECTION ( 'NONE',  ( 0.000000000000000000, 0.000000000000000000, -1.000000000000000000 ) ) ;
#18883=CARTESIAN_POINT ( 'NONE',  ( 0.000000000000000000, 0.000000000000000000, 0.000000000000000000 ) ) ;
#18896=ORIENTED_EDGE ( 'NONE', *, *, #27526, .T. ) ;
#18901=DIRECTION ( 'NONE',  ( 8.574039729943018344E-17, 1.000000000000000000, 0.000000000000000000 ) ) ;
#18909=CARTESIAN_POINT ( 'NONE',  ( 9.999999999999998224, -4.681538312723512618, -0.8254815157535732029 ) ) ;
#18917=CARTESIAN_POINT ( 'NONE',  ( 21.92250000136559507, -1.913930629741527500, 2.363507492473149618 ) ) ;
#18938=ORIENTED_EDGE ( 'NONE', *, *, #29059, .F. ) ;
#18942=LINE ( 'NONE', #13098, #32032 ) ;
#18949=LINE ( 'NONE', #29465, #28438 ) ;
#18950=DIRECTION ( 'NONE',  ( 1.000000000000000000, -8.574039729943018344E-17, -0.000000000000000000 ) ) ;
#18957=AXIS2_PLACEMENT_3D ( 'NONE', #11879, #1871, #25057 ) ;
#18959=DIRECTION ( 'NONE',  ( 1.000000000000000000, -8.574039729943018344E-17, -0.000000000000000000 ) ) ;
#18962=DIRECTION ( 'NONE',  ( -4.917867153433037856E-17, -0.5735764363510502672, 0.8191520442889889120 ) ) ;
#18963=ORIENTED_EDGE ( 'NONE', *, *, #10994, .F. ) ;
#18971=ORIENTED_EDGE ( 'NONE', *, *, #27021, .F. ) ;
#18976=ORIENTED_EDGE ( 'NONE', *, *, #19958, .F. ) ;
#18981=CARTESIAN_POINT ( 'NONE',  ( 25.42250000136559507, 1.913930629741522838, -2.363507492473150062 ) ) ;
#18997=ADVANCED_FACE ( 'NONE', ( #19876 ), #32579, .F. ) ;
#19000=DIRECTION ( 'NONE',  ( 1.000000000000000000, -0.000000000000000000, -0.000000000000000000 ) ) ;
#19011=ORIENTED_EDGE ( 'NONE', *, *, #4072, .T. ) ;
#19022=FACE_OUTER_BOUND ( 'NONE', #28228, .T. ) ;
#19032=DIRECTION ( 'NONE',  ( 0.000000000000000000, 0.7071067811865465735, -0.7071067811865484609 ) ) ;
#19038=DIRECTION ( 'NONE',  ( 1.000000000000000000, -8.574039729943018344E-17, -0.000000000000000000 ) ) ;
#19044=PLANE ( 'NONE',  #4984 ) ;
#19046=DIRECTION ( 'NONE',  ( 0.000000000000000000, 0.9659258262890664248, 0.2588190451025276784 ) ) ;
#19049=VERTEX_POINT ( 'NONE', #32711 ) ;
#19058=LINE ( 'NONE', #11373, #28892 ) ;
#19061=CARTESIAN_POINT ( 'NONE',  ( 22.04750000000000298, 2.594547506269380133, 0.7685399846772031918 ) ) ;
#19067=EDGE_CURVE ( 'NONE', #1268, #16013, #31691, .T. ) ;
#19074=CARTESIAN_POINT ( 'NONE',  ( 21.61000000273118715, -1.573300977624594976, 1.942864903642425700 ) ) ;
#19075=DIRECTION ( 'NONE',  ( 1.000000000000000000, -8.574039729943018344E-17, -0.000000000000000000 ) ) ;
#19078=DIRECTION ( 'NONE',  ( 8.574039729943018344E-17, 1.000000000000000000, 0.000000000000000000 ) ) ;
#19080=DIRECTION ( 'NONE',  ( -1.000000000000000000, 8.574039729943019576E-17, -0.000000000000000000 ) ) ;
#19081=CARTESIAN_POINT ( 'NONE',  ( 25.75999999999999801, -2.208672634433321348E-15, 0.000000000000000000 ) ) ;
#19093=EDGE_LOOP ( 'NONE', ( #1853, #16521, #8920, #180 ) ) ;
#19096=EDGE_CURVE ( 'NONE', #28338, #3987, #14447, .T. ) ;
#19098=CARTESIAN_POINT ( 'NONE',  ( 10.00000000000000178, -4.787500056513379398, 1.476463073999621622 ) ) ;
#19103=DIRECTION ( 'NONE',  ( 0.000000000000000000, -0.5735764363510502672, 0.8191520442889889120 ) ) ;
#19111=DIRECTION ( 'NONE',  ( -8.281886410780485142E-17, -0.9659258262890653146, -0.2588190451025318417 ) ) ;
#19113=CARTESIAN_POINT ( 'NONE',  ( 7.077711312404307767E-17, 0.8254815157535250192, 4.681538312723519724 ) ) ;
#19114=DIRECTION ( 'NONE',  ( -8.281886410780502398E-17, -0.9659258262890674240, -0.2588190451025242367 ) ) ;
#19115=DIRECTION ( 'NONE',  ( -8.574039729943018344E-17, -1.000000000000000000, 0.000000000000000000 ) ) ;
#19116=ORIENTED_EDGE ( 'NONE', *, *, #14282, .T. ) ;
#19128=CARTESIAN_POINT ( 'NONE',  ( 25.71477796605636001, 1.827236184277983400, 2.576170543363066834 ) ) ;
#19131=LINE ( 'NONE', #16799, #9115 ) ;
#19135=CARTESIAN_POINT ( 'NONE',  ( 17.75999999999999801, -1.902510934646483477E-15, 2.499999999999996891 ) ) ;
#19143=DIRECTION ( 'NONE',  ( 6.062761635205574522E-17, 0.7071067811865465735, 0.7071067811865484609 ) ) ;
#19149=CARTESIAN_POINT ( 'NONE',  ( 10.00000000000000178, -8.574039729943018837E-16, 0.000000000000000000 ) ) ;
#19153=EDGE_CURVE ( 'NONE', #8114, #7359, #6781, .T. ) ;
#19159=ORIENTED_EDGE ( 'NONE', *, *, #16968, .F. ) ;
#19173=CYLINDRICAL_SURFACE ( 'NONE', #14623, 6.000000000000000000 ) ;
#19177=EDGE_LOOP ( 'NONE', ( #29133, #505, #15984, #13807 ) ) ;
#19190=CARTESIAN_POINT ( 'NONE',  ( 20.67250000273118715, -2.378061970571983430, 1.291182301015471490 ) ) ;
#19192=FACE_OUTER_BOUND ( 'NONE', #19444, .T. ) ;
#19196=DIRECTION ( 'NONE',  ( 2.219124775574870561E-17, 0.2588190451025141336, 0.9659258262890700886 ) ) ;
#19198=ORIENTED_EDGE ( 'NONE', *, *, #30836, .F. ) ;
#19200=EDGE_CURVE ( 'NONE', #26609, #11371, #1287, .T. ) ;
#19215=CARTESIAN_POINT ( 'NONE',  ( 24.67249999999999943, -1.291182301015472600, -2.378061970571982098 ) ) ;
#19216=CARTESIAN_POINT ( 'NONE',  ( -3.822634483660923045E-16, -4.458382051008209501, 2.285372942704937849 ) ) ;
#19217=CARTESIAN_POINT ( 'NONE',  ( 21.79750000000000654, 0.7685399846772009713, -2.594547506269381909 ) ) ;
#19225=LINE ( 'NONE', #29762, #19957 ) ;
#19231=CARTESIAN_POINT ( 'NONE',  ( 21.98500000273118715, -0.2613211581691358698, -2.486304738420681559 ) ) ;
#19233=LINE ( 'NONE', #24560, #5510 ) ;
#19237=CARTESIAN_POINT ( 'NONE',  ( 2.037945749704312686E-16, 2.376879293651064540, 4.116875700062091248 ) ) ;
#19244=LINE ( 'NONE', #21751, #5008 ) ;
#19245=CARTESIAN_POINT ( 'NONE',  ( 10.56183597391177464, -1.750323540954535505E-14, 4.753758587302147731 ) ) ;
#19253=EDGE_LOOP ( 'NONE', ( #8254, #22368, #32622, #1385 ) ) ;
#19254=VECTOR ( 'NONE', #14527, 1000.000000000000000 ) ;
#19263=DIRECTION ( 'NONE',  ( 8.574039729943018344E-17, 1.000000000000000000, 0.000000000000000000 ) ) ;
#19268=DIRECTION ( 'NONE',  ( 0.000000000000000000, 1.000000000000000000, 0.000000000000000000 ) ) ;
#19276=ORIENTED_EDGE ( 'NONE', *, *, #10839, .T. ) ;
#19279=AXIS2_PLACEMENT_3D ( 'NONE', #24330, #6128, #1441 ) ;
#19282=CARTESIAN_POINT ( 'NONE',  ( 25.23499999999999943, 0.2613211581691317065, 2.486304738420681559 ) ) ;
#19286=VECTOR ( 'NONE', #1284, 1000.000000000000000 ) ;
#19289=DIRECTION ( 'NONE',  ( 0.000000000000000000, 1.000000000000000000, 0.000000000000000000 ) ) ;
#19299=EDGE_LOOP ( 'NONE', ( #6582, #31173, #9532, #17984 ) ) ;
#19300=CARTESIAN_POINT ( 'NONE',  ( 22.04750000136559507, -3.024605502323851169, 0.3178988483021052969 ) ) ;
#19302=CARTESIAN_POINT ( 'NONE',  ( 10.00000000000000178, -8.574039729943018837E-16, 0.000000000000000000 ) ) ;
#19305=VERTEX_POINT ( 'NONE', #31352 ) ;
#19308=VECTOR ( 'NONE', #15249, 1000.000000000000000 ) ;
#19316=LINE ( 'NONE', #8936, #21066 ) ;
#19318=AXIS2_PLACEMENT_3D ( 'NONE', #25132, #24969, #2253 ) ;
#19352=VERTEX_POINT ( 'NONE', #29307 ) ;
#19358=ORIENTED_EDGE ( 'NONE', *, *, #20254, .F. ) ;
#19363=DIRECTION ( 'NONE',  ( 0.7071067811865449082, 8.659560562354964906E-17, 0.7071067811865501263 ) ) ;
#19370=DIRECTION ( 'NONE',  ( 1.000000000000000000, -0.000000000000000000, -0.000000000000000000 ) ) ;
#19386=CARTESIAN_POINT ( 'NONE',  ( 10.00000000000000000, -0.8254815157534940440, -4.681538312723525053 ) ) ;
#19389=ORIENTED_EDGE ( 'NONE', *, *, #14754, .T. ) ;
#19392=VECTOR ( 'NONE', #5345, 1000.000000000000114 ) ;
#19394=AXIS2_PLACEMENT_3D ( 'NONE', #25572, #2681, #5531 ) ;
#19395=ADVANCED_FACE ( 'NONE', ( #27637 ), #14909, .T. ) ;
#19400=CARTESIAN_POINT ( 'NONE',  ( 24.74290772321993970, -0.1310194482076044442, -2.499999999999998668 ) ) ;
#19402=CARTESIAN_POINT ( 'NONE',  ( 24.48499999999999943, -2.486304738420683780, 0.2613211581691335383 ) ) ;
#19420=AXIS2_PLACEMENT_3D ( 'NONE', #27482, #24448, #19472 ) ;
#19432=VERTEX_POINT ( 'NONE', #27300 ) ;
#19437=ORIENTED_EDGE ( 'NONE', *, *, #32044, .T. ) ;
#19441=ORIENTED_EDGE ( 'NONE', *, *, #22336, .T. ) ;
#19444=EDGE_LOOP ( 'NONE', ( #27176, #18400, #13248, #22041 ) ) ;
#19452=CARTESIAN_POINT ( 'NONE',  ( 22.74290772321994325, -0.1310194482076041944, -2.499999999999998224 ) ) ;
#19468=FACE_OUTER_BOUND ( 'NONE', #8650, .T. ) ;
#19469=CARTESIAN_POINT ( 'NONE',  ( 10.00000000000000000, 0.6226916219172712319, -4.971152295393295617 ) ) ;
#19472=DIRECTION ( 'NONE',  ( 0.000000000000000000, 1.000000000000000000, 0.000000000000000000 ) ) ;
#19482=VERTEX_POINT ( 'NONE', #2734 ) ;
#19483=CARTESIAN_POINT ( 'NONE',  ( 22.54750000136559507, 3.024605502323846729, -0.3178988483021056854 ) ) ;
#19488=DIRECTION ( 'NONE',  ( 1.000000000000000000, -8.574039729943018344E-17, -0.000000000000000000 ) ) ;
#19490=CYLINDRICAL_SURFACE ( 'NONE', #2844, 5.010000000000000675 ) ;
#19494=EDGE_CURVE ( 'NONE', #8558, #9572, #32246, .T. ) ;
#19499=CARTESIAN_POINT ( 'NONE',  ( 25.75999999999999801, -2.208672634433321348E-15, 0.000000000000000000 ) ) ;
#19500=CARTESIAN_POINT ( 'NONE',  ( 10.00000000000000178, -8.574039729943018837E-16, 0.000000000000000000 ) ) ;
#19503=ORIENTED_EDGE ( 'NONE', *, *, #7386, .F. ) ;
#19508=ORIENTED_EDGE ( 'NONE', *, *, #21152, .F. ) ;
#19509=PLANE ( 'NONE',  #10662 ) ;
#19514=FACE_OUTER_BOUND ( 'NONE', #9643, .T. ) ;
#19515=EDGE_LOOP ( 'NONE', ( #14813, #31915, #27946 ) ) ;
#19520=CARTESIAN_POINT ( 'NONE',  ( 25.75999999999999801, -2.208672634433321348E-15, 0.000000000000000000 ) ) ;
#19535=DIRECTION ( 'NONE',  ( 0.000000000000000000, -0.4226182617407089337, 0.9063077870366456068 ) ) ;
#19537=ORIENTED_EDGE ( 'NONE', *, *, #32082, .T. ) ;
#19539=ORIENTED_EDGE ( 'NONE', *, *, #27021, .T. ) ;
#19558=CARTESIAN_POINT ( 'NONE',  ( 24.29749999999999943, -0.7685399846772070775, 2.594547506269381465 ) ) ;
#19571=CARTESIAN_POINT ( 'NONE',  ( 25.75999999999999801, -2.208672634433321348E-15, -2.499999999999997780 ) ) ;
#19573=CARTESIAN_POINT ( 'NONE',  ( 24.61000000136559152, 2.892927487894327410, -1.570731468192931635 ) ) ;
#19577=EDGE_CURVE ( 'NONE', #19954, #8466, #26763, .T. ) ;
#19580=ORIENTED_EDGE ( 'NONE', *, *, #13422, .T. ) ;
#19589=CARTESIAN_POINT ( 'NONE',  ( 10.52034268205830614, -3.672404558090062832, 3.407865132560167432 ) ) ;
#19596=EDGE_CURVE ( 'NONE', #16296, #10256, #7149, .T. ) ;
#19602=CARTESIAN_POINT ( 'NONE',  ( 10.57125986779756843, 0.8254815157535241310, 4.681538312723519724 ) ) ;
#19603=DIRECTION ( 'NONE',  ( 0.000000000000000000, 1.000000000000000000, 0.000000000000000000 ) ) ;
#19605=ADVANCED_FACE ( 'NONE', ( #26606 ), #31805, .F. ) ;
#19608=DIRECTION ( 'NONE',  ( 0.000000000000000000, 1.000000000000000000, 0.000000000000000000 ) ) ;
#19621=CARTESIAN_POINT ( 'NONE',  ( 25.75999999999999801, -2.208672634433321348E-15, 0.000000000000000000 ) ) ;
#19626=ORIENTED_EDGE ( 'NONE', *, *, #17508, .T. ) ;
#19627=ORIENTED_EDGE ( 'NONE', *, *, #381, .F. ) ;
#19633=CARTESIAN_POINT ( 'NONE',  ( 22.98500000136559862, -2.892927487894331406, 1.570731468192932523 ) ) ;
#19646=CARTESIAN_POINT ( 'NONE',  ( 25.04750000136559507, -3.024605502323851169, 0.3178988483021052969 ) ) ;
#19651=DIRECTION ( 'NONE',  ( 1.000000000000000000, -8.574039729943018344E-17, -0.000000000000000000 ) ) ;
#19659=ORIENTED_EDGE ( 'NONE', *, *, #24827, .F. ) ;
#19663=VERTEX_POINT ( 'NONE', #12061 ) ;
#19666=ORIENTED_EDGE ( 'NONE', *, *, #13751, .T. ) ;
#19671=EDGE_LOOP ( 'NONE', ( #20828, #12434, #17449, #30356 ) ) ;
#19682=EDGE_LOOP ( 'NONE', ( #16079, #432, #2073, #25858 ) ) ;
#19696=CARTESIAN_POINT ( 'NONE',  ( -2.593512329575616979E-16, -3.024842911000663381, -3.993798362933340229 ) ) ;
#19703=EDGE_CURVE ( 'NONE', #6604, #17238, #5003, .T. ) ;
#19715=CARTESIAN_POINT ( 'NONE',  ( 24.79749999999999943, 0.7685399846772009713, -2.594547506269381909 ) ) ;
#19726=AXIS2_PLACEMENT_3D ( 'NONE', #8744, #18950, #29141 ) ;
#19729=CARTESIAN_POINT ( 'NONE',  ( 24.42250000136559507, -0.3178988483021076838, -3.024605502323848949 ) ) ;
#19733=PLANE ( 'NONE',  #2884 ) ;
#19740=VECTOR ( 'NONE', #3753, 1000.000000000000000 ) ;
#19750=ORIENTED_EDGE ( 'NONE', *, *, #25518, .T. ) ;
#19761=ORIENTED_EDGE ( 'NONE', *, *, #19577, .T. ) ;
#19765=CARTESIAN_POINT ( 'NONE',  ( 23.23500000273119070, 2.486304738420679783, -0.2613211581691337604 ) ) ;
#19766=CARTESIAN_POINT ( 'NONE',  ( 25.36000000136559862, 0.9349337715887185984, -3.156283516753368268 ) ) ;
#19775=ADVANCED_FACE ( 'NONE', ( #13674 ), #29079, .F. ) ;
#19781=ORIENTED_EDGE ( 'NONE', *, *, #29608, .F. ) ;
#19787=VECTOR ( 'NONE', #30457, 1000.000000000000000 ) ;
#19793=CARTESIAN_POINT ( 'NONE',  ( 21.73500000136559507, 1.570731468192929858, 2.892927487894329630 ) ) ;
#19799=CARTESIAN_POINT ( 'NONE',  ( 10.00000000000000000, 4.467071865485493731, -1.625881193364652866 ) ) ;
#19801=CARTESIAN_POINT ( 'NONE',  ( 10.00000000000000178, -6.000000000000000000, 7.347880794884119736E-16 ) ) ;
#19802=LINE ( 'NONE', #32520, #3737 ) ;
#19803=CARTESIAN_POINT ( 'NONE',  ( 24.73500000136559507, 1.570731468192929858, 2.892927487894329186 ) ) ;
#19808=CARTESIAN_POINT ( 'NONE',  ( 10.00000000000000000, 0.2499999999999812927, 5.003758587302150396 ) ) ;
#19809=AXIS2_PLACEMENT_3D ( 'NONE', #16444, #6758, #16297 ) ;
#19810=CIRCLE ( 'NONE', #24065, 5.009999999999999787 ) ;
#19818=EDGE_CURVE ( 'NONE', #15750, #29889, #20656, .T. ) ;
#19829=ORIENTED_EDGE ( 'NONE', *, *, #15754, .T. ) ;
#19832=VECTOR ( 'NONE', #16251, 1000.000000000000000 ) ;
#19838=EDGE_CURVE ( 'NONE', #2120, #11002, #2596, .T. ) ;
#19842=CARTESIAN_POINT ( 'NONE',  ( 20.74999999999999645, -1.779113243963176091E-15, 0.000000000000000000 ) ) ;
#19847=AXIS2_PLACEMENT_3D ( 'NONE', #19302, #26995, #4098 ) ;
#19851=AXIS2_PLACEMENT_3D ( 'NONE', #8595, #18811, #29015 ) ;
#19855=DIRECTION ( 'NONE',  ( -1.000000000000000000, 8.574039729943018344E-17, -0.000000000000000000 ) ) ;
#19863=CARTESIAN_POINT ( 'NONE',  ( 24.05656763645044904, 0.8852964313267430718, -2.499999999999998224 ) ) ;
#19870=AXIS2_PLACEMENT_3D ( 'NONE', #2558, #38, #5383 ) ;
#19876=FACE_OUTER_BOUND ( 'NONE', #25325, .T. ) ;
#19880=CIRCLE ( 'NONE', #23608, 5.010000000000000675 ) ;
#19881=VECTOR ( 'NONE', #23445, 1000.000000000000000 ) ;
#19887=VECTOR ( 'NONE', #21653, 1000.000000000000000 ) ;
#19893=FACE_OUTER_BOUND ( 'NONE', #20485, .T. ) ;
#19896=CARTESIAN_POINT ( 'NONE',  ( 21.23499999999999943, 0.2613211581691317065, 2.486304738420681559 ) ) ;
#19897=VECTOR ( 'NONE', #26000, 1000.000000000000000 ) ;
#19907=ORIENTED_EDGE ( 'NONE', *, *, #9971, .F. ) ;
#19910=ORIENTED_EDGE ( 'NONE', *, *, #26957, .F. ) ;
#19919=VECTOR ( 'NONE', #10392, 999.9999999999998863 ) ;
#19920=LINE ( 'NONE', #11885, #19929 ) ;
#19927=ORIENTED_EDGE ( 'NONE', *, *, #16125, .F. ) ;
#19929=VECTOR ( 'NONE', #17545, 1000.000000000000000 ) ;
#19930=DIRECTION ( 'NONE',  ( 1.000000000000000000, -8.574039729943018344E-17, -0.000000000000000000 ) ) ;
#19932=DIRECTION ( 'NONE',  ( 3.623545766764202296E-17, 0.4226182617406974984, 0.9063077870366508249 ) ) ;
#19936=ORIENTED_EDGE ( 'NONE', *, *, #27366, .F. ) ;
#19939=VERTEX_POINT ( 'NONE', #2290 ) ;
#19944=VERTEX_POINT ( 'NONE', #7438 ) ;
#19952=EDGE_CURVE ( 'NONE', #61, #8252, #12783, .T. ) ;
#19954=VERTEX_POINT ( 'NONE', #8112 ) ;
#19956=VECTOR ( 'NONE', #27209, 1000.000000000000000 ) ;
#19957=VECTOR ( 'NONE', #6516, 1000.000000000000114 ) ;
#19958=EDGE_CURVE ( 'NONE', #24212, #26129, #3274, .T. ) ;
#19960=CARTESIAN_POINT ( 'NONE',  ( 23.54750000136559507, 3.024605502323846729, -0.3178988483021056854 ) ) ;
#19977=VECTOR ( 'NONE', #32385, 1000.000000000000000 ) ;
#19980=EDGE_CURVE ( 'NONE', #13791, #10256, #28827, .T. ) ;
#19981=FACE_OUTER_BOUND ( 'NONE', #4094, .T. ) ;
#19984=CARTESIAN_POINT ( 'NONE',  ( 21.61000000136559507, 3.156283516753366047, 0.9349337715887203748 ) ) ;
#19991=DIRECTION ( 'NONE',  ( -8.281886410780491305E-17, -0.9659258262890662028, -0.2588190451025284000 ) ) ;
#19993=CARTESIAN_POINT ( 'NONE',  ( 24.36000000136559507, 0.9349337715887185984, -3.156283516753368268 ) ) ;
#19999=DIRECTION ( 'NONE',  ( 0.000000000000000000, 1.000000000000000000, 0.000000000000000000 ) ) ;
#20015=DIRECTION ( 'NONE',  ( 0.000000000000000000, -0.4226182617407038267, 0.9063077870366479383 ) ) ;
#20016=EDGE_CURVE ( 'NONE', #32756, #14263, #9580, .T. ) ;
#20026=DIRECTION ( 'NONE',  ( 0.000000000000000000, 0.9961946980917449901, 0.08715574274766461904 ) ) ;
#20030=LINE ( 'NONE', #10586, #15081 ) ;
#20034=DIRECTION ( 'NONE',  ( 1.000000000000000000, -8.574039729943018344E-17, -0.000000000000000000 ) ) ;
#20048=ORIENTED_EDGE ( 'NONE', *, *, #28473, .T. ) ;
#20056=ORIENTED_EDGE ( 'NONE', *, *, #18267, .T. ) ;
#20068=CARTESIAN_POINT ( 'NONE',  ( 25.92250000136559507, 0.3178988483021036315, 3.024605502323848949 ) ) ;
#20071=VERTEX_POINT ( 'NONE', #24310 ) ;
#20075=LINE ( 'NONE', #15357, #28895 ) ;
#20076=VERTEX_POINT ( 'NONE', #27310 ) ;
#20081=CYLINDRICAL_SURFACE ( 'NONE', #18678, 5.010000000000000675 ) ;
#20083=CARTESIAN_POINT ( 'NONE',  ( -4.262285728429963137E-16, -4.971152295393305387, 0.6226916219171877431 ) ) ;
#20106=LINE ( 'NONE', #7535, #30592 ) ;
#20108=CARTESIAN_POINT ( 'NONE',  ( 22.50111451137534502, -3.256483526998273983E-15, 2.499999999999998668 ) ) ;
#20110=DIRECTION ( 'NONE',  ( 8.281886410780524585E-17, 0.9659258262890700886, -0.2588190451025141336 ) ) ;
#20117=CARTESIAN_POINT ( 'NONE',  ( 9.999999999999998224, -4.681538312723523276, 0.8254815157535098091 ) ) ;
#20118=CARTESIAN_POINT ( 'NONE',  ( 23.92250000136559507, -1.913930629741527500, 2.363507492473149618 ) ) ;
#20122=EDGE_LOOP ( 'NONE', ( #27143, #21363, #21350, #5665 ) ) ;
#20136=DIRECTION ( 'NONE',  ( -1.000000000000000000, 8.574039729943019576E-17, 0.000000000000000000 ) ) ;
#20151=DIRECTION ( 'NONE',  ( 0.000000000000000000, 1.000000000000000000, 0.000000000000000000 ) ) ;
#20154=DIRECTION ( 'NONE',  ( 0.000000000000000000, 1.000000000000000000, 0.000000000000000000 ) ) ;
#20171=ORIENTED_EDGE ( 'NONE', *, *, #9066, .F. ) ;
#20173=ORIENTED_EDGE ( 'NONE', *, *, #30148, .T. ) ;
#20189=CARTESIAN_POINT ( 'NONE',  ( 10.00000000000000000, 3.055657119358849094, -3.641590349731898879 ) ) ;
#20193=EDGE_LOOP ( 'NONE', ( #2582, #20441, #6986, #33008 ) ) ;
#20198=CARTESIAN_POINT ( 'NONE',  ( 23.11000000136559507, -2.892927487894331406, 1.570731468192932301 ) ) ;
#20203=VERTEX_POINT ( 'NONE', #2743 ) ;
#20214=ORIENTED_EDGE ( 'NONE', *, *, #3314, .F. ) ;
#20217=CARTESIAN_POINT ( 'NONE',  ( 22.61000000136559507, 2.892927487894327410, -1.570731468192931635 ) ) ;
#20218=ADVANCED_FACE ( 'NONE', ( #28294 ), #12433, .T. ) ;
#20221=ORIENTED_EDGE ( 'NONE', *, *, #20577, .T. ) ;
#20226=EDGE_LOOP ( 'NONE', ( #19750, #8960, #7695, #5119 ) ) ;
#20232=CARTESIAN_POINT ( 'NONE',  ( 22.36000000136559507, -1.570731468192933633, -2.892927487894330962 ) ) ;
#20240=ADVANCED_FACE ( 'NONE', ( #19981 ), #2076, .F. ) ;
#20253=FACE_OUTER_BOUND ( 'NONE', #29794, .T. ) ;
#20254=EDGE_CURVE ( 'NONE', #20076, #30689, #12249, .T. ) ;
#20257=CARTESIAN_POINT ( 'NONE',  ( 10.52034268205830614, 3.024842911000689583, 3.993798362933319357 ) ) ;
#20267=CARTESIAN_POINT ( 'NONE',  ( 23.17250000273119070, 2.378061970571979433, -1.291182301015470602 ) ) ;
#20277=ORIENTED_EDGE ( 'NONE', *, *, #25084, .T. ) ;
#20279=CARTESIAN_POINT ( 'NONE',  ( 25.67806763263881109, 1.420656155051234659, 2.597633682295764412 ) ) ;
#20291=CARTESIAN_POINT ( 'NONE',  ( 25.75999999999999801, -2.208672634433321348E-15, 0.000000000000000000 ) ) ;
#20293=CIRCLE ( 'NONE', #30440, 5.010000000000000675 ) ;
#20299=CARTESIAN_POINT ( 'NONE',  ( 3.830085165118329002E-16, 4.467071865485494619, -1.625881193364653088 ) ) ;
#20300=LINE ( 'NONE', #29558, #7541 ) ;
#20308=EDGE_CURVE ( 'NONE', #19305, #9887, #21360, .T. ) ;
#20336=ORIENTED_EDGE ( 'NONE', *, *, #6249, .T. ) ;
#20341=FACE_OUTER_BOUND ( 'NONE', #20226, .T. ) ;
#20351=CIRCLE ( 'NONE', #588, 5.009999999999999787 ) ;
#20360=CARTESIAN_POINT ( 'NONE',  ( 22.86000000136559507, 1.570731468192929858, 2.892927487894329186 ) ) ;
#20365=ORIENTED_EDGE ( 'NONE', *, *, #17508, .F. ) ;
#20367=VECTOR ( 'NONE', #3100, 1000.000000000000114 ) ;
#20378=CARTESIAN_POINT ( 'NONE',  ( 10.00000000000000000, 2.376879293651063652, 4.116875700062091248 ) ) ;
#20379=CARTESIAN_POINT ( 'NONE',  ( 10.55147673363119054, 4.116875700062082366, 2.376879293651078751 ) ) ;
#20380=EDGE_CURVE ( 'NONE', #32842, #25696, #8402, .T. ) ;
#20383=CARTESIAN_POINT ( 'NONE',  ( 22.98500000136559507, -0.9349337715887248157, 3.156283516753367824 ) ) ;
#20385=EDGE_CURVE ( 'NONE', #6820, #31424, #18942, .T. ) ;
#20392=FACE_OUTER_BOUND ( 'NONE', #11026, .T. ) ;
#20403=CARTESIAN_POINT ( 'NONE',  ( 21.92250000136559507, 0.3178988483021036315, 3.024605502323848949 ) ) ;
#20414=AXIS2_PLACEMENT_3D ( 'NONE', #22408, #19930, #7213 ) ;
#20416=CIRCLE ( 'NONE', #17725, 5.010000000000000675 ) ;
#20425=ORIENTED_EDGE ( 'NONE', *, *, #12115, .F. ) ;
#20441=ORIENTED_EDGE ( 'NONE', *, *, #24827, .T. ) ;
#20444=VECTOR ( 'NONE', #1580, 1000.000000000000114 ) ;
#20447=CARTESIAN_POINT ( 'NONE',  ( 23.79750000273118715, -2.594547506269383685, -0.7685399846772043020 ) ) ;
#20465=DIRECTION ( 'NONE',  ( -1.000000000000000000, 8.574039729943022041E-17, -0.000000000000000000 ) ) ;
#20469=VECTOR ( 'NONE', #22516, 1000.000000000000000 ) ;
#20475=DIRECTION ( 'NONE',  ( -1.000000000000000000, 8.574039729943022041E-17, 6.162975822039154730E-33 ) ) ;
#20482=ORIENTED_EDGE ( 'NONE', *, *, #24487, .T. ) ;
#20485=EDGE_LOOP ( 'NONE', ( #14760, #543, #13152, #4907 ) ) ;
#20494=CARTESIAN_POINT ( 'NONE',  ( 10.00000000000000000, -2.718385644597145046, -4.208382051008221936 ) ) ;
#20500=CARTESIAN_POINT ( 'NONE',  ( 10.55147673363118876, -4.116875700062067267, -2.376879293651108060 ) ) ;
#20506=CARTESIAN_POINT ( 'NONE',  ( 10.00000000000000000, 5.003758587302148619, -0.2499999999999991951 ) ) ;
#20516=ORIENTED_EDGE ( 'NONE', *, *, #14443, .F. ) ;
#20518=EDGE_CURVE ( 'NONE', #5453, #15485, #22957, .T. ) ;
#20526=CARTESIAN_POINT ( 'NONE',  ( 3.529825581556955655E-16, 4.116875700062116117, -2.376879293651021019 ) ) ;
#20534=DIRECTION ( 'NONE',  ( 4.917867153433032926E-17, 0.5735764363510501562, -0.8191520442889889120 ) ) ;
#20538=CARTESIAN_POINT ( 'NONE',  ( 24.00111451137534146, -6.623356326098185375E-16, -2.499999999999998224 ) ) ;
#20562=DIRECTION ( 'NONE',  ( -1.000000000000000000, 8.574039729943017111E-17, -0.000000000000000000 ) ) ;
#20564=CARTESIAN_POINT ( 'NONE',  ( 24.29750000136559507, -2.363507492473152283, -1.913930629741525280 ) ) ;
#20567=ORIENTED_EDGE ( 'NONE', *, *, #12809, .F. ) ;
#20568=AXIS2_PLACEMENT_3D ( 'NONE', #11736, #18959, #11577 ) ;
#20574=ORIENTED_EDGE ( 'NONE', *, *, #16464, .T. ) ;
#20577=EDGE_CURVE ( 'NONE', #2638, #21128, #13136, .T. ) ;
#20578=CARTESIAN_POINT ( 'NONE',  ( 10.00000000000000000, -1.745506336992504507E-14, 4.753758587302147731 ) ) ;
#20581=CARTESIAN_POINT ( 'NONE',  ( 10.00000000000000000, 3.055657119358800244, 3.641590349731939735 ) ) ;
#20592=EDGE_LOOP ( 'NONE', ( #12699, #25470, #11630, #12376 ) ) ;
#20609=CARTESIAN_POINT ( 'NONE',  ( 25.61000000136559507, 3.156283516753366047, 0.9349337715887203748 ) ) ;
#20613=CARTESIAN_POINT ( 'NONE',  ( 25.75999999999999801, -5.000000000000005329, 6.123233995736770227E-16 ) ) ;
#20615=CARTESIAN_POINT ( 'NONE',  ( 21.11000000136559152, -3.156283516753370044, -0.9349337715887220401 ) ) ;
#20617=LINE ( 'NONE', #15756, #31629 ) ;
#20651=EDGE_CURVE ( 'NONE', #18222, #3046, #114, .T. ) ;
#20654=CARTESIAN_POINT ( 'NONE',  ( 10.00000000000000000, -0.8254815157535575487, 4.681538312723514395 ) ) ;
#20656=LINE ( 'NONE', #15121, #1581 ) ;
#20657=ADVANCED_FACE ( 'NONE', ( #10116 ), #30884, .F. ) ;
#20661=CARTESIAN_POINT ( 'NONE',  ( 10.00000000000000000, -1.775199859220255486E-14, 4.753758587302147731 ) ) ;
#20671=EDGE_CURVE ( 'NONE', #21342, #16032, #6116, .T. ) ;
#20673=DIRECTION ( 'NONE',  ( 8.574039729943018344E-17, 1.000000000000000000, 0.000000000000000000 ) ) ;
#20696=CARTESIAN_POINT ( 'NONE',  ( 24.04749999999999943, 2.594547506269380133, 0.7685399846772031918 ) ) ;
#20700=ORIENTED_EDGE ( 'NONE', *, *, #25981, .F. ) ;
#20717=ORIENTED_EDGE ( 'NONE', *, *, #2823, .F. ) ;
#20720=CARTESIAN_POINT ( 'NONE',  ( 21.67250000136559507, 3.024605502323846729, -0.3178988483021056854 ) ) ;
#20721=CARTESIAN_POINT ( 'NONE',  ( 7.077711312404307767E-17, 0.8254815157535250192, 4.681538312723519724 ) ) ;
#20723=ORIENTED_EDGE ( 'NONE', *, *, #17824, .F. ) ;
#20725=CARTESIAN_POINT ( 'NONE',  ( 0.000000000000000000, 0.000000000000000000, 0.000000000000000000 ) ) ;
#20728=ORIENTED_EDGE ( 'NONE', *, *, #20254, .T. ) ;
#20730=DIRECTION ( 'NONE',  ( 1.000000000000000000, -8.574039729943018344E-17, -0.000000000000000000 ) ) ;
#20733=CARTESIAN_POINT ( 'NONE',  ( 22.11000000136559507, -2.892927487894331406, 1.570731468192932523 ) ) ;
#20744=CARTESIAN_POINT ( 'NONE',  ( 0.000000000000000000, 0.000000000000000000, 0.000000000000000000 ) ) ;
#20748=VERTEX_POINT ( 'NONE', #19799 ) ;
#20760=DIRECTION ( 'NONE',  ( 0.000000000000000000, 0.5735764363510441610, 0.8191520442889931308 ) ) ;
#20763=LINE ( 'NONE', #25448, #22105 ) ;
#20764=EDGE_CURVE ( 'NONE', #20748, #21430, #11766, .T. ) ;
#20766=CARTESIAN_POINT ( 'NONE',  ( -1.959487840848934744E-16, -2.285372942704986254, 4.458382051008185520 ) ) ;
#20767=CARTESIAN_POINT ( 'NONE',  ( 22.36000000136559152, 0.9349337715887185984, -3.156283516753368268 ) ) ;
#20776=CARTESIAN_POINT ( 'NONE',  ( 10.57125986779756843, 4.971152295393309828, -0.6226916219171529931 ) ) ;
#20784=DIRECTION ( 'NONE',  ( 1.000000000000000000, -0.000000000000000000, -0.000000000000000000 ) ) ;
#20790=EDGE_LOOP ( 'NONE', ( #20056, #15195, #19437, #30662 ) ) ;
#20808=ADVANCED_FACE ( 'NONE', ( #1430 ), #32195, .F. ) ;
#20810=ORIENTED_EDGE ( 'NONE', *, *, #3322, .F. ) ;
#20814=ADVANCED_FACE ( 'NONE', ( #24461 ), #1578, .T. ) ;
#20822=EDGE_LOOP ( 'NONE', ( #15, #22176, #585, #16754 ) ) ;
#20824=VERTEX_POINT ( 'NONE', #27146 ) ;
#20828=ORIENTED_EDGE ( 'NONE', *, *, #22697, .T. ) ;
#20832=LINE ( 'NONE', #21012, #8166 ) ;
#20863=VECTOR ( 'NONE', #31447, 1000.000000000000000 ) ;
#20864=CARTESIAN_POINT ( 'NONE',  ( 10.00000000000000000, 3.641590349731929077, 3.055657119358814011 ) ) ;
#20866=CYLINDRICAL_SURFACE ( 'NONE', #18852, 5.010000000000000675 ) ;
#20872=CARTESIAN_POINT ( 'NONE',  ( 21.23500000136559507, -3.156283516753370044, -0.9349337715887220401 ) ) ;
#20873=CARTESIAN_POINT ( 'NONE',  ( 23.75111450864416440, -1.283275288181523244E-15, -2.499999999999998668 ) ) ;
#20884=DIRECTION ( 'NONE',  ( 8.574039729943018344E-17, 1.000000000000000000, 0.000000000000000000 ) ) ;
#20888=DIRECTION ( 'NONE',  ( 0.000000000000000000, 1.000000000000000000, 0.000000000000000000 ) ) ;
#20896=MECHANICAL_CONTEXT ( 'NONE', #25714, 'mechanical' ) ;
#20900=ORIENTED_EDGE ( 'NONE', *, *, #23365, .F. ) ;
#20913=CARTESIAN_POINT ( 'NONE',  ( 7.077711312404307767E-17, 0.8254815157535250192, 4.681538312723519724 ) ) ;
#20914=( BOUNDED_CURVE ( )  B_SPLINE_CURVE ( 2, ( #29306, #16597, #24300, #11589, #4584 ),
 .UNSPECIFIED., .F., .F. ) 
 B_SPLINE_CURVE_WITH_KNOTS ( ( 3, 2, 3 ),
 ( 0.05000000059124252300, 0.07499999999999999722, 0.09661161918950035565 ),
 .UNSPECIFIED. ) 
 CURVE ( )  GEOMETRIC_REPRESENTATION_ITEM ( )  RATIONAL_B_SPLINE_CURVE ( ( 1.000000000000000000, 0.9238795325112867385, 1.000000000000000000, 0.9341965377642874602, 0.9821626249036858880 ) ) 
 REPRESENTATION_ITEM ( '' )  );
#20929=CARTESIAN_POINT ( 'NONE',  ( 24.67250000273118360, -2.378061970571983430, 1.291182301015471712 ) ) ;
#20938=AXIS2_PLACEMENT_3D ( 'NONE', #21251, #32415, #29733 ) ;
#20947=AXIS2_PLACEMENT_3D ( 'NONE', #12248, #21959, #27489 ) ;
#20952=VERTEX_POINT ( 'NONE', #7770 ) ;
#20967=CARTESIAN_POINT ( 'NONE',  ( 2.921917104085894298E-16, 3.407865132560230492, -3.672404558090004212 ) ) ;
#20983=CARTESIAN_POINT ( 'NONE',  ( 24.67250000136559507, 3.024605502323846729, -0.3178988483021056854 ) ) ;
#20989=VECTOR ( 'NONE', #3868, 1000.000000000000114 ) ;
#21001=CARTESIAN_POINT ( 'NONE',  ( 24.79750000136559507, 0.3178988483021036315, 3.024605502323848949 ) ) ;
#21012=CARTESIAN_POINT ( 'NONE',  ( -4.075891499408641642E-16, -4.753758587302147731, 0.000000000000000000 ) ) ;
#21013=ORIENTED_EDGE ( 'NONE', *, *, #10178, .T. ) ;
#21023=CIRCLE ( 'NONE', #6592, 5.010000000000000675 ) ;
#21027=CARTESIAN_POINT ( 'NONE',  ( 22.92250000273118715, -1.291182301015472600, -2.378061970571982098 ) ) ;
#21033=EDGE_CURVE ( 'NONE', #5334, #18559, #6074, .T. ) ;
#21037=ORIENTED_EDGE ( 'NONE', *, *, #15460, .F. ) ;
#21066=VECTOR ( 'NONE', #19143, 1000.000000000000000 ) ;
#21080=ADVANCED_FACE ( 'NONE', ( #26960 ), #31972, .F. ) ;
#21105=PRODUCT_DEFINITION ( 'UNKNOWN', '', #5017, #457 ) ;
#21107=CARTESIAN_POINT ( 'NONE',  ( 24.17250000273118360, 2.378061970571979433, -1.291182301015470824 ) ) ;
#21108=DIRECTION ( 'NONE',  ( -7.472768010110897478E-18, -0.08715574274765533480, -0.9961946980917457672 ) ) ;
#21119=DIRECTION ( 'NONE',  ( 8.574039729943018344E-17, 1.000000000000000000, 0.000000000000000000 ) ) ;
#21128=VERTEX_POINT ( 'NONE', #16569 ) ;
#21132=ORIENTED_EDGE ( 'NONE', *, *, #19096, .F. ) ;
#21134=DIRECTION ( 'NONE',  ( 1.000000000000000000, -8.574039729943018344E-17, -0.000000000000000000 ) ) ;
#21150=ORIENTED_EDGE ( 'NONE', *, *, #15508, .T. ) ;
#21151=CARTESIAN_POINT ( 'NONE',  ( 22.98500000136559507, -0.9349337715887248157, 3.156283516753367824 ) ) ;
#21152=EDGE_CURVE ( 'NONE', #15187, #16550, #22409, .T. ) ;
#21153=CARTESIAN_POINT ( 'NONE',  ( 25.51240124312818480, -1.336128462440899334, -2.459621423140391894 ) ) ;
#21165=CARTESIAN_POINT ( 'NONE',  ( 25.04750000136559507, -3.024605502323851169, 0.3178988483021052969 ) ) ;
#21175=ORIENTED_EDGE ( 'NONE', *, *, #16698, .T. ) ;
#21191=CYLINDRICAL_SURFACE ( 'NONE', #11387, 2.499999999999997780 ) ;
#21198=EDGE_CURVE ( 'NONE', #3400, #14263, #2204, .T. ) ;
#21200=DIRECTION ( 'NONE',  ( -6.062761635205589313E-17, -0.7071067811865484609, 0.7071067811865465735 ) ) ;
#21203=ADVANCED_FACE ( 'NONE', ( #9718 ), #25438, .T. ) ;
#21205=DIRECTION ( 'NONE',  ( 0.000000000000000000, -0.5735764363510552633, 0.8191520442889853593 ) ) ;
#21212=DIRECTION ( 'NONE',  ( 1.000000000000000000, -8.574039729943018344E-17, -0.000000000000000000 ) ) ;
#21214=EDGE_LOOP ( 'NONE', ( #4244, #3339, #13094, #26647 ) ) ;
#21216=DIRECTION ( 'NONE',  ( 1.000000000000000000, -8.574039729943018344E-17, -0.000000000000000000 ) ) ;
#21217=ADVANCED_FACE ( 'NONE', ( #18070 ), #14884, .T. ) ;
#21218=EDGE_CURVE ( 'NONE', #21729, #26855, #21778, .T. ) ;
#21223=LINE ( 'NONE', #26423, #23623 ) ;
#21225=EDGE_LOOP ( 'NONE', ( #28933, #28992, #9522, #27771 ) ) ;
#21227=EDGE_CURVE ( 'NONE', #12922, #13681, #22918, .T. ) ;
#21234=CARTESIAN_POINT ( 'NONE',  ( 25.75999999999999801, -2.208672634433321348E-15, 0.000000000000000000 ) ) ;
#21237=MANIFOLD_SOLID_BREP ( 'CirPattern1', #8665 ) ;
#21248=EDGE_CURVE ( 'NONE', #5341, #15697, #10210, .T. ) ;
#21251=CARTESIAN_POINT ( 'NONE',  ( 25.75999999999999801, -2.208672634433321348E-15, 0.000000000000000000 ) ) ;
#21255=CARTESIAN_POINT ( 'NONE',  ( 25.75999999999999801, -2.208672634433321348E-15, 0.000000000000000000 ) ) ;
#21275=LINE ( 'NONE', #8259, #9155 ) ;
#21278=ORIENTED_EDGE ( 'NONE', *, *, #3322, .T. ) ;
#21285=EDGE_CURVE ( 'NONE', #6857, #7133, #10044, .T. ) ;
#21287=DIRECTION ( 'NONE',  ( -2.219124775574902609E-17, -0.2588190451025176309, -0.9659258262890692004 ) ) ;
#21295=EDGE_LOOP ( 'NONE', ( #20336, #7764, #17104, #7583, #15813, #32806, #30183, #9554, #14808, #18666, #12915, #8222, #2535, #13731, #5593, #13249, #12623, #857, #23998, #30948, #6555, #28998, #18411, #25750, #16678, #16284, #11265, #22179, #15274, #8344, #22909, #23398, #16882, #9558, #29070, #9579, #1088, #19159, #25067, #6394, #27456, #29637, #28650, #10203, #13755, #1218, #10670, #21942, #16850, #26425, #3714, #32406, #19936, #6845, #15078, #20567, #15267, #22680, #9267, #25610, #20574, #356, #24025, #27022, #1041, #4227, #6634, #15537, #28577, #31181, #7435, #22689, #17944, #9699, #1915, #18194, #746, #11718, #28950, #16294, #17593, #27234, #25722, #11159, #23184, #8688, #6897, #31426, #7803, #12644, #1927, #20171, #3219, #32507, #28203, #4324, #12631, #32149, #26413, #31778, #3279, #32506, #18356, #5203, #29989, #20277, #13192, #5123 ) ) ;
#21298=ORIENTED_EDGE ( 'NONE', *, *, #20518, .F. ) ;
#21316=CYLINDRICAL_SURFACE ( 'NONE', #16227, 5.010000000000000675 ) ;
#21323=CYLINDRICAL_SURFACE ( 'NONE', #25681, 5.010000000000000675 ) ;
#21325=DIRECTION ( 'NONE',  ( 0.000000000000000000, 0.5735764363510496011, -0.8191520442889893561 ) ) ;
#21328=DIRECTION ( 'NONE',  ( 3.623545766764302137E-17, 0.4226182617407097108, -0.9063077870366451627 ) ) ;
#21330=DIRECTION ( 'NONE',  ( 0.000000000000000000, 1.000000000000000000, 0.000000000000000000 ) ) ;
#21342=VERTEX_POINT ( 'NONE', #13207 ) ;
#21350=ORIENTED_EDGE ( 'NONE', *, *, #27945, .F. ) ;
#21360=CIRCLE ( 'NONE', #24015, 2.499999999999996891 ) ;
#21363=ORIENTED_EDGE ( 'NONE', *, *, #16125, .T. ) ;
#21371=EDGE_LOOP ( 'NONE', ( #5059, #19011, #7693, #6597 ) ) ;
#21386=AXIS2_PLACEMENT_3D ( 'NONE', #11811, #27533, #22018 ) ;
#21406=CARTESIAN_POINT ( 'NONE',  ( 21.04750000136559507, -3.024605502323851169, 0.3178988483021052969 ) ) ;
#21412=CARTESIAN_POINT ( 'NONE',  ( 20.98500000273118715, -0.2613211581691358698, -2.486304738420681559 ) ) ;
#21424=DIRECTION ( 'NONE',  ( -1.000000000000000000, 8.574039729943017111E-17, -0.000000000000000000 ) ) ;
#21425=LINE ( 'NONE', #24081, #19832 ) ;
#21427=VECTOR ( 'NONE', #32338, 1000.000000000000000 ) ;
#21430=VERTEX_POINT ( 'NONE', #9003 ) ;
#21435=DIRECTION ( 'NONE',  ( -1.000000000000000000, 8.574039729943018344E-17, -0.000000000000000000 ) ) ;
#21441=AXIS2_PLACEMENT_3D ( 'NONE', #3606, #26818, #23663 ) ;
#21444=DIRECTION ( 'NONE',  ( 8.281886410780507329E-17, 0.9659258262890679791, 0.2588190451025216277 ) ) ;
#21445=DIRECTION ( 'NONE',  ( 0.000000000000000000, 1.000000000000000000, 0.000000000000000000 ) ) ;
#21455=EDGE_CURVE ( 'NONE', #22729, #28583, #28301, .T. ) ;
#21460=LINE ( 'NONE', #31677, #4958 ) ;
#21464=CARTESIAN_POINT ( 'NONE',  ( 25.00111451137534146, -4.139597703811366476E-17, -2.499999999999998668 ) ) ;
#21469=CARTESIAN_POINT ( 'NONE',  ( 25.40183372063117417, -2.672122287336369251, 0.04926763101708898224 ) ) ;
#21472=DIRECTION ( 'NONE',  ( 0.000000000000000000, 0.08715574274765461316, 0.9961946980917457672 ) ) ;
#21475=VECTOR ( 'NONE', #31958, 1000.000000000000114 ) ;
#21483=CARTESIAN_POINT ( 'NONE',  ( 25.75999999999999446, 1.024942698525265428, 2.863353032229740691 ) ) ;
#21493=VECTOR ( 'NONE', #22200, 1000.000000000000114 ) ;
#21494=CARTESIAN_POINT ( 'NONE',  ( 21.99290772595112387, -0.1310194482076041944, -2.499999999999998224 ) ) ;
#21505=VECTOR ( 'NONE', #15737, 999.9999999999998863 ) ;
#21529=PLANE ( 'NONE',  #24030 ) ;
#21533=( BOUNDED_SURFACE ( )  B_SPLINE_SURFACE ( 1, 2, ( 
 ( #31605, #2898, #366, #16221, #23898, #3196, #693, #10884, #29101, #23407, #512, #32287, #29251, #12034, #9170, #6335, #32438, #1666, #9348, #29411, #17020, #14337, #11861, #19715, #16524, #26735, #4170, #24543, #19402, #27226, #22070, #19558, #29914, #3853, #14027, #29755, #6835, #29600, #21576, #6683, #16872, #4023, #21881, #16711, #4341, #24238, #27068, #1856, #26918, #6507, #1356, #14520, #24732, #22229, #9500, #16373, #11375, #26582, #3683, #31782, #13843, #24051, #32097, #1176, #11530, #8853, #9001, #19061, #14190, #21726, #31936, #19217, #24388, #1505, #11683, #17526, #32596, #27416, #17692, #25230, #19896 ),
 ( #20068, #17209, #23046, #4522, #22380, #12180, #30111, #30264, #32937, #30601, #14696, #12678, #15350, #10353, #7684, #22563, #9668, #14843, #22882, #168, #12526, #24895, #5020, #27906, #25555, #15198, #20564, #9856, #6997, #27573, #7187, #7335, #2160, #25042, #28075, #27720, #2007, #17380, #4673, #12829, #17882, #12344, #33084, #10162, #22733, #10007, #2660, #20383, #32778, #25400, #4828, #15009, #2351, #20217, #30413, #7491, #2510, #5172, #13174, #28575, #15849, #23864, #28225, #31258, #13501, #10508, #26405, #23532, #20720, #13661, #15994, #23715, #10661, #31086, #5981, #20872, #8176, #7843, #972, #18036, #13024 ) ),
 .UNSPECIFIED., .F., .F., .F. ) 
 B_SPLINE_SURFACE_WITH_KNOTS ( ( 2, 2 ),
 ( 3, 2, 2, 2, 2, 2, 2, 2, 2, 2, 2, 2, 2, 2, 2, 2, 2, 2, 2, 2, 2, 2, 2, 2, 2, 2, 2, 2, 2, 2, 2, 2, 2, 2, 2, 2, 2, 2, 2, 2, 3 ),
 ( 0.000000000000000000, 1.000000000000000000 ),
 ( 0.000000000000000000, 0.02500000000000000139, 0.05000000000000000278, 0.07499999999999999722, 0.1000000000000000056, 0.1250000000000000000, 0.1499999999999999944, 0.1749999999999999889, 0.2000000000000000111, 0.2250000000000000056, 0.2500000000000000000, 0.2750000000000000222, 0.2999999999999999889, 0.3250000000000000111, 0.3499999999999999778, 0.3750000000000000000, 0.4000000000000000222, 0.4249999999999999889, 0.4500000000000000111, 0.4749999999999999778, 0.5000000000000000000, 0.5250000000000000222, 0.5500000000000000444, 0.5749999999999999556, 0.5999999999999999778, 0.6250000000000000000, 0.6500000000000000222, 0.6750000000000000444, 0.6999999999999999556, 0.7249999999999999778, 0.7500000000000000000, 0.7750000000000000222, 0.8000000000000000444, 0.8249999999999999556, 0.8499999999999999778, 0.8750000000000000000, 0.9000000000000000222, 0.9250000000000000444, 0.9499999999999999556, 0.9749999999999999778, 1.000000000000000000 ),
 .UNSPECIFIED. ) 
 GEOMETRIC_REPRESENTATION_ITEM ( )  RATIONAL_B_SPLINE_SURFACE ( (
 ( 1.000000000000000000, 0.9238795325112867385, 1.000000000000000000, 0.9238795325112867385, 1.000000000000000000, 0.9238795325112867385, 1.000000000000000000, 0.9238795325112867385, 1.000000000000000000, 0.9238795325112867385, 1.000000000000000000, 0.9238795325112867385, 1.000000000000000000, 0.9238795325112867385, 1.000000000000000000, 0.9238795325112867385, 1.000000000000000000, 0.9238795325112867385, 1.000000000000000000, 0.9238795325112867385, 1.000000000000000000, 0.9238795325112867385, 1.000000000000000000, 0.9238795325112867385, 1.000000000000000000, 0.9238795325112867385, 1.000000000000000000, 0.9238795325112867385, 1.000000000000000000, 0.9238795325112867385, 1.000000000000000000, 0.9238795325112867385, 1.000000000000000000, 0.9238795325112867385, 1.000000000000000000, 0.9238795325112867385, 1.000000000000000000, 0.9238795325112867385, 1.000000000000000000, 0.9238795325112867385, 1.000000000000000000, 0.9238795325112867385, 1.000000000000000000, 0.9238795325112867385, 1.000000000000000000, 0.9238795325112867385, 1.000000000000000000, 0.9238795325112867385, 1.000000000000000000, 0.9238795325112867385, 1.000000000000000000, 0.9238795325112867385, 1.000000000000000000, 0.9238795325112867385, 1.000000000000000000, 0.9238795325112867385, 1.000000000000000000, 0.9238795325112867385, 1.000000000000000000, 0.9238795325112867385, 1.000000000000000000, 0.9238795325112867385, 1.000000000000000000, 0.9238795325112867385, 1.000000000000000000, 0.9238795325112867385, 1.000000000000000000, 0.9238795325112867385, 1.000000000000000000, 0.9238795325112867385, 1.000000000000000000, 0.9238795325112867385, 1.000000000000000000, 0.9238795325112867385, 1.000000000000000000, 0.9238795325112867385, 1.000000000000000000, 0.9238795325112867385, 1.000000000000000000, 0.9238795325112867385, 1.000000000000000000),
 ( 1.000000000000000000, 0.9238795325112867385, 1.000000000000000000, 0.9238795325112867385, 1.000000000000000000, 0.9238795325112867385, 1.000000000000000000, 0.9238795325112867385, 1.000000000000000000, 0.9238795325112867385, 1.000000000000000000, 0.9238795325112867385, 1.000000000000000000, 0.9238795325112867385, 1.000000000000000000, 0.9238795325112867385, 1.000000000000000000, 0.9238795325112867385, 1.000000000000000000, 0.9238795325112867385, 1.000000000000000000, 0.9238795325112867385, 1.000000000000000000, 0.9238795325112867385, 1.000000000000000000, 0.9238795325112867385, 1.000000000000000000, 0.9238795325112867385, 1.000000000000000000, 0.9238795325112867385, 1.000000000000000000, 0.9238795325112867385, 1.000000000000000000, 0.9238795325112867385, 1.000000000000000000, 0.9238795325112867385, 1.000000000000000000, 0.9238795325112867385, 1.000000000000000000, 0.9238795325112867385, 1.000000000000000000, 0.9238795325112867385, 1.000000000000000000, 0.9238795325112867385, 1.000000000000000000, 0.9238795325112867385, 1.000000000000000000, 0.9238795325112867385, 1.000000000000000000, 0.9238795325112867385, 1.000000000000000000, 0.9238795325112867385, 1.000000000000000000, 0.9238795325112867385, 1.000000000000000000, 0.9238795325112867385, 1.000000000000000000, 0.9238795325112867385, 1.000000000000000000, 0.9238795325112867385, 1.000000000000000000, 0.9238795325112867385, 1.000000000000000000, 0.9238795325112867385, 1.000000000000000000, 0.9238795325112867385, 1.000000000000000000, 0.9238795325112867385, 1.000000000000000000, 0.9238795325112867385, 1.000000000000000000, 0.9238795325112867385, 1.000000000000000000, 0.9238795325112867385, 1.000000000000000000, 0.9238795325112867385, 1.000000000000000000, 0.9238795325112867385, 1.000000000000000000, 0.9238795325112867385, 1.000000000000000000) ) ) 
 REPRESENTATION_ITEM ( '' )  SURFACE ( )  );
#21534=VECTOR ( 'NONE', #991, 1000.000000000000114 ) ;
#21542=ORIENTED_EDGE ( 'NONE', *, *, #8126, .T. ) ;
#21554=DIRECTION ( 'NONE',  ( 8.574039729943018344E-17, 1.000000000000000000, 0.000000000000000000 ) ) ;
#21559=EDGE_CURVE ( 'NONE', #12555, #32100, #6685, .T. ) ;
#21560=DIRECTION ( 'NONE',  ( 2.219124775574988582E-17, 0.2588190451025276784, -0.9659258262890664248 ) ) ;
#21572=ORIENTED_EDGE ( 'NONE', *, *, #11444, .T. ) ;
#21576=CARTESIAN_POINT ( 'NONE',  ( 23.86000000000000298, 1.573300977624590313, -1.942864903642426144 ) ) ;
#21587=CARTESIAN_POINT ( 'NONE',  ( 22.17250000273118715, 2.378061970571979433, -1.291182301015470824 ) ) ;
#21594=CARTESIAN_POINT ( 'NONE',  ( 10.55147673363118876, 2.376879293651121383, -4.116875700062057497 ) ) ;
#21596=ORIENTED_EDGE ( 'NONE', *, *, #1343, .T. ) ;
#21597=AXIS2_PLACEMENT_3D ( 'NONE', #2128, #32745, #25525 ) ;
#21599=ADVANCED_FACE ( 'NONE', ( #6510 ), #16713, .F. ) ;
#21601=DIRECTION ( 'NONE',  ( 0.000000000000000000, 1.000000000000000000, 0.000000000000000000 ) ) ;
#21605=ORIENTED_EDGE ( 'NONE', *, *, #22410, .T. ) ;
#21610=ORIENTED_EDGE ( 'NONE', *, *, #24060, .F. ) ;
#21626=CARTESIAN_POINT ( 'NONE',  ( 9.999999999999998224, -4.681538312723523276, 0.8254815157535098091 ) ) ;
#21627=ORIENTED_EDGE ( 'NONE', *, *, #921, .T. ) ;
#21653=DIRECTION ( 'NONE',  ( 2.219124775575017240E-17, 0.2588190451025310646, -0.9659258262890655367 ) ) ;
#21663=CARTESIAN_POINT ( 'NONE',  ( 2.330754651808344910E-16, 2.718385644597233863, -4.208382051008164204 ) ) ;
#21668=EDGE_CURVE ( 'NONE', #3071, #16406, #13027, .T. ) ;
#21680=EDGE_LOOP ( 'NONE', ( #11759, #1494, #24624, #17403 ) ) ;
#21705=LINE ( 'NONE', #17359, #164 ) ;
#21706=VERTEX_POINT ( 'NONE', #20873 ) ;
#21707=DIRECTION ( 'NONE',  ( -1.000000000000000000, 8.574039729943022041E-17, -3.081487911019577365E-33 ) ) ;
#21710=CARTESIAN_POINT ( 'NONE',  ( 25.75999999999999446, 2.338214438728005273, 1.985154692390100006 ) ) ;
#21712=EDGE_LOOP ( 'NONE', ( #28531, #13837, #31967, #607 ) ) ;
#21724=CARTESIAN_POINT ( 'NONE',  ( 24.35999999999999943, -1.573300977624594976, 1.942864903642425700 ) ) ;
#21726=CARTESIAN_POINT ( 'NONE',  ( 21.92250000000000298, 2.378061970571979433, -1.291182301015470824 ) ) ;
#21729=VERTEX_POINT ( 'NONE', #649 ) ;
#21733=LINE ( 'NONE', #29922, #7593 ) ;
#21741=CARTESIAN_POINT ( 'NONE',  ( 23.04750000273119070, 0.7685399846772009713, -2.594547506269381909 ) ) ;
#21751=CARTESIAN_POINT ( 'NONE',  ( 10.57125986779756843, 1.115095498423374076, -4.884328206559825247 ) ) ;
#21772=FACE_OUTER_BOUND ( 'NONE', #12092, .T. ) ;
#21778=( BOUNDED_CURVE ( )  B_SPLINE_CURVE ( 2, ( #20108, #17564, #22608, #4715, #25594, #217, #2703, #30810, #7878, #28112, #5370 ),
 .UNSPECIFIED., .F., .F. ) 
 B_SPLINE_CURVE_WITH_KNOTS ( ( 3, 2, 2, 2, 2, 3 ),
 ( 0.5966116191895003418, 0.5999999999999999778, 0.6250000000000000000, 0.6500000000000000222, 0.6750000000000000444, 0.6966116191895003196 ),
 .UNSPECIFIED. ) 
 CURVE ( )  GEOMETRIC_REPRESENTATION_ITEM ( )  RATIONAL_B_SPLINE_CURVE ( ( 0.9821626249036858880, 0.9896829947469992783, 1.000000000000000000, 0.9238795325112867385, 1.000000000000000000, 0.9238795325112867385, 1.000000000000000000, 0.9238795325112867385, 1.000000000000000000, 0.9341965377642874602, 0.9821626249036858880 ) ) 
 REPRESENTATION_ITEM ( '' )  );
#21797=CARTESIAN_POINT ( 'NONE',  ( 22.79750000136559862, 0.3178988483021036315, 3.024605502323848949 ) ) ;
#21801=CARTESIAN_POINT ( 'NONE',  ( 10.57125986779756843, 0.8254815157535864145, -4.681538312723508177 ) ) ;
#21813=EDGE_CURVE ( 'NONE', #5237, #16550, #29717, .T. ) ;
#21837=ORIENTED_EDGE ( 'NONE', *, *, #27272, .T. ) ;
#21855=VERTEX_POINT ( 'NONE', #31899 ) ;
#21878=EDGE_CURVE ( 'NONE', #15946, #18549, #17966, .T. ) ;
#21879=CARTESIAN_POINT ( 'NONE',  ( 24.30656763371926132, -0.8852964313267484009, 2.499999999999997780 ) ) ;
#21881=CARTESIAN_POINT ( 'NONE',  ( 23.61000000000000298, -1.942864903642428587, -1.573300977624592756 ) ) ;
#21885=ORIENTED_EDGE ( 'NONE', *, *, #9978, .T. ) ;
#21887=CARTESIAN_POINT ( 'NONE',  ( 10.56870887191539587, -1.476463073999605857, -4.787500056513382063 ) ) ;
#21894=CARTESIAN_POINT ( 'NONE',  ( 20.67250000273118715, -2.378061970571983430, 1.291182301015471712 ) ) ;
#21895=AXIS2_PLACEMENT_3D ( 'NONE', #3157, #21200, #31397 ) ;
#21899=LINE ( 'NONE', #27084, #3307 ) ;
#21907=VERTEX_POINT ( 'NONE', #32405 ) ;
#21922=AXIS2_PLACEMENT_3D ( 'NONE', #5025, #30418, #27579 ) ;
#21925=VECTOR ( 'NONE', #561, 1000.000000000000114 ) ;
#21942=ORIENTED_EDGE ( 'NONE', *, *, #25966, .F. ) ;
#21945=DIRECTION ( 'NONE',  ( 7.472768010110316618E-18, 0.08715574274764853469, 0.9961946980917464334 ) ) ;
#21946=FACE_OUTER_BOUND ( 'NONE', #24795, .T. ) ;
#21954=EDGE_CURVE ( 'NONE', #3611, #18559, #10590, .T. ) ;
#21959=DIRECTION ( 'NONE',  ( 4.917867153432958970E-17, 0.5735764363510412744, 0.8191520442889951292 ) ) ;
#21964=CARTESIAN_POINT ( 'NONE',  ( 20.92250000136559507, -1.913930629741527500, 2.363507492473149618 ) ) ;
#21965=ORIENTED_EDGE ( 'NONE', *, *, #6188, .F. ) ;
#21966=CARTESIAN_POINT ( 'NONE',  ( 10.57125986779756843, 4.681538312723516171, 0.8254815157535410064 ) ) ;
#21970=LINE ( 'NONE', #9892, #6011 ) ;
#21979=CARTESIAN_POINT ( 'NONE',  ( 10.56183597391177464, 0.2500000000000523470, -5.003758587302145955 ) ) ;
#21984=CARTESIAN_POINT ( 'NONE',  ( 0.000000000000000000, 0.000000000000000000, 0.000000000000000000 ) ) ;
#21991=EDGE_CURVE ( 'NONE', #866, #25870, #23155, .T. ) ;
#21995=CARTESIAN_POINT ( 'NONE',  ( 17.75999999999999801, -2.208672634433321348E-15, -2.499999999999996891 ) ) ;
#21997=VECTOR ( 'NONE', #26742, 1000.000000000000114 ) ;
#22004=AXIS2_PLACEMENT_3D ( 'NONE', #2668, #31092, #2357 ) ;
#22010=VERTEX_POINT ( 'NONE', #7924 ) ;
#22012=AXIS2_PLACEMENT_3D ( 'NONE', #9487, #21560, #19046 ) ;
#22018=DIRECTION ( 'NONE',  ( 0.000000000000000000, 0.8191520442889873577, 0.5735764363510524877 ) ) ;
#22025=VERTEX_POINT ( 'NONE', #17162 ) ;
#22033=CARTESIAN_POINT ( 'NONE',  ( 10.56870887191539587, 1.625881193364757449, -4.467071865485455540 ) ) ;
#22037=LINE ( 'NONE', #30075, #25221 ) ;
#22041=ORIENTED_EDGE ( 'NONE', *, *, #7785, .F. ) ;
#22046=CARTESIAN_POINT ( 'NONE',  ( 10.00000000000000000, -1.625881193364669297, -4.467071865485488402 ) ) ;
#22048=DIRECTION ( 'NONE',  ( -1.000000000000000000, 8.574039729943019576E-17, 1.232595164407830946E-32 ) ) ;
#22050=CARTESIAN_POINT ( 'NONE',  ( 25.75999999999999446, 1.024942698525265428, 2.863353032229740691 ) ) ;
#22055=VECTOR ( 'NONE', #15961, 1000.000000000000000 ) ;
#22060=EDGE_CURVE ( 'NONE', #2638, #13159, #16041, .T. ) ;
#22063=LINE ( 'NONE', #14185, #3375 ) ;
#22068=CYLINDRICAL_SURFACE ( 'NONE', #2842, 5.010000000000000675 ) ;
#22070=CARTESIAN_POINT ( 'NONE',  ( 24.35999999999999943, -1.573300977624594976, 1.942864903642425700 ) ) ;
#22077=CARTESIAN_POINT ( 'NONE',  ( 24.25111450864415730, -3.256483526998273983E-15, 2.499999999999998668 ) ) ;
#22079=ORIENTED_EDGE ( 'NONE', *, *, #28473, .F. ) ;
#22082=AXIS2_PLACEMENT_3D ( 'NONE', #27653, #27325, #1768 ) ;
#22089=CARTESIAN_POINT ( 'NONE',  ( 25.17250000136559507, -3.024605502323851169, 0.3178988483021052969 ) ) ;
#22094=EDGE_CURVE ( 'NONE', #20952, #25185, #10752, .T. ) ;
#22105=VECTOR ( 'NONE', #32984, 1000.000000000000114 ) ;
#22108=ORIENTED_EDGE ( 'NONE', *, *, #14889, .F. ) ;
#22116=CARTESIAN_POINT ( 'NONE',  ( 25.76000000000000512, 2.749440278475487442, 1.299952413566024756 ) ) ;
#22119=CARTESIAN_POINT ( 'NONE',  ( 22.73500000000000298, -0.2613211581691358698, -2.486304738420681559 ) ) ;
#22122=CARTESIAN_POINT ( 'NONE',  ( 0.000000000000000000, 0.000000000000000000, 0.000000000000000000 ) ) ;
#22126=CARTESIAN_POINT ( 'NONE',  ( 23.49290772595113097, 0.1310194482076003919, 2.499999999999998668 ) ) ;
#22127=CARTESIAN_POINT ( 'NONE',  ( 24.11000000136559862, -3.156283516753370044, -0.9349337715887220401 ) ) ;
#22147=ORIENTED_EDGE ( 'NONE', *, *, #14296, .T. ) ;
#22149=CARTESIAN_POINT ( 'NONE',  ( 20.79750000136559507, 0.3178988483021036315, 3.024605502323848949 ) ) ;
#22150=ORIENTED_EDGE ( 'NONE', *, *, #16680, .T. ) ;
#22159=CARTESIAN_POINT ( 'NONE',  ( 24.61000000136559862, 3.156283516753366047, 0.9349337715887203748 ) ) ;
#22166=LINE ( 'NONE', #24473, #16589 ) ;
#22175=CARTESIAN_POINT ( 'NONE',  ( 3.122314033877900197E-16, 3.641590349731971710, -3.055657119358763829 ) ) ;
#22176=ORIENTED_EDGE ( 'NONE', *, *, #5664, .T. ) ;
#22179=ORIENTED_EDGE ( 'NONE', *, *, #8134, .T. ) ;
#22182=PLANE ( 'NONE',  #15501 ) ;
#22185=( BOUNDED_CURVE ( )  B_SPLINE_CURVE ( 2, ( #3140, #26036, #13297, #21027, #31533, #26377, #23837, #13635, #28366, #15672, #31235 ),
 .UNSPECIFIED., .F., .F. ) 
 B_SPLINE_CURVE_WITH_KNOTS ( ( 3, 2, 2, 2, 2, 3 ),
 ( 0.4966116191895003640, 0.5000000000000000000, 0.5250000000000000222, 0.5500000000000000444, 0.5749999999999999556, 0.5966116191895003418 ),
 .UNSPECIFIED. ) 
 CURVE ( )  GEOMETRIC_REPRESENTATION_ITEM ( )  RATIONAL_B_SPLINE_CURVE ( ( 0.9821626249036858880, 0.9896829947469992783, 1.000000000000000000, 0.9238795325112867385, 1.000000000000000000, 0.9238795325112867385, 1.000000000000000000, 0.9238795325112867385, 1.000000000000000000, 0.9341965377642874602, 0.9821626249036858880 ) ) 
 REPRESENTATION_ITEM ( '' )  );
#22192=DIRECTION ( 'NONE',  ( 0.000000000000000000, 0.4226182617406914477, 0.9063077870366536004 ) ) ;
#22199=CARTESIAN_POINT ( 'NONE',  ( 25.75999999999999801, -1.838216977691246972E-15, 3.024999999999999911 ) ) ;
#22200=DIRECTION ( 'NONE',  ( -4.917867153432939248E-17, -0.5735764363510388320, -0.8191520442889969056 ) ) ;
#22205=FACE_OUTER_BOUND ( 'NONE', #17479, .T. ) ;
#22211=CARTESIAN_POINT ( 'NONE',  ( -3.529825581556913254E-16, -4.116875700062066379, -2.376879293651108060 ) ) ;
#22224=DIRECTION ( 'NONE',  ( 1.000000000000000000, -0.000000000000000000, -0.000000000000000000 ) ) ;
#22229=CARTESIAN_POINT ( 'NONE',  ( 22.92250000000000298, 2.378061970571979433, -1.291182301015470824 ) ) ;
#22243=LINE ( 'NONE', #27082, #31241 ) ;
#22245=CARTESIAN_POINT ( 'NONE',  ( 24.79750000136559507, 2.363507492473148286, 1.913930629741525058 ) ) ;
#22248=CARTESIAN_POINT ( 'NONE',  ( 25.75999999999999801, -2.208672634433321348E-15, 0.000000000000000000 ) ) ;
#22254=EDGE_CURVE ( 'NONE', #25766, #8558, #15893, .T. ) ;
#22260=CARTESIAN_POINT ( 'NONE',  ( 10.00000000000000000, 1.115095498423308129, 4.884328206559840346 ) ) ;
#22280=CARTESIAN_POINT ( 'NONE',  ( 25.79750000136559507, 0.3178988483021036315, 3.024605502323848949 ) ) ;
#22289=EDGE_CURVE ( 'NONE', #9958, #28295, #11200, .T. ) ;
#22295=VERTEX_POINT ( 'NONE', #3206 ) ;
#22302=CARTESIAN_POINT ( 'NONE',  ( 22.61000000136559507, 3.156283516753366047, 0.9349337715887203748 ) ) ;
#22310=CARTESIAN_POINT ( 'NONE',  ( 22.48500000136559507, 2.892927487894327410, -1.570731468192931635 ) ) ;
#22317=DIRECTION ( 'NONE',  ( 1.000000000000000000, -8.574039729943018344E-17, -0.000000000000000000 ) ) ;
#22334=CARTESIAN_POINT ( 'NONE',  ( -7.077711312404582636E-17, -0.8254815157535566605, 4.681538312723514395 ) ) ;
#22336=EDGE_CURVE ( 'NONE', #14852, #17282, #17652, .T. ) ;
#22342=ADVANCED_FACE ( 'NONE', ( #704 ), #16381, .F. ) ;
#22358=CARTESIAN_POINT ( 'NONE',  ( 20.55656763645045260, -0.8852964313267484009, 2.499999999999997780 ) ) ;
#22361=CARTESIAN_POINT ( 'NONE',  ( 24.92250000136559507, 0.3178988483021036315, 3.024605502323848949 ) ) ;
#22368=ORIENTED_EDGE ( 'NONE', *, *, #20764, .T. ) ;
#22371=EDGE_CURVE ( 'NONE', #5198, #16296, #11384, .T. ) ;
#22376=CARTESIAN_POINT ( 'NONE',  ( 25.56220348721820201, -1.341958225229829886E-11, -2.827203487218203914 ) ) ;
#22380=CARTESIAN_POINT ( 'NONE',  ( 25.67250000136559507, 3.024605502323846729, -0.3178988483021056854 ) ) ;
#22395=CARTESIAN_POINT ( 'NONE',  ( 25.67250000136559507, 3.024605502323846729, -0.3178988483021056854 ) ) ;
#22408=CARTESIAN_POINT ( 'NONE',  ( 25.75999999999999801, -2.208672634433321348E-15, 0.000000000000000000 ) ) ;
#22409=B_SPLINE_CURVE_WITH_KNOTS ( 'NONE', 3,
 ( #22116, #32329, #29798, #29287 ),
 .UNSPECIFIED., .F., .F.,
 ( 4, 4 ),
 ( 1.353369231834851200E-16, 0.0001748182243391414533 ),
 .UNSPECIFIED. ) ;
#22410=EDGE_CURVE ( 'NONE', #13368, #3046, #1867, .T. ) ;
#22420=EDGE_CURVE ( 'NONE', #9958, #5198, #11873, .T. ) ;
#22421=EDGE_LOOP ( 'NONE', ( #10035, #9766, #30365, #23404 ) ) ;
#22424=ORIENTED_EDGE ( 'NONE', *, *, #21152, .T. ) ;
#22430=ORIENTED_EDGE ( 'NONE', *, *, #13399, .T. ) ;
#22431=CYLINDRICAL_SURFACE ( 'NONE', #13544, 5.010000000000000675 ) ;
#22435=CARTESIAN_POINT ( 'NONE',  ( 23.00111451137534502, -1.283275288181523244E-15, -2.499999999999998668 ) ) ;
#22436=CARTESIAN_POINT ( 'NONE',  ( 23.79750000136559507, 0.3178988483021036315, 3.024605502323848949 ) ) ;
#22443=LINE ( 'NONE', #4732, #3366 ) ;
#22453=FACE_OUTER_BOUND ( 'NONE', #8352, .T. ) ;
#22463=CARTESIAN_POINT ( 'NONE',  ( 23.42250000136559862, 1.913930629741522838, -2.363507492473150062 ) ) ;
#22472=CARTESIAN_POINT ( 'NONE',  ( 25.11000000136559507, -3.156283516753370044, -0.9349337715887220401 ) ) ;
#22480=AXIS2_PLACEMENT_3D ( 'NONE', #28343, #3609, #26996 ) ;
#22485=CARTESIAN_POINT ( 'NONE',  ( 10.00000000000000000, -4.787500056513357194, -1.476463073999686459 ) ) ;
#22491=ORIENTED_EDGE ( 'NONE', *, *, #2022, .F. ) ;
#22497=ORIENTED_EDGE ( 'NONE', *, *, #14657, .F. ) ;
#22506=VECTOR ( 'NONE', #17615, 1000.000000000000000 ) ;
#22516=DIRECTION ( 'NONE',  ( 4.917867153432985471E-17, 0.5735764363510441610, 0.8191520442889931308 ) ) ;
#22517=VECTOR ( 'NONE', #21424, 1000.000000000000000 ) ;
#22526=CARTESIAN_POINT ( 'NONE',  ( -4.013969549054187630E-16, -4.681538312723522388, 0.8254815157535098091 ) ) ;
#22532=VECTOR ( 'NONE', #29043, 1000.000000000000000 ) ;
#22534=VERTEX_POINT ( 'NONE', #27026 ) ;
#22537=CIRCLE ( 'NONE', #25737, 5.010000000000000675 ) ;
#22561=CARTESIAN_POINT ( 'NONE',  ( -3.529825581556942343E-16, -4.116875700062099241, 2.376879293651050329 ) ) ;
#22563=CARTESIAN_POINT ( 'NONE',  ( 24.98500000136559507, -0.9349337715887248157, 3.156283516753367824 ) ) ;
#22572=DIRECTION ( 'NONE',  ( 0.000000000000000000, -0.9063077870366467170, -0.4226182617407064912 ) ) ;
#22579=DIRECTION ( 'NONE',  ( 0.000000000000000000, 1.000000000000000000, 0.000000000000000000 ) ) ;
#22587=CARTESIAN_POINT ( 'NONE',  ( 24.98499999999999943, 2.486304738420679783, -0.2613211581691337604 ) ) ;
#22588=VECTOR ( 'NONE', #720, 1000.000000000000000 ) ;
#22599=ORIENTED_EDGE ( 'NONE', *, *, #1843, .F. ) ;
#22605=ORIENTED_EDGE ( 'NONE', *, *, #4072, .F. ) ;
#22608=CARTESIAN_POINT ( 'NONE',  ( 22.48500000273118715, 0.2613211581691317065, 2.486304738420681559 ) ) ;
#22618=VERTEX_POINT ( 'NONE', #9613 ) ;
#22619=LINE ( 'NONE', #32157, #18365 ) ;
#22623=FACE_OUTER_BOUND ( 'NONE', #19177, .T. ) ;
#22624=CARTESIAN_POINT ( 'NONE',  ( 24.04750000136559507, -3.024605502323851169, 0.3178988483021052969 ) ) ;
#22630=CARTESIAN_POINT ( 'NONE',  ( -1.444447458290426890E-30, -1.659765939693074585E-14, 4.753758587302147731 ) ) ;
#22631=ADVANCED_FACE ( 'NONE', ( #19514 ), #22182, .F. ) ;
#22643=PLANE ( 'NONE',  #3321 ) ;
#22653=DIRECTION ( 'NONE',  ( -1.000000000000000000, 8.574039729943018344E-17, -0.000000000000000000 ) ) ;
#22659=CARTESIAN_POINT ( 'NONE',  ( -3.122314033877883927E-16, -3.641590349731949505, 3.055657119358789142 ) ) ;
#22668=ADVANCED_FACE ( 'NONE', ( #20392 ), #2167, .F. ) ;
#22672=CARTESIAN_POINT ( 'NONE',  ( 20.48500000273118715, 0.2613211581691317065, 2.486304738420681559 ) ) ;
#22678=LINE ( 'NONE', #15135, #9251 ) ;
#22680=ORIENTED_EDGE ( 'NONE', *, *, #12830, .T. ) ;
#22689=ORIENTED_EDGE ( 'NONE', *, *, #31794, .F. ) ;
#22697=EDGE_CURVE ( 'NONE', #17091, #4235, #20075, .T. ) ;
#22699=DIRECTION ( 'NONE',  ( -4.917867153432941097E-17, -0.5735764363510392760, -0.8191520442889965725 ) ) ;
#22700=EDGE_LOOP ( 'NONE', ( #11846, #25893, #16063, #19659 ) ) ;
#22705=EDGE_CURVE ( 'NONE', #22534, #14366, #25203, .T. ) ;
#22711=ORIENTED_EDGE ( 'NONE', *, *, #19200, .F. ) ;
#22715=CARTESIAN_POINT ( 'NONE',  ( 25.29750000136559507, -2.363507492473152283, -1.913930629741525280 ) ) ;
#22722=ORIENTED_EDGE ( 'NONE', *, *, #25340, .F. ) ;
#22726=CARTESIAN_POINT ( 'NONE',  ( 10.55147673363119232, -2.718385644597145046, -4.208382051008221048 ) ) ;
#22729=VERTEX_POINT ( 'NONE', #25407 ) ;
#22733=CARTESIAN_POINT ( 'NONE',  ( 23.17250000136559862, -3.024605502323851169, 0.3178988483021052969 ) ) ;
#22738=DIRECTION ( 'NONE',  ( 0.000000000000000000, -0.2588190451025310090, 0.9659258262890655367 ) ) ;
#22740=CARTESIAN_POINT ( 'NONE',  ( 22.17250000000000298, 1.291182301015469047, 2.378061970571981654 ) ) ;
#22746=CARTESIAN_POINT ( 'NONE',  ( 10.52034268205830259, 3.641590349731929077, 3.055657119358814011 ) ) ;
#22753=CARTESIAN_POINT ( 'NONE',  ( 25.23500000000000654, 2.486304733690583912, -0.2613212031729839624 ) ) ;
#22762=VERTEX_POINT ( 'NONE', #7499 ) ;
#22781=CARTESIAN_POINT ( 'NONE',  ( 10.00000000000000178, -8.574039729943018837E-16, 0.000000000000000000 ) ) ;
#22782=LINE ( 'NONE', #2220, #19308 ) ;
#22789=CARTESIAN_POINT ( 'NONE',  ( 2.037945749704312686E-16, 2.376879293651064540, 4.116875700062091248 ) ) ;
#22818=DIRECTION ( 'NONE',  ( -1.000000000000000000, 8.574039729943019576E-17, 0.000000000000000000 ) ) ;
#22826=DIRECTION ( 'NONE',  ( 0.000000000000000000, 1.000000000000000000, 0.000000000000000000 ) ) ;
#22837=EDGE_CURVE ( 'NONE', #9508, #5926, #16065, .T. ) ;
#22862=CARTESIAN_POINT ( 'NONE',  ( 24.11000000136559862, -2.892927487894331406, 1.570731468192932301 ) ) ;
#22879=ADVANCED_FACE ( 'NONE', ( #27041 ), #6653, .F. ) ;
#22882=CARTESIAN_POINT ( 'NONE',  ( 24.79750000136559507, 2.363507492473148286, 1.913930629741525058 ) ) ;
#22895=DIRECTION ( 'NONE',  ( 1.000000000000000000, -8.574039729943018344E-17, -0.000000000000000000 ) ) ;
#22896=CARTESIAN_POINT ( 'NONE',  ( 21.61000000136559507, 2.892927487894327410, -1.570731468192931635 ) ) ;
#22908=LINE ( 'NONE', #7717, #11369 ) ;
#22909=ORIENTED_EDGE ( 'NONE', *, *, #13809, .T. ) ;
#22918=LINE ( 'NONE', #30299, #27800 ) ;
#22925=ORIENTED_EDGE ( 'NONE', *, *, #30321, .T. ) ;
#22928=CARTESIAN_POINT ( 'NONE',  ( 23.92250000273118715, -1.291182301015472378, -2.378061970571982098 ) ) ;
#22932=EDGE_LOOP ( 'NONE', ( #14720, #14176 ) ) ;
#22937=ORIENTED_EDGE ( 'NONE', *, *, #8345, .F. ) ;
#22938=ADVANCED_FACE ( 'NONE', ( #29375 ), #24693, .F. ) ;
#22941=ADVANCED_FACE ( 'NONE', ( #4303 ), #24361, .T. ) ;
#22947=VERTEX_POINT ( 'NONE', #1477 ) ;
#22952=CARTESIAN_POINT ( 'NONE',  ( 3.122314033877864698E-16, 3.641590349731929965, 3.055657119358814011 ) ) ;
#22953=VECTOR ( 'NONE', #28501, 999.9999999999998863 ) ;
#22957=CIRCLE ( 'NONE', #8, 5.010000000000000675 ) ;
#22963=CARTESIAN_POINT ( 'NONE',  ( 2.619932554246601438E-16, 3.055657119358849982, -3.641590349731898879 ) ) ;
#22974=EDGE_LOOP ( 'NONE', ( #21596, #30545, #22079, #24779 ) ) ;
#22977=AXIS2_PLACEMENT_3D ( 'NONE', #14076, #1900, #9540 ) ;
#23002=VECTOR ( 'NONE', #14162, 1000.000000000000000 ) ;
#23003=VECTOR ( 'NONE', #24741, 1000.000000000000000 ) ;
#23009=LINE ( 'NONE', #22526, #23699 ) ;
#23034=EDGE_CURVE ( 'NONE', #10425, #9712, #25682, .T. ) ;
#23046=CARTESIAN_POINT ( 'NONE',  ( 25.79750000136559507, 2.363507492473148286, 1.913930629741525058 ) ) ;
#23059=VECTOR ( 'NONE', #2403, 1000.000000000000114 ) ;
#23067=CARTESIAN_POINT ( 'NONE',  ( 24.17250000136559507, -3.024605502323851169, 0.3178988483021052969 ) ) ;
#23072=DIRECTION ( 'NONE',  ( -6.062761635205574522E-17, -0.7071067811865465735, -0.7071067811865484609 ) ) ;
#23077=VECTOR ( 'NONE', #5994, 1000.000000000000000 ) ;
#23095=DIRECTION ( 'NONE',  ( 1.000000000000000000, -8.574039729943018344E-17, -0.000000000000000000 ) ) ;
#23098=VERTEX_POINT ( 'NONE', #1980 ) ;
#23102=CARTESIAN_POINT ( 'NONE',  ( 24.48500000136559507, 2.892927487894327410, -1.570731468192931635 ) ) ;
#23111=CARTESIAN_POINT ( 'NONE',  ( 21.36000000136559507, 0.9349337715887185984, -3.156283516753368268 ) ) ;
#23113=AXIS2_PLACEMENT_3D ( 'NONE', #26334, #31201, #28516 ) ;
#23135=ORIENTED_EDGE ( 'NONE', *, *, #28515, .T. ) ;
#23143=VECTOR ( 'NONE', #29698, 1000.000000000000000 ) ;
#23144=AXIS2_PLACEMENT_3D ( 'NONE', #19081, #7024, #25257 ) ;
#23149=EDGE_LOOP ( 'NONE', ( #27647, #7830, #13874, #18277 ) ) ;
#23155=LINE ( 'NONE', #28310, #8531 ) ;
#23184=ORIENTED_EDGE ( 'NONE', *, *, #7553, .T. ) ;
#23186=ORIENTED_EDGE ( 'NONE', *, *, #20651, .F. ) ;
#23197=ORIENTED_EDGE ( 'NONE', *, *, #17824, .T. ) ;
#23228=FACE_OUTER_BOUND ( 'NONE', #23518, .T. ) ;
#23231=CARTESIAN_POINT ( 'NONE',  ( 10.00000000000000000, 0.8254815157535241310, 4.681538312723519724 ) ) ;
#23233=ORIENTED_EDGE ( 'NONE', *, *, #7146, .F. ) ;
#23242=CARTESIAN_POINT ( 'NONE',  ( 23.73500000136559507, 3.156283516753366047, 0.9349337715887203748 ) ) ;
#23266=( BOUNDED_CURVE ( )  B_SPLINE_CURVE ( 2, ( #5793, #15970, #8619, #29039, #6130, #20696, #25881, #2997, #26191, #30897, #7970 ),
 .UNSPECIFIED., .F., .T. ) 
 B_SPLINE_CURVE_WITH_KNOTS ( ( 3, 2, 2, 2, 2, 3 ),
 ( 0.3966116191895003862, 0.4000000000000000222, 0.4249999999999999889, 0.4500000000000000111, 0.4749999999999999778, 0.4966116191895003640 ),
 .UNSPECIFIED. ) 
 CURVE ( )  GEOMETRIC_REPRESENTATION_ITEM ( )  RATIONAL_B_SPLINE_CURVE ( ( 0.9821626249036858880, 0.9896829947469992783, 1.000000000000000000, 0.9238795325112867385, 1.000000000000000000, 0.9238795325112867385, 1.000000000000000000, 0.9238795325112867385, 1.000000000000000000, 0.9341965377642874602, 0.9821626249036858880 ) ) 
 REPRESENTATION_ITEM ( '' )  );
#23271=CARTESIAN_POINT ( 'NONE',  ( 21.48500000136559507, 0.9349337715887185984, -3.156283516753368268 ) ) ;
#23279=CARTESIAN_POINT ( 'NONE',  ( 24.98500000273118715, -0.2613211581691358698, -2.486304738420681559 ) ) ;
#23281=EDGE_CURVE ( 'NONE', #32470, #20203, #29520, .T. ) ;
#23293=ORIENTED_EDGE ( 'NONE', *, *, #14280, .T. ) ;
#23294=DIRECTION ( 'NONE',  ( -1.000000000000000000, 8.574039729943017111E-17, -0.000000000000000000 ) ) ;
#23305=ORIENTED_EDGE ( 'NONE', *, *, #6038, .T. ) ;
#23328=EDGE_LOOP ( 'NONE', ( #6064, #26847, #7907, #25808 ) ) ;
#23333=ORIENTED_EDGE ( 'NONE', *, *, #3684, .F. ) ;
#23336=DIRECTION ( 'NONE',  ( -1.000000000000000000, 8.574039729943017111E-17, -0.000000000000000000 ) ) ;
#23338=ORIENTED_EDGE ( 'NONE', *, *, #9971, .T. ) ;
#23344=FACE_OUTER_BOUND ( 'NONE', #26160, .T. ) ;
#23349=CARTESIAN_POINT ( 'NONE',  ( 10.00000000000000000, -1.625881193364728805, 4.467071865485467086 ) ) ;
#23359=ORIENTED_EDGE ( 'NONE', *, *, #27945, .T. ) ;
#23365=EDGE_CURVE ( 'NONE', #17091, #25011, #5964, .T. ) ;
#23369=LINE ( 'NONE', #20864, #17621 ) ;
#23370=DIRECTION ( 'NONE',  ( 0.000000000000000000, 1.000000000000000000, 0.000000000000000000 ) ) ;
#23380=DIRECTION ( 'NONE',  ( 0.000000000000000000, 1.000000000000000000, 0.000000000000000000 ) ) ;
#23381=ORIENTED_EDGE ( 'NONE', *, *, #31853, .F. ) ;
#23386=CARTESIAN_POINT ( 'NONE',  ( 23.61000000136559507, 2.892927487894327410, -1.570731468192931635 ) ) ;
#23388=DIRECTION ( 'NONE',  ( 1.000000000000000000, -8.574039729943018344E-17, -0.000000000000000000 ) ) ;
#23389=DIRECTION ( 'NONE',  ( 8.574039729943018344E-17, 1.000000000000000000, 0.000000000000000000 ) ) ;
#23398=ORIENTED_EDGE ( 'NONE', *, *, #24866, .F. ) ;
#23404=ORIENTED_EDGE ( 'NONE', *, *, #12830, .F. ) ;
#23407=CARTESIAN_POINT ( 'NONE',  ( 25.67249999999999943, -1.291182301015472378, -2.378061970571982098 ) ) ;
#23416=DIRECTION ( 'NONE',  ( 6.062761635205578219E-17, 0.7071067811865465735, 0.7071067811865484609 ) ) ;
#23418=LINE ( 'NONE', #7887, #14094 ) ;
#23421=CARTESIAN_POINT ( 'NONE',  ( 25.29750000273118715, 2.594547506269380133, 0.7685399846772031918 ) ) ;
#23426=ORIENTED_EDGE ( 'NONE', *, *, #873, .T. ) ;
#23431=CARTESIAN_POINT ( 'NONE',  ( 4.285194126261599773E-30, 4.979297819079224069E-14, -4.753758587302147731 ) ) ;
#23437=VERTEX_POINT ( 'NONE', #24979 ) ;
#23444=ORIENTED_EDGE ( 'NONE', *, *, #25289, .T. ) ;
#23445=DIRECTION ( 'NONE',  ( 1.000000000000000000, -0.000000000000000000, -0.000000000000000000 ) ) ;
#23455=EDGE_CURVE ( 'NONE', #19663, #14569, #32375, .T. ) ;
#23462=CIRCLE ( 'NONE', #13822, 5.010000000000000675 ) ;
#23471=CARTESIAN_POINT ( 'NONE',  ( 22.61000000136559507, 2.892927487894327410, -1.570731468192931635 ) ) ;
#23476=ADVANCED_FACE ( 'NONE', ( #30858 ), #272, .F. ) ;
#23486=EDGE_CURVE ( 'NONE', #2105, #18770, #25645, .T. ) ;
#23488=VECTOR ( 'NONE', #31335, 1000.000000000000227 ) ;
#23506=VECTOR ( 'NONE', #26302, 1000.000000000000114 ) ;
#23518=EDGE_LOOP ( 'NONE', ( #26182, #6814 ) ) ;
#23519=CARTESIAN_POINT ( 'NONE',  ( 10.00000000000000178, -1.115095498423344988, 4.884328206559834129 ) ) ;
#23531=LINE ( 'NONE', #3648, #8095 ) ;
#23532=CARTESIAN_POINT ( 'NONE',  ( 21.73500000136559507, 3.156283516753366047, 0.9349337715887203748 ) ) ;
#23541=EDGE_CURVE ( 'NONE', #32276, #22947, #28504, .T. ) ;
#23559=ORIENTED_EDGE ( 'NONE', *, *, #7386, .T. ) ;
#23560=DIRECTION ( 'NONE',  ( 1.000000000000000000, -8.574039729943018344E-17, -0.000000000000000000 ) ) ;
#23565=VECTOR ( 'NONE', #9191, 1000.000000000000114 ) ;
#23566=ORIENTED_EDGE ( 'NONE', *, *, #19952, .F. ) ;
#23568=CONICAL_SURFACE ( 'NONE', #9142, 3.024999999999999911, 0.7853981633974520538 ) ;
#23579=CIRCLE ( 'NONE', #11871, 5.009999999999999787 ) ;
#23581=EDGE_CURVE ( 'NONE', #23867, #30399, #1553, .T. ) ;
#23582=DIRECTION ( 'NONE',  ( 1.000000000000000000, -8.574039729943018344E-17, -0.000000000000000000 ) ) ;
#23589=CARTESIAN_POINT ( 'NONE',  ( 25.04750000273118715, 0.7685399846772009713, -2.594547506269381909 ) ) ;
#23602=LINE ( 'NONE', #20776, #25070 ) ;
#23605=CARTESIAN_POINT ( 'NONE',  ( 0.000000000000000000, 0.000000000000000000, 0.000000000000000000 ) ) ;
#23608=AXIS2_PLACEMENT_3D ( 'NONE', #29670, #2075, #32184 ) ;
#23612=DIRECTION ( 'NONE',  ( 0.000000000000000000, 1.000000000000000000, 0.000000000000000000 ) ) ;
#23620=VECTOR ( 'NONE', #29076, 1000.000000000000000 ) ;
#23623=VECTOR ( 'NONE', #18698, 1000.000000000000000 ) ;
#23644=CARTESIAN_POINT ( 'NONE',  ( 21.79750000136559507, 2.363507492473148286, 1.913930629741525058 ) ) ;
#23647=CARTESIAN_POINT ( 'NONE',  ( 25.34177696560086446, -2.134796180801955323, 1.506068310576387015 ) ) ;
#23653=EDGE_LOOP ( 'NONE', ( #18713, #4700, #11452, #8800 ) ) ;
#23658=ADVANCED_FACE ( 'NONE', ( #11735 ), #14240, .F. ) ;
#23660=CARTESIAN_POINT ( 'NONE',  ( 22.86000000000000298, 1.573300977624590313, -1.942864903642426144 ) ) ;
#23663=DIRECTION ( 'NONE',  ( 8.574039729943018344E-17, 1.000000000000000000, 0.000000000000000000 ) ) ;
#23669=EDGE_CURVE ( 'NONE', #8466, #25541, #13846, .T. ) ;
#23676=VECTOR ( 'NONE', #51, 1000.000000000000114 ) ;
#23684=CARTESIAN_POINT ( 'NONE',  ( 24.00111451137534146, -6.623356326098185375E-16, -2.499999999999998224 ) ) ;
#23685=CARTESIAN_POINT ( 'NONE',  ( 10.55147673363119232, 2.376879293651063652, 4.116875700062091248 ) ) ;
#23691=VERTEX_POINT ( 'NONE', #28988 ) ;
#23699=VECTOR ( 'NONE', #20534, 999.9999999999998863 ) ;
#23705=VECTOR ( 'NONE', #4905, 1000.000000000000000 ) ;
#23708=DIRECTION ( 'NONE',  ( -8.541412920197219815E-17, -0.9961946980917455452, 0.08715574274765799934 ) ) ;
#23714=CARTESIAN_POINT ( 'NONE',  ( -1.265925305626641768E-16, -1.476463073999604969, -4.787500056513382063 ) ) ;
#23715=CARTESIAN_POINT ( 'NONE',  ( 21.48500000136559507, 0.9349337715887185984, -3.156283516753368268 ) ) ;
#23719=CARTESIAN_POINT ( 'NONE',  ( -1.394036994807634510E-16, -1.625881193364727917, 4.467071865485467086 ) ) ;
#23736=ORIENTED_EDGE ( 'NONE', *, *, #13809, .F. ) ;
#23738=ORIENTED_EDGE ( 'NONE', *, *, #18407, .T. ) ;
#23741=EDGE_CURVE ( 'NONE', #23437, #24462, #30310, .T. ) ;
#23760=VERTEX_POINT ( 'NONE', #32985 ) ;
#23762=CARTESIAN_POINT ( 'NONE',  ( 23.42250000273118715, 1.291182301015469047, 2.378061970571981654 ) ) ;
#23763=EDGE_CURVE ( 'NONE', #32887, #5204, #24326, .T. ) ;
#23777=ORIENTED_EDGE ( 'NONE', *, *, #4515, .F. ) ;
#23778=EDGE_CURVE ( 'NONE', #6604, #32678, #15070, .T. ) ;
#23782=EDGE_CURVE ( 'NONE', #26129, #1852, #29808, .T. ) ;
#23797=CARTESIAN_POINT ( 'NONE',  ( 24.50111451137534146, -3.256483526998273983E-15, 2.499999999999998668 ) ) ;
#23806=CARTESIAN_POINT ( 'NONE',  ( 22.04750000136559507, -1.913930629741527500, 2.363507492473149618 ) ) ;
#23808=CARTESIAN_POINT ( 'NONE',  ( 25.48003937004066444, -2.000525074609735832, -1.887699336444768505 ) ) ;
#23813=ORIENTED_EDGE ( 'NONE', *, *, #31797, .T. ) ;
#23816=LINE ( 'NONE', #23962, #13967 ) ;
#23822=ORIENTED_EDGE ( 'NONE', *, *, #3314, .T. ) ;
#23827=LINE ( 'NONE', #31369, #14367 ) ;
#23834=CARTESIAN_POINT ( 'NONE',  ( 10.57125986779756843, 0.8254815157535241310, 4.681538312723519724 ) ) ;
#23836=DIRECTION ( 'NONE',  ( 2.219124775574934040E-17, 0.2588190451025216832, -0.9659258262890680902 ) ) ;
#23837=CARTESIAN_POINT ( 'NONE',  ( 22.73500000273118715, -2.486304738420683780, 0.2613211581691335383 ) ) ;
#23840=EDGE_CURVE ( 'NONE', #22762, #3071, #30163, .T. ) ;
#23841=CARTESIAN_POINT ( 'NONE',  ( 21.42249999999999943, -2.378061970571983430, 1.291182301015471490 ) ) ;
#23855=ADVANCED_FACE ( 'NONE', ( #22623 ), #32832, .F. ) ;
#23863=DIRECTION ( 'NONE',  ( -1.000000000000000000, 8.574039729943022041E-17, 1.232595164407830946E-32 ) ) ;
#23864=CARTESIAN_POINT ( 'NONE',  ( 22.11000000136559507, -2.892927487894331406, 1.570731468192932301 ) ) ;
#23867=VERTEX_POINT ( 'NONE', #20766 ) ;
#23868=CARTESIAN_POINT ( 'NONE',  ( 0.000000000000000000, 0.000000000000000000, 0.000000000000000000 ) ) ;
#23873=CARTESIAN_POINT ( 'NONE',  ( 20.74999999999999645, -6.000000000000003553, 7.347880794884121708E-16 ) ) ;
#23876=CARTESIAN_POINT ( 'NONE',  ( 10.56870887191539587, 4.467071865485493731, -1.625881193364653088 ) ) ;
#23878=CARTESIAN_POINT ( 'NONE',  ( 9.560873106162633529E-17, 1.115095498423374965, -4.884328206559825247 ) ) ;
#23894=ORIENTED_EDGE ( 'NONE', *, *, #10917, .F. ) ;
#23898=CARTESIAN_POINT ( 'NONE',  ( 25.98499999999999943, 2.486304738420679783, -0.2613211581691337604 ) ) ;
#23906=CARTESIAN_POINT ( 'NONE',  ( 21.73500000136559507, 1.570731468192929858, 2.892927487894329186 ) ) ;
#23911=CARTESIAN_POINT ( 'NONE',  ( 21.23500000273118715, 2.486304738420679783, -0.2613211581691337604 ) ) ;
#23916=EDGE_CURVE ( 'NONE', #17640, #26134, #30014, .T. ) ;
#23925=ORIENTED_EDGE ( 'NONE', *, *, #22420, .F. ) ;
#23929=CARTESIAN_POINT ( 'NONE',  ( -1.394036994807583480E-16, -1.625881193364668409, -4.467071865485488402 ) ) ;
#23930=ORIENTED_EDGE ( 'NONE', *, *, #25311, .T. ) ;
#23939=CARTESIAN_POINT ( 'NONE',  ( 10.00000000000000178, -8.574039729943018837E-16, 0.000000000000000000 ) ) ;
#23944=CARTESIAN_POINT ( 'NONE',  ( 24.67250000273118715, -2.378061970571983430, 1.291182301015471490 ) ) ;
#23949=ORIENTED_EDGE ( 'NONE', *, *, #26545, .F. ) ;
#23957=ORIENTED_EDGE ( 'NONE', *, *, #12858, .T. ) ;
#23958=DIRECTION ( 'NONE',  ( 8.541412920197221047E-17, 0.9961946980917458783, -0.08715574274765462703 ) ) ;
#23962=CARTESIAN_POINT ( 'NONE',  ( 2.619932554246560023E-16, 3.055657119358801133, 3.641590349731939735 ) ) ;
#23965=ORIENTED_EDGE ( 'NONE', *, *, #17760, .T. ) ;
#23973=CARTESIAN_POINT ( 'NONE',  ( 21.92250000273118715, -1.291182301015472600, -2.378061970571982098 ) ) ;
#23978=VECTOR ( 'NONE', #7808, 1000.000000000000000 ) ;
#23982=ADVANCED_FACE ( 'NONE', ( #29114 ), #6660, .T. ) ;
#23986=CARTESIAN_POINT ( 'NONE',  ( 21.75111450864415730, -1.283275288181523244E-15, -2.499999999999998668 ) ) ;
#23997=VECTOR ( 'NONE', #6120, 1000.000000000000000 ) ;
#23998=ORIENTED_EDGE ( 'NONE', *, *, #24403, .T. ) ;
#24004=DIRECTION ( 'NONE',  ( 0.000000000000000000, 1.000000000000000000, 0.000000000000000000 ) ) ;
#24008=LINE ( 'NONE', #13804, #30523 ) ;
#24011=ADVANCED_FACE ( 'NONE', ( #18733 ), #13960, .F. ) ;
#24015=AXIS2_PLACEMENT_3D ( 'NONE', #8733, #20784, #16070 ) ;
#24021=PLANE ( 'NONE',  #15133 ) ;
#24025=ORIENTED_EDGE ( 'NONE', *, *, #20671, .F. ) ;
#24030=AXIS2_PLACEMENT_3D ( 'NONE', #4130, #16980, #20026 ) ;
#24033=ORIENTED_EDGE ( 'NONE', *, *, #3666, .F. ) ;
#24039=EDGE_CURVE ( 'NONE', #32678, #30689, #13554, .T. ) ;
#24048=ORIENTED_EDGE ( 'NONE', *, *, #1021, .F. ) ;
#24051=CARTESIAN_POINT ( 'NONE',  ( 22.42250000000000298, -2.378061970571983430, 1.291182301015471712 ) ) ;
#24059=CARTESIAN_POINT ( 'NONE',  ( 21.98500000136559507, -2.892927487894331406, 1.570731468192932301 ) ) ;
#24060=EDGE_CURVE ( 'NONE', #31165, #9839, #14487, .T. ) ;
#24065=AXIS2_PLACEMENT_3D ( 'NONE', #25140, #2440, #15280 ) ;
#24067=CARTESIAN_POINT ( 'NONE',  ( 22.67250000273118715, -2.378061970571983430, 1.291182301015471712 ) ) ;
#24079=DIRECTION ( 'NONE',  ( 0.000000000000000000, 0.7071067811865460184, 0.7071067811865490160 ) ) ;
#24081=CARTESIAN_POINT ( 'NONE',  ( 10.56870887191539587, -1.625881193364728805, 4.467071865485467086 ) ) ;
#24096=CIRCLE ( 'NONE', #4361, 5.009999999999999787 ) ;
#24098=CIRCLE ( 'NONE', #15571, 5.010000000000000675 ) ;
#24116=( BOUNDED_CURVE ( )  B_SPLINE_CURVE ( 2, ( #27247, #30434, #1689, #12369, #22587, #4365, #32801, #14544, #1876 ),
 .UNSPECIFIED., .F., .F. ) 
 B_SPLINE_CURVE_WITH_KNOTS ( ( 3, 2, 2, 2, 3 ),
 ( 0.2000000000000001776, 0.2250000000000001166, 0.2500000000000000555, 0.2750000000000000777, 0.2966116191895003529 ),
 .UNSPECIFIED. ) 
 CURVE ( )  GEOMETRIC_REPRESENTATION_ITEM ( )  RATIONAL_B_SPLINE_CURVE ( ( 0.9999999999999994449, 0.9238795325112872936, 1.000000000000000000, 0.9238795325112867385, 1.000000000000000000, 0.9238795325112867385, 1.000000000000000000, 0.9341965377642874602, 0.9821626249036858880 ) ) 
 REPRESENTATION_ITEM ( '' )  );
#24122=PLANE ( 'NONE',  #18863 ) ;
#24126=AXIS2_PLACEMENT_3D ( 'NONE', #13732, #18599, #10742 ) ;
#24141=CARTESIAN_POINT ( 'NONE',  ( 24.92250000136559507, -1.913930629741527500, 2.363507492473149618 ) ) ;
#24142=ADVANCED_FACE ( 'NONE', ( #27550 ), #4646, .F. ) ;
#24151=CARTESIAN_POINT ( 'NONE',  ( 21.50111451137534146, -3.256483526998273983E-15, 2.499999999999998668 ) ) ;
#24153=VECTOR ( 'NONE', #15426, 1000.000000000000000 ) ;
#24161=CARTESIAN_POINT ( 'NONE',  ( 25.75999999999999801, -2.208672634433321348E-15, -2.499999999999997780 ) ) ;
#24169=VECTOR ( 'NONE', #14169, 1000.000000000000114 ) ;
#24172=ORIENTED_EDGE ( 'NONE', *, *, #32900, .T. ) ;
#24183=ORIENTED_EDGE ( 'NONE', *, *, #19153, .T. ) ;
#24212=VERTEX_POINT ( 'NONE', #3480 ) ;
#24235=EDGE_LOOP ( 'NONE', ( #24575, #11486, #2451, #14597 ) ) ;
#24238=CARTESIAN_POINT ( 'NONE',  ( 23.42249999999999943, -2.378061970571983430, 1.291182301015471712 ) ) ;
#24242=VECTOR ( 'NONE', #2713, 1000.000000000000000 ) ;
#24250=CARTESIAN_POINT ( 'NONE',  ( 23.61000000273119070, -1.573300977624594976, 1.942864903642425700 ) ) ;
#24253=DIRECTION ( 'NONE',  ( 0.000000000000000000, 1.000000000000000000, 0.000000000000000000 ) ) ;
#24256=LINE ( 'NONE', #14209, #16180 ) ;
#24262=AXIS2_PLACEMENT_3D ( 'NONE', #23834, #11124, #21325 ) ;
#24267=DIRECTION ( 'NONE',  ( 0.000000000000000000, 0.000000000000000000, -1.000000000000000000 ) ) ;
#24300=CARTESIAN_POINT ( 'NONE',  ( 25.11000000273118715, 1.573300977624590313, -1.942864903642426144 ) ) ;
#24310=CARTESIAN_POINT ( 'NONE',  ( 3.830085165118310759E-16, 4.467071865485471527, 1.625881193364712596 ) ) ;
#24313=CARTESIAN_POINT ( 'NONE',  ( 24.23500000136559507, -1.570731468192933633, -2.892927487894330962 ) ) ;
#24320=CARTESIAN_POINT ( 'NONE',  ( 2.619932554246560023E-16, 3.055657119358801133, 3.641590349731939735 ) ) ;
#24322=DIRECTION ( 'NONE',  ( 1.000000000000000000, -8.574039729943018344E-17, -0.000000000000000000 ) ) ;
#24326=( BOUNDED_CURVE ( )  B_SPLINE_CURVE ( 2, ( #17574, #22126, #9399, #14745, #10054, #27118, #19765, #20267, #24943, #12228, #22435 ),
 .UNSPECIFIED., .F., .F. ) 
 B_SPLINE_CURVE_WITH_KNOTS ( ( 3, 2, 2, 2, 2, 3 ),
 ( 0.3966116191895003862, 0.4000000000000000222, 0.4249999999999999889, 0.4500000000000000111, 0.4749999999999999778, 0.4966116191895003640 ),
 .UNSPECIFIED. ) 
 CURVE ( )  GEOMETRIC_REPRESENTATION_ITEM ( )  RATIONAL_B_SPLINE_CURVE ( ( 0.9821626249036858880, 0.9896829947469992783, 1.000000000000000000, 0.9238795325112867385, 1.000000000000000000, 0.9238795325112867385, 1.000000000000000000, 0.9238795325112867385, 1.000000000000000000, 0.9341965377642874602, 0.9821626249036858880 ) ) 
 REPRESENTATION_ITEM ( '' )  );
#24327=CARTESIAN_POINT ( 'NONE',  ( 10.00000000000000000, 4.116875700062082366, 2.376879293651078751 ) ) ;
#24329=CARTESIAN_POINT ( 'NONE',  ( 10.55147673363118876, -2.376879293651094294, 4.116875700062075261 ) ) ;
#24330=CARTESIAN_POINT ( 'NONE',  ( 25.75999999999999801, 5.000000000000000000, 0.000000000000000000 ) ) ;
#24332=FACE_OUTER_BOUND ( 'NONE', #7518, .T. ) ;
#24333=DIRECTION ( 'NONE',  ( 0.000000000000000000, 0.000000000000000000, -1.000000000000000000 ) ) ;
#24349=CYLINDRICAL_SURFACE ( 'NONE', #8042, 5.010000000000000675 ) ;
#24356=CARTESIAN_POINT ( 'NONE',  ( 25.65417410921524421, 2.315637413981730841, -1.793282383124906065 ) ) ;
#24361=CYLINDRICAL_SURFACE ( 'NONE', #27822, 6.000000000000000000 ) ;
#24367=CARTESIAN_POINT ( 'NONE',  ( 21.00111451137534146, -1.283275288181523244E-15, -2.499999999999998668 ) ) ;
#24372=EDGE_CURVE ( 'NONE', #26262, #285, #32211, .T. ) ;
#24378=VERTEX_POINT ( 'NONE', #9094 ) ;
#24383=DIRECTION ( 'NONE',  ( 8.281886410780523353E-17, 0.9659258262890698665, -0.2588190451025149663 ) ) ;
#24386=CARTESIAN_POINT ( 'NONE',  ( 25.75999999999999801, -2.208672634433321348E-15, 0.000000000000000000 ) ) ;
#24387=CARTESIAN_POINT ( 'NONE',  ( 10.00000000000000000, -3.641590349731909537, -3.055657119358837992 ) ) ;
#24388=CARTESIAN_POINT ( 'NONE',  ( 21.73499999999999943, -0.2613211581691358698, -2.486304738420681559 ) ) ;
#24394=PLANE ( 'NONE',  #15586 ) ;
#24395=LINE ( 'NONE', #27075, #21997 ) ;
#24400=CARTESIAN_POINT ( 'NONE',  ( 20.73500000273118715, -2.486304738420683780, 0.2613211581691335383 ) ) ;
#24402=CARTESIAN_POINT ( 'NONE',  ( 25.61000000136559507, 2.892927487894327410, -1.570731468192931635 ) ) ;
#24403=EDGE_CURVE ( 'NONE', #3558, #16126, #22537, .T. ) ;
#24406=DIRECTION ( 'NONE',  ( -1.000000000000000000, 8.574039729943018344E-17, -0.000000000000000000 ) ) ;
#24429=EDGE_CURVE ( 'NONE', #31023, #15485, #16962, .T. ) ;
#24443=DIRECTION ( 'NONE',  ( 1.000000000000000000, -8.574039729943018344E-17, -0.000000000000000000 ) ) ;
#24444=DIRECTION ( 'NONE',  ( 1.000000000000000000, -8.574039729943018344E-17, -0.000000000000000000 ) ) ;
#24448=DIRECTION ( 'NONE',  ( 1.000000000000000000, -8.574039729943018344E-17, -0.000000000000000000 ) ) ;
#24457=CARTESIAN_POINT ( 'NONE',  ( 23.29750000136559862, -0.3178988483021076838, -3.024605502323848949 ) ) ;
#24461=FACE_OUTER_BOUND ( 'NONE', #14948, .T. ) ;
#24462=VERTEX_POINT ( 'NONE', #6618 ) ;
#24472=ADVANCED_FACE ( 'NONE', ( #24332 ), #4264, .F. ) ;
#24473=CARTESIAN_POINT ( 'NONE',  ( 9.999999999999998224, -4.681538312723512618, -0.8254815157535732029 ) ) ;
#24474=CYLINDRICAL_SURFACE ( 'NONE', #6506, 5.010000000000000675 ) ;
#24475=CARTESIAN_POINT ( 'NONE',  ( 23.73500000273118715, -2.486304738420683780, 0.2613211581691335383 ) ) ;
#24476=CARTESIAN_POINT ( 'NONE',  ( 21.60999999999999943, -1.942864903642428587, -1.573300977624592756 ) ) ;
#24487=EDGE_CURVE ( 'NONE', #7070, #32887, #15337, .T. ) ;
#24498=LINE ( 'NONE', #9969, #8563 ) ;
#24500=DIRECTION ( 'NONE',  ( -1.000000000000000000, 8.574039729943022041E-17, 1.232595164407830946E-32 ) ) ;
#24511=DIRECTION ( 'NONE',  ( 8.541412920197218582E-17, 0.9961946980917461003, -0.08715574274765119922 ) ) ;
#24513=DIRECTION ( 'NONE',  ( -7.472768010110610900E-18, -0.08715574274765197638, -0.9961946980917461003 ) ) ;
#24524=CARTESIAN_POINT ( 'NONE',  ( 10.00000000000000000, -0.8254815157534942660, -4.681538312723525053 ) ) ;
#24534=VECTOR ( 'NONE', #6938, 1000.000000000000000 ) ;
#24537=CARTESIAN_POINT ( 'NONE',  ( 25.75999999999999801, -2.208672634433321348E-15, 0.000000000000000000 ) ) ;
#24540=PLANE ( 'NONE',  #30059 ) ;
#24543=CARTESIAN_POINT ( 'NONE',  ( 24.54749999999999943, -2.594547506269383685, -0.7685399846772043020 ) ) ;
#24547=CARTESIAN_POINT ( 'NONE',  ( 0.000000000000000000, 0.000000000000000000, 0.000000000000000000 ) ) ;
#24550=CARTESIAN_POINT ( 'NONE',  ( 10.56183597391177464, -4.753758587302148619, 0.000000000000000000 ) ) ;
#24556=VERTEX_POINT ( 'NONE', #22672 ) ;
#24557=DIRECTION ( 'NONE',  ( 1.000000000000000000, -8.574039729943018344E-17, -0.000000000000000000 ) ) ;
#24560=CARTESIAN_POINT ( 'NONE',  ( 10.56183597391177464, -0.2500000000000192624, 5.003758587302147731 ) ) ;
#24564=CYLINDRICAL_SURFACE ( 'NONE', #15668, 5.010000000000000675 ) ;
#24568=ORIENTED_EDGE ( 'NONE', *, *, #24787, .T. ) ;
#24571=AXIS2_PLACEMENT_3D ( 'NONE', #5712, #28453, #25950 ) ;
#24572=DIRECTION ( 'NONE',  ( 1.000000000000000000, -8.574039729943018344E-17, -0.000000000000000000 ) ) ;
#24575=ORIENTED_EDGE ( 'NONE', *, *, #24372, .T. ) ;
#24581=CIRCLE ( 'NONE', #21922, 5.010000000000000675 ) ;
#24586=VECTOR ( 'NONE', #23416, 1000.000000000000114 ) ;
#24599=CARTESIAN_POINT ( 'NONE',  ( 24.92250000136559507, -1.913930629741527500, 2.363507492473149618 ) ) ;
#24607=EDGE_LOOP ( 'NONE', ( #1880, #14752, #1042, #28192 ) ) ;
#24609=AXIS2_PLACEMENT_3D ( 'NONE', #27914, #12352, #22572 ) ;
#24624=ORIENTED_EDGE ( 'NONE', *, *, #13121, .T. ) ;
#24625=CARTESIAN_POINT ( 'NONE',  ( 23.98500000136559507, -2.892927487894331406, 1.570731468192932523 ) ) ;
#24636=CARTESIAN_POINT ( 'NONE',  ( 21.42250000136559507, -0.3178988483021076838, -3.024605502323848949 ) ) ;
#24658=CARTESIAN_POINT ( 'NONE',  ( 25.75999999999999801, -1.902510934646483477E-15, 2.499999999999997780 ) ) ;
#24661=VERTEX_POINT ( 'NONE', #5616 ) ;
#24677=FACE_OUTER_BOUND ( 'NONE', #7366, .T. ) ;
#24680=DIRECTION ( 'NONE',  ( 0.000000000000000000, -0.9659258262890662028, -0.2588190451025284000 ) ) ;
#24686=CARTESIAN_POINT ( 'NONE',  ( 25.74353197755034373, 2.942305264091934713, 0.6717076152027443570 ) ) ;
#24688=VECTOR ( 'NONE', #215, 1000.000000000000114 ) ;
#24693=PLANE ( 'NONE',  #17677 ) ;
#24696=VECTOR ( 'NONE', #11434, 1000.000000000000000 ) ;
#24700=CARTESIAN_POINT ( 'NONE',  ( 24.36000000273118715, 1.942864903642424146, 1.573300977624592534 ) ) ;
#24701=DIRECTION ( 'NONE',  ( -1.000000000000000000, 8.574039729943018344E-17, -0.000000000000000000 ) ) ;
#24703=CIRCLE ( 'NONE', #18822, 5.009999999999999787 ) ;
#24704=CARTESIAN_POINT ( 'NONE',  ( 20.99290772595112387, -0.1310194482076047495, -2.499999999999998668 ) ) ;
#24706=AXIS2_PLACEMENT_3D ( 'NONE', #3845, #29096, #31777 ) ;
#24714=EDGE_CURVE ( 'NONE', #22010, #16013, #10600, .T. ) ;
#24716=ORIENTED_EDGE ( 'NONE', *, *, #7167, .F. ) ;
#24719=EDGE_CURVE ( 'NONE', #19305, #4647, #5758, .T. ) ;
#24732=CARTESIAN_POINT ( 'NONE',  ( 22.98500000000000298, 2.486304738420679783, -0.2613211581691337604 ) ) ;
#24735=ORIENTED_EDGE ( 'NONE', *, *, #27240, .T. ) ;
#24741=DIRECTION ( 'NONE',  ( -1.000000000000000000, 8.574039729943018344E-17, -0.000000000000000000 ) ) ;
#24749=DIRECTION ( 'NONE',  ( 1.000000000000000000, -0.000000000000000000, -0.000000000000000000 ) ) ;
#24750=VECTOR ( 'NONE', #2491, 1000.000000000000114 ) ;
#24756=CARTESIAN_POINT ( 'NONE',  ( 10.56870887191539587, -1.946309384392624464, 4.616489984850525197 ) ) ;
#24768=ORIENTED_EDGE ( 'NONE', *, *, #9236, .T. ) ;
#24776=CARTESIAN_POINT ( 'NONE',  ( 23.67250000000000298, -1.291182301015472600, -2.378061970571982098 ) ) ;
#24779=ORIENTED_EDGE ( 'NONE', *, *, #21248, .F. ) ;
#24787=EDGE_CURVE ( 'NONE', #8864, #32058, #26630, .T. ) ;
#24792=CARTESIAN_POINT ( 'NONE',  ( 10.00000000000000178, -8.574039729943018837E-16, 0.000000000000000000 ) ) ;
#24793=LINE ( 'NONE', #21626, #28952 ) ;
#24794=CIRCLE ( 'NONE', #31219, 5.010000000000000675 ) ;
#24795=EDGE_LOOP ( 'NONE', ( #23965, #11625, #21037, #4198 ) ) ;
#24807=ORIENTED_EDGE ( 'NONE', *, *, #5919, .T. ) ;
#24813=CARTESIAN_POINT ( 'NONE',  ( 21.86000000136559507, -0.9349337715887247047, 3.156283516753367824 ) ) ;
#24818=ORIENTED_EDGE ( 'NONE', *, *, #25443, .T. ) ;
#24820=LINE ( 'NONE', #75, #2692 ) ;
#24821=CARTESIAN_POINT ( 'NONE',  ( 24.42250000136559507, 1.913930629741522838, -2.363507492473150062 ) ) ;
#24822=FACE_OUTER_BOUND ( 'NONE', #10566, .T. ) ;
#24826=CARTESIAN_POINT ( 'NONE',  ( 10.00000000000000178, -8.574039729943018837E-16, 0.000000000000000000 ) ) ;
#24827=EDGE_CURVE ( 'NONE', #27475, #24998, #1246, .T. ) ;
#24831=CARTESIAN_POINT ( 'NONE',  ( 23.55656763645045615, -0.8852964313267484009, 2.499999999999997780 ) ) ;
#24840=PLANE ( 'NONE',  #15451 ) ;
#24842=EDGE_LOOP ( 'NONE', ( #21278, #4735, #18976, #5991 ) ) ;
#24851=DIRECTION ( 'NONE',  ( 0.000000000000000000, -0.8191520442889833609, -0.5735764363510580388 ) ) ;
#24852=FACE_OUTER_BOUND ( 'NONE', #13887, .T. ) ;
#24866=EDGE_CURVE ( 'NONE', #1564, #15750, #21460, .T. ) ;
#24881=CARTESIAN_POINT ( 'NONE',  ( 25.76000000000000512, 2.749440278475487442, 1.299952413566024756 ) ) ;
#24883=ORIENTED_EDGE ( 'NONE', *, *, #23782, .F. ) ;
#24890=DIRECTION ( 'NONE',  ( -1.000000000000000000, 8.574039729943018344E-17, -0.000000000000000000 ) ) ;
#24895=CARTESIAN_POINT ( 'NONE',  ( 24.61000000136559862, 2.892927487894327410, -1.570731468192931635 ) ) ;
#24905=ORIENTED_EDGE ( 'NONE', *, *, #23486, .T. ) ;
#24907=LINE ( 'NONE', #19571, #31774 ) ;
#24909=ADVANCED_FACE ( 'NONE', ( #7242 ), #2564, .F. ) ;
#24914=DIRECTION ( 'NONE',  ( -7.472768010110281180E-18, -0.08715574274764813223, -0.9961946980917464334 ) ) ;
#24915=DIRECTION ( 'NONE',  ( -1.000000000000000000, 8.574039729943022041E-17, -1.232595164407830946E-32 ) ) ;
#24920=FACE_OUTER_BOUND ( 'NONE', #17556, .T. ) ;
#24922=ORIENTED_EDGE ( 'NONE', *, *, #24960, .F. ) ;
#24928=ORIENTED_EDGE ( 'NONE', *, *, #26372, .T. ) ;
#24930=CARTESIAN_POINT ( 'NONE',  ( 20.86000000136559507, 0.3178988483021036315, 3.024605502323848949 ) ) ;
#24934=ORIENTED_EDGE ( 'NONE', *, *, #2985, .F. ) ;
#24937=( BOUNDED_CURVE ( )  B_SPLINE_CURVE ( 2, ( #26511, #21494, #14268, #23973, #18639, #28837, #8601, #11608, #3763, #31705, #24151 ),
 .UNSPECIFIED., .F., .F. ) 
 B_SPLINE_CURVE_WITH_KNOTS ( ( 3, 2, 2, 2, 2, 3 ),
 ( 0.6966116191895003196, 0.6999999999999999556, 0.7249999999999999778, 0.7500000000000000000, 0.7750000000000000222, 0.7966116191895004084 ),
 .UNSPECIFIED. ) 
 CURVE ( )  GEOMETRIC_REPRESENTATION_ITEM ( )  RATIONAL_B_SPLINE_CURVE ( ( 0.9821626249036858880, 0.9896829947469992783, 1.000000000000000000, 0.9238795325112867385, 1.000000000000000000, 0.9238795325112867385, 1.000000000000000000, 0.9238795325112867385, 1.000000000000000000, 0.9341965377642874602, 0.9821626249036858880 ) ) 
 REPRESENTATION_ITEM ( '' )  );
#24943=CARTESIAN_POINT ( 'NONE',  ( 23.11000000273118715, 1.573300977624590313, -1.942864903642426144 ) ) ;
#24944=CARTESIAN_POINT ( 'NONE',  ( 24.36000000136559507, 0.9349337715887185984, -3.156283516753368268 ) ) ;
#24960=EDGE_CURVE ( 'NONE', #3463, #14136, #29814, .T. ) ;
#24966=ORIENTED_EDGE ( 'NONE', *, *, #31283, .F. ) ;
#24967=CARTESIAN_POINT ( 'NONE',  ( 21.11000000136559507, -3.156283516753370488, -0.9349337715887220401 ) ) ;
#24969=DIRECTION ( 'NONE',  ( -6.062761635205554800E-17, -0.7071067811865441310, -0.7071067811865510144 ) ) ;
#24974=CARTESIAN_POINT ( 'NONE',  ( 20.92250000136559507, 0.3178988483021036315, 3.024605502323848949 ) ) ;
#24979=CARTESIAN_POINT ( 'NONE',  ( 10.00000000000000178, -4.971152295393308940, 0.6226916219171868550 ) ) ;
#24992=FACE_OUTER_BOUND ( 'NONE', #12149, .T. ) ;
#24998=VERTEX_POINT ( 'NONE', #22630 ) ;
#24999=LINE ( 'NONE', #17480, #28363 ) ;
#25003=FACE_OUTER_BOUND ( 'NONE', #32753, .T. ) ;
#25004=CARTESIAN_POINT ( 'NONE',  ( -1.444447458290426890E-30, -1.659765939693074585E-14, 4.753758587302147731 ) ) ;
#25006=ADVANCED_FACE ( 'NONE', ( #27631 ), #2223, .F. ) ;
#25009=EDGE_CURVE ( 'NONE', #1852, #17100, #22443, .T. ) ;
#25011=VERTEX_POINT ( 'NONE', #10906 ) ;
#25020=DIRECTION ( 'NONE',  ( -7.770718973608957703E-17, -0.9063077870366483824, -0.4226182617407029940 ) ) ;
#25025=CARTESIAN_POINT ( 'NONE',  ( 25.79750000136559507, 2.363507492473148286, 1.913930629741525058 ) ) ;
#25040=CARTESIAN_POINT ( 'NONE',  ( 10.56183597391177464, 4.888740217817763464E-14, -4.753758587302147731 ) ) ;
#25042=CARTESIAN_POINT ( 'NONE',  ( 23.86000000136559507, 1.570731468192929858, 2.892927487894329186 ) ) ;
#25057=DIRECTION ( 'NONE',  ( 0.000000000000000000, 0.9063077870366497146, -0.4226182617406998299 ) ) ;
#25067=ORIENTED_EDGE ( 'NONE', *, *, #12013, .F. ) ;
#25070=VECTOR ( 'NONE', #31160, 1000.000000000000000 ) ;
#25084=EDGE_CURVE ( 'NONE', #28105, #28295, #12407, .T. ) ;
#25089=ORIENTED_EDGE ( 'NONE', *, *, #5006, .F. ) ;
#25100=CARTESIAN_POINT ( 'NONE',  ( 25.29750000136559507, -0.3178988483021076838, -3.024605502323848949 ) ) ;
#25107=CARTESIAN_POINT ( 'NONE',  ( -3.529825581556942343E-16, -4.116875700062099241, 2.376879293651050329 ) ) ;
#25132=CARTESIAN_POINT ( 'NONE',  ( 10.56183597391177464, -1.750323540954535505E-14, 4.753758587302147731 ) ) ;
#25140=CARTESIAN_POINT ( 'NONE',  ( 0.000000000000000000, 0.000000000000000000, 0.000000000000000000 ) ) ;
#25144=VECTOR ( 'NONE', #18538, 1000.000000000000000 ) ;
#25152=AXIS2_PLACEMENT_3D ( 'NONE', #1465, #11641, #24004 ) ;
#25157=VECTOR ( 'NONE', #2430, 1000.000000000000114 ) ;
#25160=ORIENTED_EDGE ( 'NONE', *, *, #5859, .T. ) ;
#25168=VECTOR ( 'NONE', #7744, 999.9999999999998863 ) ;
#25184=AXIS2_PLACEMENT_3D ( 'NONE', #14838, #22224, #2345 ) ;
#25185=VERTEX_POINT ( 'NONE', #29266 ) ;
#25187=FACE_OUTER_BOUND ( 'NONE', #14422, .T. ) ;
#25192=CARTESIAN_POINT ( 'NONE',  ( 10.00000000000000000, -3.055657119358826446, 3.641590349731918863 ) ) ;
#25197=AXIS2_PLACEMENT_3D ( 'NONE', #11255, #19114, #3259 ) ;
#25203=( BOUNDED_CURVE ( )  B_SPLINE_CURVE ( 2, ( #12838, #30271, #18043, #22740, #12685, #32604, #2014, #5179, #7343, #28232, #9677 ),
 .UNSPECIFIED., .F., .F. ) 
 B_SPLINE_CURVE_WITH_KNOTS ( ( 3, 2, 2, 2, 2, 3 ),
 ( 0.7966116191895004084, 0.8000000000000000444, 0.8249999999999999556, 0.8499999999999999778, 0.8750000000000000000, 0.8966116191895003862 ),
 .UNSPECIFIED. ) 
 CURVE ( )  GEOMETRIC_REPRESENTATION_ITEM ( )  RATIONAL_B_SPLINE_CURVE ( ( 0.9821626249036858880, 0.9896829947469992783, 1.000000000000000000, 0.9238795325112867385, 1.000000000000000000, 0.9238795325112867385, 1.000000000000000000, 0.9238795325112867385, 1.000000000000000000, 0.9341965377642874602, 0.9821626249036858880 ) ) 
 REPRESENTATION_ITEM ( '' )  );
#25204=CARTESIAN_POINT ( 'NONE',  ( 25.67250000136559507, 3.024605502323846729, -0.3178988483021056854 ) ) ;
#25221=VECTOR ( 'NONE', #32412, 1000.000000000000114 ) ;
#25226=CIRCLE ( 'NONE', #28947, 5.010000000000000675 ) ;
#25227=CARTESIAN_POINT ( 'NONE',  ( 10.00000000000000000, -3.055657119358825557, 3.641590349731918863 ) ) ;
#25228=CARTESIAN_POINT ( 'NONE',  ( 21.75111450864415730, -1.283275288181523244E-15, -2.499999999999998668 ) ) ;
#25229=AXIS2_PLACEMENT_3D ( 'NONE', #6236, #19111, #6887 ) ;
#25230=CARTESIAN_POINT ( 'NONE',  ( 21.29750000000000654, -0.7685399846772070775, 2.594547506269381465 ) ) ;
#25234=ORIENTED_EDGE ( 'NONE', *, *, #4230, .T. ) ;
#25247=CARTESIAN_POINT ( 'NONE',  ( 23.29750000136559862, -2.363507492473152283, -1.913930629741525280 ) ) ;
#25252=CARTESIAN_POINT ( 'NONE',  ( 1.668773398854356759E-16, 1.946309384392655106, -4.616489984850511874 ) ) ;
#25257=DIRECTION ( 'NONE',  ( 0.000000000000000000, 0.000000000000000000, -1.000000000000000000 ) ) ;
#25259=DIRECTION ( 'NONE',  ( 8.574039729943018344E-17, 1.000000000000000000, 0.000000000000000000 ) ) ;
#25282=CARTESIAN_POINT ( 'NONE',  ( -4.262285728429958207E-16, -4.971152295393298282, -0.6226916219172566880 ) ) ;
#25289=EDGE_CURVE ( 'NONE', #19049, #19482, #24256, .T. ) ;
#25291=CARTESIAN_POINT ( 'NONE',  ( 24.61000000136559862, 3.156283516753366047, 0.9349337715887203748 ) ) ;
#25300=EDGE_CURVE ( 'NONE', #18479, #18222, #18317, .T. ) ;
#25311=EDGE_CURVE ( 'NONE', #2976, #10505, #32120, .T. ) ;
#25325=EDGE_LOOP ( 'NONE', ( #4090, #28670, #27570, #13692 ) ) ;
#25328=CARTESIAN_POINT ( 'NONE',  ( 10.57125986779756843, 4.681538312723528605, -0.8254815157534771686 ) ) ;
#25334=DIRECTION ( 'NONE',  ( -1.000000000000000000, 8.574039729943018344E-17, -0.000000000000000000 ) ) ;
#25340=EDGE_CURVE ( 'NONE', #9839, #14852, #9017, .T. ) ;
#25346=ORIENTED_EDGE ( 'NONE', *, *, #25657, .F. ) ;
#25364=DIRECTION ( 'NONE',  ( -4.917867153433105649E-17, -0.5735764363510581498, 0.8191520442889834719 ) ) ;
#25369=CARTESIAN_POINT ( 'NONE',  ( 21.11000000273118715, 1.573300977624590313, -1.942864903642426144 ) ) ;
#25374=LINE ( 'NONE', #25192, #2259 ) ;
#25382=CARTESIAN_POINT ( 'NONE',  ( 22.17250000136559507, -3.024605502323851169, 0.3178988483021052969 ) ) ;
#25386=ORIENTED_EDGE ( 'NONE', *, *, #15588, .T. ) ;
#25389=ORIENTED_EDGE ( 'NONE', *, *, #10839, .F. ) ;
#25400=CARTESIAN_POINT ( 'NONE',  ( 22.86000000136559507, 1.570731468192929858, 2.892927487894329186 ) ) ;
#25407=CARTESIAN_POINT ( 'NONE',  ( -4.187842409712531875E-16, -4.884328206559829688, -1.115095498423360310 ) ) ;
#25410=ORIENTED_EDGE ( 'NONE', *, *, #10902, .T. ) ;
#25414=CARTESIAN_POINT ( 'NONE',  ( 10.00000000000000178, -8.574039729943018837E-16, 0.000000000000000000 ) ) ;
#25416=CARTESIAN_POINT ( 'NONE',  ( 21.73500000136559507, 3.156283516753366047, 0.9349337715887203748 ) ) ;
#25420=DIRECTION ( 'NONE',  ( 1.000000000000000000, -8.574039729943018344E-17, -0.000000000000000000 ) ) ;
#25426=DIRECTION ( 'NONE',  ( -2.219124775574841595E-17, -0.2588190451025108030, -0.9659258262890709767 ) ) ;
#25430=DIRECTION ( 'NONE',  ( 1.000000000000000000, -8.574039729943018344E-17, -0.000000000000000000 ) ) ;
#25432=VERTEX_POINT ( 'NONE', #7354 ) ;
#25438=PLANE ( 'NONE',  #9095 ) ;
#25441=FACE_OUTER_BOUND ( 'NONE', #30083, .T. ) ;
#25443=EDGE_CURVE ( 'NONE', #26609, #32682, #19920, .T. ) ;
#25445=ADVANCED_FACE ( 'NONE', ( #27742 ), #19733, .F. ) ;
#25447=ORIENTED_EDGE ( 'NONE', *, *, #4921, .F. ) ;
#25448=CARTESIAN_POINT ( 'NONE',  ( 7.077711312404847644E-17, 0.8254815157535873027, -4.681538312723508177 ) ) ;
#25449=EDGE_CURVE ( 'NONE', #5453, #5774, #30130, .T. ) ;
#25451=CARTESIAN_POINT ( 'NONE',  ( 24.04750000273118360, 0.7685399846772009713, -2.594547506269381909 ) ) ;
#25457=CARTESIAN_POINT ( 'NONE',  ( 25.75999999999999801, -1.902510934646483477E-15, 2.499999999999997780 ) ) ;
#25470=ORIENTED_EDGE ( 'NONE', *, *, #19494, .T. ) ;
#25477=VERTEX_POINT ( 'NONE', #25252 ) ;
#25484=ADVANCED_FACE ( 'NONE', ( #17398 ), #24564, .T. ) ;
#25485=DIRECTION ( 'NONE',  ( 0.000000000000000000, 1.000000000000000000, 0.000000000000000000 ) ) ;
#25489=CARTESIAN_POINT ( 'NONE',  ( 23.75111450864416440, -1.283275288181523244E-15, -2.499999999999998668 ) ) ;
#25491=EDGE_CURVE ( 'NONE', #27630, #19954, #24116, .T. ) ;
#25518=EDGE_CURVE ( 'NONE', #6857, #15836, #31107, .T. ) ;
#25525=DIRECTION ( 'NONE',  ( 0.000000000000000000, 1.000000000000000000, 0.000000000000000000 ) ) ;
#25531=ORIENTED_EDGE ( 'NONE', *, *, #23840, .T. ) ;
#25541=VERTEX_POINT ( 'NONE', #7859 ) ;
#25553=EDGE_CURVE ( 'NONE', #32816, #9958, #10522, .T. ) ;
#25555=CARTESIAN_POINT ( 'NONE',  ( 24.42250000136559507, -0.3178988483021076838, -3.024605502323848949 ) ) ;
#25563=ORIENTED_EDGE ( 'NONE', *, *, #28766, .F. ) ;
#25568=CARTESIAN_POINT ( 'NONE',  ( 23.92250000136559507, 0.3178988483021036315, 3.024605502323848949 ) ) ;
#25572=CARTESIAN_POINT ( 'NONE',  ( 25.75999999999999801, -2.208672634433321348E-15, 0.000000000000000000 ) ) ;
#25594=CARTESIAN_POINT ( 'NONE',  ( 22.36000000273118715, 1.942864903642424146, 1.573300977624592534 ) ) ;
#25595=ORIENTED_EDGE ( 'NONE', *, *, #30965, .T. ) ;
#25599=CARTESIAN_POINT ( 'NONE',  ( 24.29750000136559507, -0.3178988483021076838, -3.024605502323848949 ) ) ;
#25604=DIRECTION ( 'NONE',  ( 0.000000000000000000, -0.08715574274764813223, -0.9961946980917464334 ) ) ;
#25605=CARTESIAN_POINT ( 'NONE',  ( 22.79750000136559862, 0.3178988483021036315, 3.024605502323848949 ) ) ;
#25606=CARTESIAN_POINT ( 'NONE',  ( 10.00000000000000000, 4.681538312723516171, 0.8254815157535410064 ) ) ;
#25610=ORIENTED_EDGE ( 'NONE', *, *, #11546, .F. ) ;
#25615=EDGE_LOOP ( 'NONE', ( #3169, #9254, #14199, #3844 ) ) ;
#25616=CIRCLE ( 'NONE', #19726, 5.010000000000000675 ) ;
#25617=CARTESIAN_POINT ( 'NONE',  ( 25.59254563806580762, 1.901228607813702398, 2.157594591774798509 ) ) ;
#25621=ADVANCED_FACE ( 'NONE', ( #28419 ), #15366, .T. ) ;
#25622=EDGE_LOOP ( 'NONE', ( #3385, #10897, #26797, #31912 ) ) ;
#25641=DIRECTION ( 'NONE',  ( -1.000000000000000000, 8.574039729943019576E-17, 1.232595164407830946E-32 ) ) ;
#25645=LINE ( 'NONE', #15789, #11292 ) ;
#25646=LINE ( 'NONE', #20654, #14643 ) ;
#25656=VECTOR ( 'NONE', #29610, 1000.000000000000000 ) ;
#25657=EDGE_CURVE ( 'NONE', #31776, #19352, #15107, .T. ) ;
#25678=AXIS2_PLACEMENT_3D ( 'NONE', #28080, #2515, #22738 ) ;
#25681=AXIS2_PLACEMENT_3D ( 'NONE', #5944, #18341, #26366 ) ;
#25682=CIRCLE ( 'NONE', #12329, 6.000000000000000888 ) ;
#25684=VECTOR ( 'NONE', #18229, 1000.000000000000000 ) ;
#25687=EDGE_CURVE ( 'NONE', #21907, #3071, #27934, .T. ) ;
#25690=VECTOR ( 'NONE', #9708, 1000.000000000000000 ) ;
#25696=VERTEX_POINT ( 'NONE', #26896 ) ;
#25709=AXIS2_PLACEMENT_3D ( 'NONE', #2676, #20730, #15712 ) ;
#25710=CIRCLE ( 'NONE', #26239, 5.009999999999999787 ) ;
#25714=APPLICATION_CONTEXT ( 'configuration controlled 3d designs of mechanical parts and assemblies' ) ;
#25720=CARTESIAN_POINT ( 'NONE',  ( 25.23499999999999943, 0.2613211581691317065, 2.486304738420681559 ) ) ;
#25722=ORIENTED_EDGE ( 'NONE', *, *, #15754, .F. ) ;
#25734=ORIENTED_EDGE ( 'NONE', *, *, #6427, .F. ) ;
#25737=AXIS2_PLACEMENT_3D ( 'NONE', #19500, #14133, #31873 ) ;
#25742=LINE ( 'NONE', #22746, #3905 ) ;
#25743=AXIS2_PLACEMENT_3D ( 'NONE', #12776, #25855, #20673 ) ;
#25748=LINE ( 'NONE', #350, #3902 ) ;
#25750=ORIENTED_EDGE ( 'NONE', *, *, #21559, .F. ) ;
#25753=VECTOR ( 'NONE', #9524, 1000.000000000000000 ) ;
#25755=VECTOR ( 'NONE', #22818, 1000.000000000000000 ) ;
#25759=AXIS2_PLACEMENT_3D ( 'NONE', #8795, #6275, #1443 ) ;
#25766=VERTEX_POINT ( 'NONE', #22211 ) ;
#25771=CIRCLE ( 'NONE', #24706, 5.010000000000000675 ) ;
#25775=CARTESIAN_POINT ( 'NONE',  ( 25.75999999999999801, 5.000000000000000000, 0.000000000000000000 ) ) ;
#25780=CARTESIAN_POINT ( 'NONE',  ( 23.42250000136559862, 1.913930629741522838, -2.363507492473150062 ) ) ;
#25787=VECTOR ( 'NONE', #32957, 1000.000000000000227 ) ;
#25789=CARTESIAN_POINT ( 'NONE',  ( 25.17250000273118715, 2.378061970571979433, -1.291182301015470824 ) ) ;
#25790=CIRCLE ( 'NONE', #32214, 5.009999999999999787 ) ;
#25794=AXIS2_PLACEMENT_3D ( 'NONE', #27476, #17580, #4577 ) ;
#25808=ORIENTED_EDGE ( 'NONE', *, *, #19838, .F. ) ;
#25813=AXIS2_PLACEMENT_3D ( 'NONE', #8985, #19196, #16690 ) ;
#25816=ORIENTED_EDGE ( 'NONE', *, *, #31151, .T. ) ;
#25829=LINE ( 'NONE', #30854, #23488 ) ;
#25836=EDGE_CURVE ( 'NONE', #17341, #9887, #29896, .T. ) ;
#25837=CARTESIAN_POINT ( 'NONE',  ( 3.122314033877900197E-16, 3.641590349731971710, -3.055657119358763829 ) ) ;
#25847=AXIS2_PLACEMENT_3D ( 'NONE', #29124, #9024, #21119 ) ;
#25855=DIRECTION ( 'NONE',  ( 1.000000000000000000, -8.574039729943018344E-17, -0.000000000000000000 ) ) ;
#25858=ORIENTED_EDGE ( 'NONE', *, *, #19596, .T. ) ;
#25862=CARTESIAN_POINT ( 'NONE',  ( 25.76000000000000512, 0.9672760553990802368, 2.878205665084649478 ) ) ;
#25869=CARTESIAN_POINT ( 'NONE',  ( 10.00000000000000000, -4.467071865485462645, -1.625881193364742572 ) ) ;
#25870=VERTEX_POINT ( 'NONE', #19696 ) ;
#25872=CARTESIAN_POINT ( 'NONE',  ( 25.75999999999999801, -2.208672634433321348E-15, 0.000000000000000000 ) ) ;
#25877=ADVANCED_FACE ( 'NONE', ( #29579 ), #6169, .T. ) ;
#25881=CARTESIAN_POINT ( 'NONE',  ( 23.98499999999999943, 2.486304738420679783, -0.2613211581691337604 ) ) ;
#25885=EDGE_LOOP ( 'NONE', ( #19580, #12283, #28523, #6742 ) ) ;
#25893=ORIENTED_EDGE ( 'NONE', *, *, #29080, .T. ) ;
#25906=CARTESIAN_POINT ( 'NONE',  ( 10.57125986779756843, -0.8254815157534942660, -4.681538312723525053 ) ) ;
#25908=EDGE_CURVE ( 'NONE', #5049, #32842, #3058, .T. ) ;
#25921=CARTESIAN_POINT ( 'NONE',  ( 21.17250000136559507, -3.024605502323851169, 0.3178988483021052969 ) ) ;
#25942=DIRECTION ( 'NONE',  ( -4.917867153433028611E-17, -0.5735764363510496011, 0.8191520442889893561 ) ) ;
#25948=CARTESIAN_POINT ( 'NONE',  ( 22.11000000136559507, -3.156283516753370044, -0.9349337715887220401 ) ) ;
#25950=DIRECTION ( 'NONE',  ( 0.000000000000000000, 1.000000000000000000, 0.000000000000000000 ) ) ;
#25957=CARTESIAN_POINT ( 'NONE',  ( 20.79750000136559507, 0.3178988483021036315, 3.024605502323848949 ) ) ;
#25958=EDGE_CURVE ( 'NONE', #3558, #31165, #24395, .T. ) ;
#25963=DIRECTION ( 'NONE',  ( 1.000000000000000000, -8.574039729943018344E-17, -0.000000000000000000 ) ) ;
#25966=EDGE_CURVE ( 'NONE', #31776, #19663, #19225, .T. ) ;
#25981=EDGE_CURVE ( 'NONE', #22947, #25870, #21733, .T. ) ;
#26000=DIRECTION ( 'NONE',  ( 2.219124775575021862E-17, 0.2588190451025318417, -0.9659258262890653146 ) ) ;
#26002=CARTESIAN_POINT ( 'NONE',  ( -2.330754651808319766E-16, -2.718385644597204553, 4.208382051008182856 ) ) ;
#26003=EDGE_LOOP ( 'NONE', ( #13951, #9652, #6257, #18140, #397, #3133, #27805, #19927, #30329, #25089, #26286, #9345, #16704, #30728, #28043, #361, #9895, #14490, #18165, #14255, #2572, #24048, #9260, #31356, #24883, #19627, #296, #23186, #7377, #23894, #13607, #149, #29763, #24934, #13355, #29821, #26743, #19781, #15172, #31331, #31846, #10038, #3679, #13923, #20700, #30879, #9075, #28775, #4194, #10476, #28072, #7196, #28394, #32463, #20365, #18096, #29596, #6135, #27282, #26570, #30464, #24716, #22599, #15224, #28146, #26350, #5811, #14687, #24922, #30715, #959, #8443, #11980, #32359, #14635, #31168, #4482, #13217, #14194, #11599, #17295, #29324, #11379, #23777, #18172, #22108, #18938, #732, #19503, #23381, #8525, #5161, #18362, #22497, #27910, #22722, #18963, #10605, #8071, #17068, #10080, #9351, #6552, #11251, #16707, #16563, #11051, #29456 ) ) ;
#26004=CARTESIAN_POINT ( 'NONE',  ( 23.67250000136559507, 3.024605502323846729, -0.3178988483021056854 ) ) ;
#26014=CARTESIAN_POINT ( 'NONE',  ( 10.00000000000000178, -8.574039729943018837E-16, 0.000000000000000000 ) ) ;
#26015=EDGE_LOOP ( 'NONE', ( #1882, #25531, #26642, #12781 ) ) ;
#26024=DIRECTION ( 'NONE',  ( -8.541412920197222280E-17, -0.9961946980917457672, 0.08715574274765533480 ) ) ;
#26026=FACE_OUTER_BOUND ( 'NONE', #17728, .T. ) ;
#26027=LINE ( 'NONE', #12980, #26337 ) ;
#26033=CARTESIAN_POINT ( 'NONE',  ( 3.822634483660907761E-16, 4.458382051008192626, 2.285372942704970267 ) ) ;
#26036=CARTESIAN_POINT ( 'NONE',  ( 22.99290772595112387, -0.1310194482076047495, -2.499999999999998668 ) ) ;
#26040=ORIENTED_EDGE ( 'NONE', *, *, #8345, .T. ) ;
#26054=PLANE ( 'NONE',  #10706 ) ;
#26057=ORIENTED_EDGE ( 'NONE', *, *, #24714, .T. ) ;
#26070=ORIENTED_EDGE ( 'NONE', *, *, #19818, .F. ) ;
#26079=ORIENTED_EDGE ( 'NONE', *, *, #12240, .T. ) ;
#26106=CARTESIAN_POINT ( 'NONE',  ( 22.61000000136559507, 3.156283516753366047, 0.9349337715887203748 ) ) ;
#26115=ORIENTED_EDGE ( 'NONE', *, *, #15116, .F. ) ;
#26116=CARTESIAN_POINT ( 'NONE',  ( 25.55210404927549916, 2.101042102276441170, 1.904186784126992604 ) ) ;
#26129=VERTEX_POINT ( 'NONE', #5526 ) ;
#26134=VERTEX_POINT ( 'NONE', #31574 ) ;
#26137=CARTESIAN_POINT ( 'NONE',  ( 25.23499999999999943, -2.208672634433321348E-15, 0.000000000000000000 ) ) ;
#26147=CARTESIAN_POINT ( 'NONE',  ( 10.56870887191539587, 4.467071865485493731, -1.625881193364653088 ) ) ;
#26150=DIRECTION ( 'NONE',  ( 1.000000000000000000, -0.000000000000000000, -0.000000000000000000 ) ) ;
#26154=CARTESIAN_POINT ( 'NONE',  ( 10.00000000000000178, 4.787500056513387392, -1.476463073999587872 ) ) ;
#26155=ORIENTED_EDGE ( 'NONE', *, *, #4921, .T. ) ;
#26156=CARTESIAN_POINT ( 'NONE',  ( 24.86000000136559862, 1.570731468192929858, 2.892927487894329186 ) ) ;
#26158=EDGE_CURVE ( 'NONE', #27483, #18153, #21023, .T. ) ;
#26160=EDGE_LOOP ( 'NONE', ( #31239, #17674, #2937, #15339 ) ) ;
#26161=CARTESIAN_POINT ( 'NONE',  ( 4.290242492657217039E-16, 5.003758587302148619, -0.2499999999999991951 ) ) ;
#26171=CARTESIAN_POINT ( 'NONE',  ( 24.48500000136559507, 2.892927487894327410, -1.570731468192931635 ) ) ;
#26178=DIRECTION ( 'NONE',  ( 4.917867153433085311E-17, 0.5735764363510552633, -0.8191520442889853593 ) ) ;
#26181=ADVANCED_FACE ( 'NONE', ( #3516 ), #24021, .F. ) ;
#26182=ORIENTED_EDGE ( 'NONE', *, *, #10140, .T. ) ;
#26188=VECTOR ( 'NONE', #27029, 1000.000000000000000 ) ;
#26189=FACE_OUTER_BOUND ( 'NONE', #30147, .T. ) ;
#26191=CARTESIAN_POINT ( 'NONE',  ( 23.86000000000000298, 1.573300977624590313, -1.942864903642426144 ) ) ;
#26199=AXIS2_PLACEMENT_3D ( 'NONE', #18076, #703, #10707 ) ;
#26205=ORIENTED_EDGE ( 'NONE', *, *, #26240, .T. ) ;
#26226=ORIENTED_EDGE ( 'NONE', *, *, #21285, .T. ) ;
#26239=AXIS2_PLACEMENT_3D ( 'NONE', #16661, #4136, #11995 ) ;
#26240=EDGE_CURVE ( 'NONE', #12555, #32142, #10854, .T. ) ;
#26248=DIRECTION ( 'NONE',  ( 0.000000000000000000, 1.000000000000000000, 0.000000000000000000 ) ) ;
#26251=DIRECTION ( 'NONE',  ( -6.062761635205578219E-17, -0.7071067811865465735, 0.7071067811865484609 ) ) ;
#26258=CARTESIAN_POINT ( 'NONE',  ( 2.037945749704312686E-16, 2.376879293651064540, 4.116875700062091248 ) ) ;
#26262=VERTEX_POINT ( 'NONE', #8976 ) ;
#26267=CARTESIAN_POINT ( 'NONE',  ( 20.92250000136559507, -1.913930629741527500, 2.363507492473149618 ) ) ;
#26274=EDGE_CURVE ( 'NONE', #31424, #20071, #26704, .T. ) ;
#26276=CARTESIAN_POINT ( 'NONE',  ( 21.79750000273118715, -2.594547506269383685, -0.7685399846772043020 ) ) ;
#26286=ORIENTED_EDGE ( 'NONE', *, *, #4184, .F. ) ;
#26302=DIRECTION ( 'NONE',  ( 7.770718973608941679E-17, 0.9063077870366467170, 0.4226182617407064912 ) ) ;
#26308=EDGE_LOOP ( 'NONE', ( #7463, #30487, #8538, #26436 ) ) ;
#26312=ADVANCED_FACE ( 'NONE', ( #22205 ), #14316, .F. ) ;
#26323=CARTESIAN_POINT ( 'NONE',  ( 24.55656763645044904, -0.8852964313267484009, 2.499999999999997780 ) ) ;
#26327=DIRECTION ( 'NONE',  ( 1.000000000000000000, -0.000000000000000000, -0.000000000000000000 ) ) ;
#26332=LINE ( 'NONE', #32346, #654 ) ;
#26334=CARTESIAN_POINT ( 'NONE',  ( 17.75999999999999801, -2.208672634433321348E-15, 0.000000000000000000 ) ) ;
#26336=CARTESIAN_POINT ( 'NONE',  ( 22.36000000136559152, -1.570731468192933633, -2.892927487894330074 ) ) ;
#26337=VECTOR ( 'NONE', #7810, 1000.000000000000000 ) ;
#26344=CIRCLE ( 'NONE', #26874, 3.024999999999999911 ) ;
#26350=ORIENTED_EDGE ( 'NONE', *, *, #8107, .F. ) ;
#26354=ORIENTED_EDGE ( 'NONE', *, *, #20308, .T. ) ;
#26355=CARTESIAN_POINT ( 'NONE',  ( 21.25111450864416085, -3.256483526998273983E-15, 2.499999999999998668 ) ) ;
#26366=DIRECTION ( 'NONE',  ( 0.000000000000000000, 1.000000000000000000, 0.000000000000000000 ) ) ;
#26370=ADVANCED_FACE ( 'NONE', ( #1827 ), #6969, .F. ) ;
#26372=EDGE_CURVE ( 'NONE', #24462, #9763, #11827, .T. ) ;
#26376=DIRECTION ( 'NONE',  ( 0.000000000000000000, 0.9659258262890679791, 0.2588190451025216277 ) ) ;
#26377=CARTESIAN_POINT ( 'NONE',  ( 22.79750000273118715, -2.594547506269383685, -0.7685399846772043020 ) ) ;
#26383=VERTEX_POINT ( 'NONE', #11658 ) ;
#26399=CARTESIAN_POINT ( 'NONE',  ( 10.56870887191539587, -4.616489984850547401, 1.946309384392575392 ) ) ;
#26405=CARTESIAN_POINT ( 'NONE',  ( 21.79750000136559507, 2.363507492473148286, 1.913930629741525058 ) ) ;
#26413=ORIENTED_EDGE ( 'NONE', *, *, #4463, .F. ) ;
#26415=VECTOR ( 'NONE', #417, 1000.000000000000000 ) ;
#26423=CARTESIAN_POINT ( 'NONE',  ( 10.00000000000000000, 4.893557421779793832E-14, -4.753758587302147731 ) ) ;
#26425=ORIENTED_EDGE ( 'NONE', *, *, #17739, .F. ) ;
#26430=DIRECTION ( 'NONE',  ( 0.000000000000000000, 1.000000000000000000, 0.000000000000000000 ) ) ;
#26434=CYLINDRICAL_SURFACE ( 'NONE', #5498, 2.499999999999997780 ) ;
#26436=ORIENTED_EDGE ( 'NONE', *, *, #21878, .F. ) ;
#26446=EDGE_CURVE ( 'NONE', #25541, #7070, #30977, .T. ) ;
#26448=CARTESIAN_POINT ( 'NONE',  ( 20.79750000136559507, 0.3178988483021036315, 3.024605502323848949 ) ) ;
#26450=ORIENTED_EDGE ( 'NONE', *, *, #6346, .T. ) ;
#26455=LINE ( 'NONE', #13376, #6572 ) ;
#26471=FACE_OUTER_BOUND ( 'NONE', #19093, .T. ) ;
#26482=CARTESIAN_POINT ( 'NONE',  ( 25.75999999999999801, -2.208672634433321348E-15, 0.000000000000000000 ) ) ;
#26483=CARTESIAN_POINT ( 'NONE',  ( 24.61000000273118715, -1.573300977624594976, 1.942864903642425700 ) ) ;
#26493=CARTESIAN_POINT ( 'NONE',  ( 25.30158241411874798, -1.345927778950697595, 2.192379955416479120 ) ) ;
#26498=EDGE_CURVE ( 'NONE', #5204, #21729, #22185, .T. ) ;
#26505=FACE_OUTER_BOUND ( 'NONE', #11367, .T. ) ;
#26511=CARTESIAN_POINT ( 'NONE',  ( 22.00111451137534502, -1.241879311143409511E-16, -2.499999999999998668 ) ) ;
#26517=FACE_OUTER_BOUND ( 'NONE', #24842, .T. ) ;
#26520=DIRECTION ( 'NONE',  ( 0.000000000000000000, 0.9659258262890698665, -0.2588190451025149663 ) ) ;
#26530=EDGE_CURVE ( 'NONE', #20748, #26134, #456, .T. ) ;
#26544=ORIENTED_EDGE ( 'NONE', *, *, #12013, .T. ) ;
#26545=EDGE_CURVE ( 'NONE', #15334, #21706, #23266, .T. ) ;
#26552=CARTESIAN_POINT ( 'NONE',  ( 25.75999999999999801, 5.000000000000000000, 0.000000000000000000 ) ) ;
#26557=LINE ( 'NONE', #8661, #25144 ) ;
#26560=ORIENTED_EDGE ( 'NONE', *, *, #22094, .T. ) ;
#26570=ORIENTED_EDGE ( 'NONE', *, *, #26966, .F. ) ;
#26579=EDGE_LOOP ( 'NONE', ( #9067, #15155, #29505, #11901 ) ) ;
#26582=CARTESIAN_POINT ( 'NONE',  ( 22.67249999999999943, -1.291182301015472378, -2.378061970571982098 ) ) ;
#26590=DIRECTION ( 'NONE',  ( 0.000000000000000000, -0.8191520442889869136, -0.5735764363510531538 ) ) ;
#26595=DIRECTION ( 'NONE',  ( -1.000000000000000000, 8.574039729943022041E-17, -3.081487911019577365E-33 ) ) ;
#26606=FACE_OUTER_BOUND ( 'NONE', #22700, .T. ) ;
#26609=VERTEX_POINT ( 'NONE', #27627 ) ;
#26611=DIRECTION ( 'NONE',  ( 0.000000000000000000, 0.5735764363510391650, 0.8191520442889965725 ) ) ;
#26615=DIRECTION ( 'NONE',  ( 1.000000000000000000, -8.574039729943018344E-17, -0.000000000000000000 ) ) ;
#26617=DIRECTION ( 'NONE',  ( -1.000000000000000000, 8.574039729943018344E-17, -0.000000000000000000 ) ) ;
#26623=DIRECTION ( 'NONE',  ( 1.000000000000000000, -8.574039729943018344E-17, -0.000000000000000000 ) ) ;
#26625=CARTESIAN_POINT ( 'NONE',  ( 24.86000000273118715, -1.942864903642428587, -1.573300977624592756 ) ) ;
#26630=LINE ( 'NONE', #19113, #11895 ) ;
#26636=EDGE_CURVE ( 'NONE', #13368, #4840, #13947, .T. ) ;
#26639=ORIENTED_EDGE ( 'NONE', *, *, #13719, .T. ) ;
#26642=ORIENTED_EDGE ( 'NONE', *, *, #21668, .T. ) ;
#26647=ORIENTED_EDGE ( 'NONE', *, *, #11876, .F. ) ;
#26654=CARTESIAN_POINT ( 'NONE',  ( 25.75999999999999801, -2.208672634433321348E-15, 0.000000000000000000 ) ) ;
#26656=CARTESIAN_POINT ( 'NONE',  ( 10.00000000000000178, 3.024842911000690915, 3.993798362933321133 ) ) ;
#26667=CARTESIAN_POINT ( 'NONE',  ( 21.54750000000000298, -2.594547506269383685, -0.7685399846772043020 ) ) ;
#26693=CARTESIAN_POINT ( 'NONE',  ( 25.57927635680546175, 0.4793050474504166325, -2.813602956598889815 ) ) ;
#26703=CARTESIAN_POINT ( 'NONE',  ( 25.75999999999999801, -2.208672634433321348E-15, 0.000000000000000000 ) ) ;
#26704=LINE ( 'NONE', #9137, #30597 ) ;
#26710=ORIENTED_EDGE ( 'NONE', *, *, #18575, .F. ) ;
#26715=VECTOR ( 'NONE', #10303, 1000.000000000000000 ) ;
#26729=VERTEX_POINT ( 'NONE', #25606 ) ;
#26735=CARTESIAN_POINT ( 'NONE',  ( 24.67249999999999943, -1.291182301015472378, -2.378061970571982098 ) ) ;
#26742=DIRECTION ( 'NONE',  ( 2.219124775574956535E-17, 0.2588190451025241812, -0.9659258262890673130 ) ) ;
#26743=ORIENTED_EDGE ( 'NONE', *, *, #27238, .F. ) ;
#26749=CARTESIAN_POINT ( 'NONE',  ( 20.92250000273118360, -1.291182301015472378, -2.378061970571982098 ) ) ;
#26763=LINE ( 'NONE', #28957, #3417 ) ;
#26769=EDGE_CURVE ( 'NONE', #19049, #6820, #25226, .T. ) ;
#26777=CYLINDRICAL_SURFACE ( 'NONE', #25184, 2.499999999999997780 ) ;
#26782=VERTEX_POINT ( 'NONE', #18434 ) ;
#26791=EDGE_CURVE ( 'NONE', #12161, #6820, #20617, .T. ) ;
#26792=AXIS2_PLACEMENT_3D ( 'NONE', #16093, #26327, #16273 ) ;
#26797=ORIENTED_EDGE ( 'NONE', *, *, #25340, .T. ) ;
#26800=VECTOR ( 'NONE', #11531, 1000.000000000000000 ) ;
#26811=CIRCLE ( 'NONE', #5475, 5.009999999999999787 ) ;
#26818=DIRECTION ( 'NONE',  ( 1.000000000000000000, -8.574039729943018344E-17, -0.000000000000000000 ) ) ;
#26828=VECTOR ( 'NONE', #30250, 1000.000000000000000 ) ;
#26832=EDGE_CURVE ( 'NONE', #22618, #21128, #18084, .T. ) ;
#26836=LINE ( 'NONE', #24327, #10269 ) ;
#26839=CARTESIAN_POINT ( 'NONE',  ( 10.56870887191539587, 4.616489984850530526, 1.946309384392607811 ) ) ;
#26843=CIRCLE ( 'NONE', #12432, 5.009999999999999787 ) ;
#26847=ORIENTED_EDGE ( 'NONE', *, *, #568, .T. ) ;
#26855=VERTEX_POINT ( 'NONE', #30823 ) ;
#26864=AXIS2_PLACEMENT_3D ( 'NONE', #26482, #16269, #19268 ) ;
#26874=AXIS2_PLACEMENT_3D ( 'NONE', #5042, #15219, #27595 ) ;
#26882=CARTESIAN_POINT ( 'NONE',  ( 20.79750000136559507, 0.3178988483021036315, 3.024605502323848949 ) ) ;
#26889=CARTESIAN_POINT ( 'NONE',  ( 24.42250000273118715, 1.291182301015469047, 2.378061970571981654 ) ) ;
#26890=DIRECTION ( 'NONE',  ( 0.000000000000000000, 0.4226182617407097108, -0.9063077870366451627 ) ) ;
#26891=EDGE_LOOP ( 'NONE', ( #13569, #27987, #23444, #8461 ) ) ;
#26892=LINE ( 'NONE', #1831, #18313 ) ;
#26893=EDGE_LOOP ( 'NONE', ( #1422, #5239, #10992, #5325 ) ) ;
#26894=LINE ( 'NONE', #22046, #27905 ) ;
#26896=CARTESIAN_POINT ( 'NONE',  ( -1.394036994807583480E-16, -1.625881193364668409, -4.467071865485488402 ) ) ;
#26912=EDGE_LOOP ( 'NONE', ( #24818, #8079, #25160, #20723 ) ) ;
#26918=CARTESIAN_POINT ( 'NONE',  ( 23.23500000000000298, 0.2613211581691317065, 2.486304738420681559 ) ) ;
#26920=CARTESIAN_POINT ( 'NONE',  ( 10.52034268205830614, 3.641590349731970822, -3.055657119358763829 ) ) ;
#26926=DIRECTION ( 'NONE',  ( 0.000000000000000000, -0.4226182617406906705, -0.9063077870366540445 ) ) ;
#26932=CARTESIAN_POINT ( 'NONE',  ( 22.04750000273119070, 0.7685399846772009713, -2.594547506269381909 ) ) ;
#26943=ADVANCED_FACE ( 'NONE', ( #31796 ), #16385, .T. ) ;
#26949=ORIENTED_EDGE ( 'NONE', *, *, #4698, .T. ) ;
#26955=VERTEX_POINT ( 'NONE', #14045 ) ;
#26956=EDGE_CURVE ( 'NONE', #502, #6248, #29263, .T. ) ;
#26957=EDGE_CURVE ( 'NONE', #19352, #32781, #6349, .T. ) ;
#26958=CARTESIAN_POINT ( 'NONE',  ( 23.30656763371926488, -0.8852964313267484009, 2.499999999999997780 ) ) ;
#26960=FACE_OUTER_BOUND ( 'NONE', #7563, .T. ) ;
#26963=CARTESIAN_POINT ( 'NONE',  ( 22.61000000000000298, -1.942864903642428587, -1.573300977624592756 ) ) ;
#26966=EDGE_CURVE ( 'NONE', #15085, #21907, #5720, .T. ) ;
#26970=CARTESIAN_POINT ( 'NONE',  ( 24.92250000273118360, -1.291182301015472600, -2.378061970571982098 ) ) ;
#26974=FACE_OUTER_BOUND ( 'NONE', #10460, .T. ) ;
#26992=CARTESIAN_POINT ( 'NONE',  ( 21.48500000136559507, 2.892927487894327410, -1.570731468192931635 ) ) ;
#26995=DIRECTION ( 'NONE',  ( 1.000000000000000000, -8.574039729943018344E-17, -0.000000000000000000 ) ) ;
#26996=DIRECTION ( 'NONE',  ( 0.000000000000000000, 1.000000000000000000, 0.000000000000000000 ) ) ;
#27007=EDGE_CURVE ( 'NONE', #17346, #17028, #19233, .T. ) ;
#27011=CARTESIAN_POINT ( 'NONE',  ( 23.92250000273118715, -1.291182301015472600, -2.378061970571982098 ) ) ;
#27012=CARTESIAN_POINT ( 'NONE',  ( 21.74290772321993970, -0.1310194482076047495, -2.499999999999998668 ) ) ;
#27021=EDGE_CURVE ( 'NONE', #15187, #10158, #27555, .T. ) ;
#27022=ORIENTED_EDGE ( 'NONE', *, *, #1514, .T. ) ;
#27024=EDGE_CURVE ( 'NONE', #27475, #13277, #4845, .T. ) ;
#27026=CARTESIAN_POINT ( 'NONE',  ( 22.25111450864416085, -3.256483526998273983E-15, 2.499999999999998668 ) ) ;
#27029=DIRECTION ( 'NONE',  ( -1.000000000000000000, 8.574039729943022041E-17, -1.232595164407830946E-32 ) ) ;
#27036=CARTESIAN_POINT ( 'NONE',  ( 25.70386696102259805, 2.933694492117787433, -0.5143199855282081234 ) ) ;
#27041=FACE_OUTER_BOUND ( 'NONE', #2376, .T. ) ;
#27056=EDGE_CURVE ( 'NONE', #6248, #12746, #25742, .T. ) ;
#27061=CARTESIAN_POINT ( 'NONE',  ( 10.00000000000000178, -8.574039729943018837E-16, 0.000000000000000000 ) ) ;
#27066=CARTESIAN_POINT ( 'NONE',  ( 24.54749999999999943, -2.594547506269383685, -0.7685399846772043020 ) ) ;
#27068=CARTESIAN_POINT ( 'NONE',  ( 23.36000000000000298, -1.573300977624594976, 1.942864903642425700 ) ) ;
#27075=CARTESIAN_POINT ( 'NONE',  ( 10.00000000000000000, 2.376879293651063652, 4.116875700062091248 ) ) ;
#27078=EDGE_LOOP ( 'NONE', ( #27944, #22424, #5868, #26710, #14607, #27307 ) ) ;
#27082=CARTESIAN_POINT ( 'NONE',  ( 10.57125986779756843, 0.6226916219172707878, -4.971152295393295617 ) ) ;
#27083=CARTESIAN_POINT ( 'NONE',  ( 25.29750000136559507, -2.363507492473152283, -1.913930629741525280 ) ) ;
#27084=CARTESIAN_POINT ( 'NONE',  ( 10.55147673363119054, 4.458382051008191738, 2.285372942704970267 ) ) ;
#27095=CYLINDRICAL_SURFACE ( 'NONE', #6422, 2.499999999999997780 ) ;
#27096=ORIENTED_EDGE ( 'NONE', *, *, #8074, .T. ) ;
#27097=CARTESIAN_POINT ( 'NONE',  ( 1.394036994807608625E-16, 1.625881193364697719, 4.467071865485476856 ) ) ;
#27108=CARTESIAN_POINT ( 'NONE',  ( -3.529825581556913254E-16, -4.116875700062066379, -2.376879293651108060 ) ) ;
#27118=CARTESIAN_POINT ( 'NONE',  ( 23.29750000273119070, 2.594547506269380133, 0.7685399846772031918 ) ) ;
#27121=LINE ( 'NONE', #1914, #18813 ) ;
#27125=DIRECTION ( 'NONE',  ( 7.472768010110040824E-18, 0.08715574274764535667, 0.9961946980917466554 ) ) ;
#27133=EDGE_CURVE ( 'NONE', #25870, #32468, #25790, .T. ) ;
#27135=ORIENTED_EDGE ( 'NONE', *, *, #7722, .T. ) ;
#27141=CARTESIAN_POINT ( 'NONE',  ( 21.92250000136559507, -1.913930629741527500, 2.363507492473149618 ) ) ;
#27143=ORIENTED_EDGE ( 'NONE', *, *, #28766, .T. ) ;
#27146=CARTESIAN_POINT ( 'NONE',  ( 3.424298583717156572E-16, 3.993798362933309143, 3.024842911000705570 ) ) ;
#27151=CARTESIAN_POINT ( 'NONE',  ( 23.11000000136559507, -3.156283516753370044, -0.9349337715887220401 ) ) ;
#27169=ORIENTED_EDGE ( 'NONE', *, *, #28166, .T. ) ;
#27176=ORIENTED_EDGE ( 'NONE', *, *, #14113, .T. ) ;
#27180=CARTESIAN_POINT ( 'NONE',  ( 25.75999999999999801, -2.208672634433321348E-15, 0.000000000000000000 ) ) ;
#27196=CARTESIAN_POINT ( 'NONE',  ( -4.104821569165014520E-16, -4.787500056513378510, 1.476463073999619846 ) ) ;
#27205=VECTOR ( 'NONE', #28307, 1000.000000000000114 ) ;
#27206=CARTESIAN_POINT ( 'NONE',  ( 25.54750000136559507, 1.913930629741522838, -2.363507492473150062 ) ) ;
#27208=CARTESIAN_POINT ( 'NONE',  ( 25.75999999999999446, 1.400653562255665729, 2.728866609423114209 ) ) ;
#27209=DIRECTION ( 'NONE',  ( -1.000000000000000000, 8.574039729943022041E-17, 6.162975822039154730E-33 ) ) ;
#27214=SHAPE_DEFINITION_REPRESENTATION ( #2877, #13 ) ;
#27219=PLANE ( 'NONE',  #16010 ) ;
#27221=FACE_OUTER_BOUND ( 'NONE', #21712, .T. ) ;
#27225=DIRECTION ( 'NONE',  ( 1.000000000000000000, -0.000000000000000000, -0.000000000000000000 ) ) ;
#27226=CARTESIAN_POINT ( 'NONE',  ( 24.42249999999999943, -2.378061970571983430, 1.291182301015471712 ) ) ;
#27234=ORIENTED_EDGE ( 'NONE', *, *, #28848, .T. ) ;
#27237=ORIENTED_EDGE ( 'NONE', *, *, #31726, .F. ) ;
#27238=EDGE_CURVE ( 'NONE', #24661, #23691, #21705, .T. ) ;
#27240=EDGE_CURVE ( 'NONE', #2902, #4647, #10649, .T. ) ;
#27243=CARTESIAN_POINT ( 'NONE',  ( 25.36000000136559507, -1.570731468192933633, -2.892927487894330962 ) ) ;
#27244=AXIS2_PLACEMENT_3D ( 'NONE', #1234, #26623, #31824 ) ;
#27247=CARTESIAN_POINT ( 'NONE',  ( 25.23499999999999943, 0.2613211581691317065, 2.486304738420681559 ) ) ;
#27249=LINE ( 'NONE', #16891, #7088 ) ;
#27252=AXIS2_PLACEMENT_3D ( 'NONE', #19520, #32899, #30376 ) ;
#27256=CARTESIAN_POINT ( 'NONE',  ( 4.262285728429960179E-16, 4.971152295393301834, 0.6226916219172224931 ) ) ;
#27257=DIRECTION ( 'NONE',  ( -7.770718973608995913E-17, -0.9063077870366526012, 0.4226182617406938902 ) ) ;
#27260=DIRECTION ( 'NONE',  ( -1.000000000000000000, 8.574039729943022041E-17, -0.000000000000000000 ) ) ;
#27272=EDGE_CURVE ( 'NONE', #16013, #17299, #26892, .T. ) ;
#27276=AXIS2_PLACEMENT_3D ( 'NONE', #3644, #8643, #16480 ) ;
#27282=ORIENTED_EDGE ( 'NONE', *, *, #25687, .F. ) ;
#27284=EDGE_CURVE ( 'NONE', #6630, #12161, #1987, .T. ) ;
#27285=AXIS2_PLACEMENT_3D ( 'NONE', #30636, #31116, #26248 ) ;
#27287=CARTESIAN_POINT ( 'NONE',  ( 25.54750000136559507, 3.024605502323846729, -0.3178988483021056854 ) ) ;
#27290=LINE ( 'NONE', #4410, #29477 ) ;
#27298=CIRCLE ( 'NONE', #1155, 5.009999999999999787 ) ;
#27300=CARTESIAN_POINT ( 'NONE',  ( 3.529825581556955655E-16, 4.116875700062116117, -2.376879293651021019 ) ) ;
#27301=ORIENTED_EDGE ( 'NONE', *, *, #21991, .F. ) ;
#27307=ORIENTED_EDGE ( 'NONE', *, *, #1372, .T. ) ;
#27310=CARTESIAN_POINT ( 'NONE',  ( 10.00000000000000178, -4.616489984850518979, -1.946309384392642228 ) ) ;
#27313=CARTESIAN_POINT ( 'NONE',  ( 21.04750000136559507, -3.024605502323851169, 0.3178988483021052969 ) ) ;
#27324=CARTESIAN_POINT ( 'NONE',  ( 22.73500000136559862, 1.570731468192929858, 2.892927487894329186 ) ) ;
#27325=DIRECTION ( 'NONE',  ( 8.281886410780514724E-17, 0.9659258262890692004, -0.2588190451025176309 ) ) ;
#27333=VECTOR ( 'NONE', #31027, 1000.000000000000000 ) ;
#27337=CARTESIAN_POINT ( 'NONE',  ( 23.61000000273119070, -1.573300977624594976, 1.942864903642425700 ) ) ;
#27361=CARTESIAN_POINT ( 'NONE',  ( 10.00000000000000178, 3.993798362933351775, -3.024842911000649615 ) ) ;
#27364=PLANE ( 'NONE',  #21386 ) ;
#27366=EDGE_CURVE ( 'NONE', #7714, #29657, #12765, .T. ) ;
#27367=FACE_OUTER_BOUND ( 'NONE', #9535, .T. ) ;
#27377=CARTESIAN_POINT ( 'NONE',  ( 10.00000000000000000, -1.476463073999670472, 4.787500056513361635 ) ) ;
#27390=AXIS2_PLACEMENT_3D ( 'NONE', #21966, #32193, #5662 ) ;
#27399=CARTESIAN_POINT ( 'NONE',  ( -3.830085165118302378E-16, -4.467071865485461757, -1.625881193364742572 ) ) ;
#27411=VERTEX_POINT ( 'NONE', #26002 ) ;
#27414=CARTESIAN_POINT ( 'NONE',  ( 24.60999999999999943, -1.942864903642428587, -1.573300977624592756 ) ) ;
#27416=CARTESIAN_POINT ( 'NONE',  ( 21.42249999999999943, -2.378061970571983430, 1.291182301015471712 ) ) ;
#27422=DIRECTION ( 'NONE',  ( 1.000000000000000000, -8.574039729943018344E-17, -0.000000000000000000 ) ) ;
#27434=ADVANCED_FACE ( 'NONE', ( #918 ), #7093, .F. ) ;
#27456=ORIENTED_EDGE ( 'NONE', *, *, #23, .F. ) ;
#27475=VERTEX_POINT ( 'NONE', #20661 ) ;
#27476=CARTESIAN_POINT ( 'NONE',  ( 25.75999999999999801, -2.208672634433321348E-15, 0.000000000000000000 ) ) ;
#27482=CARTESIAN_POINT ( 'NONE',  ( 25.75999999999999801, -2.208672634433321348E-15, 0.000000000000000000 ) ) ;
#27483=VERTEX_POINT ( 'NONE', #26154 ) ;
#27487=ADVANCED_FACE ( 'NONE', ( #15796 ), #30866, .F. ) ;
#27489=DIRECTION ( 'NONE',  ( 0.000000000000000000, -0.8191520442889951292, 0.5735764363510412744 ) ) ;
#27501=CARTESIAN_POINT ( 'NONE',  ( 23.79750000136559507, 0.3178988483021036315, 3.024605502323848949 ) ) ;
#27520=FACE_OUTER_BOUND ( 'NONE', #26579, .T. ) ;
#27522=EDGE_LOOP ( 'NONE', ( #23197, #18064, #2618, #22711 ) ) ;
#27526=EDGE_CURVE ( 'NONE', #61, #32887, #13119, .T. ) ;
#27527=EDGE_LOOP ( 'NONE', ( #22430, #28612, #6501, #20717 ) ) ;
#27528=DIRECTION ( 'NONE',  ( -7.023442172597881513E-17, -0.8191520442889946851, 0.5735764363510420516 ) ) ;
#27533=DIRECTION ( 'NONE',  ( 4.917867153433058194E-17, 0.5735764363510524877, -0.8191520442889873577 ) ) ;
#27537=LINE ( 'NONE', #2474, #13493 ) ;
#27539=ORIENTED_EDGE ( 'NONE', *, *, #23778, .T. ) ;
#27542=LINE ( 'NONE', #3996, #23002 ) ;
#27546=DIRECTION ( 'NONE',  ( 8.574039729943018344E-17, 1.000000000000000000, 0.000000000000000000 ) ) ;
#27550=FACE_OUTER_BOUND ( 'NONE', #24235, .T. ) ;
#27555=( BOUNDED_CURVE ( )  B_SPLINE_CURVE ( 2, ( #17034, #6526, #22395, #24402, #32611, #1521, #9190, #27243, #27083, #4185, #22089, #14353, #4360, #14538, #1873, #1684, #22245, #11880, #32304, #19573, #2023, #6848, #19729, #29929, #12195, #17542, #23067, #30278, #2524, #5528, #25568, #15529, #13184, #23242, #188, #23386, #15363, #15027, #30431, #10180, #25247, #13041, #30784, #28089, #2678, #12846, #8009, #7510, #32951, #27922, #10368, #5035, #28415, #347, #7855, #20232, #2368, #10520, #30933, #20733, #15716, #18050, #20403, #15213, #7735, #25416, #12691, #22896, #17712, #28238, #12542, #30618, #7701, #17896, #25921, #27739, #5187, #3029, #9870 ),
 .UNSPECIFIED., .F., .F. ) 
 B_SPLINE_CURVE_WITH_KNOTS ( ( 3, 2, 2, 2, 2, 2, 2, 2, 2, 2, 2, 2, 2, 2, 2, 2, 2, 2, 2, 2, 2, 2, 2, 2, 2, 2, 2, 2, 2, 2, 2, 2, 2, 2, 2, 2, 2, 2, 2, 3 ),
 ( 0.03266179187250656257, 0.05000000000000000278, 0.07499999999999999722, 0.1000000000000000056, 0.1250000000000000000, 0.1499999999999999944, 0.1749999999999999889, 0.2000000000000000111, 0.2250000000000000056, 0.2500000000000000000, 0.2750000000000000222, 0.2999999999999999889, 0.3250000000000000111, 0.3499999999999999778, 0.3749999999999999445, 0.4000000000000000222, 0.4249999999999999889, 0.4500000000000000111, 0.4749999999999999778, 0.5000000000000000000, 0.5250000000000000222, 0.5500000000000000444, 0.5749999999999999556, 0.5999999999999998668, 0.6250000000000000000, 0.6499999999999999112, 0.6750000000000000444, 0.6999999999999999556, 0.7249999999999998668, 0.7500000000000000000, 0.7749999999999999112, 0.8000000000000000444, 0.8249999999999999556, 0.8499999999999998668, 0.8750000000000000000, 0.8999999999999999112, 0.9250000000000000444, 0.9499999999999999556, 0.9749999999999998668, 1.000000000000000000 ),
 .UNSPECIFIED. ) 
 CURVE ( )  GEOMETRIC_REPRESENTATION_ITEM ( )  RATIONAL_B_SPLINE_CURVE ( ( 0.9676416783621977213, 0.9472082996767436924, 1.000000000000000000, 0.9238795325112867385, 1.000000000000000000, 0.9238795325112867385, 1.000000000000000000, 0.9238795325112867385, 1.000000000000000000, 0.9238795325112867385, 1.000000000000000000, 0.9238795325112867385, 1.000000000000000000, 0.9238795325112867385, 1.000000000000000000, 0.9238795325112867385, 1.000000000000000000, 0.9238795325112867385, 1.000000000000000000, 0.9238795325112867385, 1.000000000000000000, 0.9238795325112867385, 1.000000000000000000, 0.9238795325112867385, 1.000000000000000000, 0.9238795325112867385, 1.000000000000000000, 0.9238795325112867385, 1.000000000000000000, 0.9238795325112867385, 1.000000000000000000, 0.9238795325112867385, 1.000000000000000000, 0.9238795325112867385, 1.000000000000000000, 0.9238795325112867385, 1.000000000000000000, 0.9238795325112867385, 1.000000000000000000, 0.9238795325112867385, 1.000000000000000000, 0.9238795325112867385, 1.000000000000000000, 0.9238795325112867385, 1.000000000000000000, 0.9238795325112867385, 1.000000000000000000, 0.9238795325112867385, 1.000000000000000000, 0.9238795325112867385, 1.000000000000000000, 0.9238795325112867385, 1.000000000000000000, 0.9238795325112867385, 1.000000000000000000, 0.9238795325112867385, 1.000000000000000000, 0.9238795325112867385, 1.000000000000000000, 0.9238795325112867385, 1.000000000000000000, 0.9238795325112867385, 1.000000000000000000, 0.9238795325112867385, 1.000000000000000000, 0.9238795325112867385, 1.000000000000000000, 0.9238795325112867385, 1.000000000000000000, 0.9238795325112867385, 1.000000000000000000, 0.9238795325112867385, 1.000000000000000000, 0.9238795325112867385, 1.000000000000000000, 0.9238795325112867385, 1.000000000000000000, 0.9238795325112867385, 1.000000000000000000 ) ) 
 REPRESENTATION_ITEM ( '' )  );
#27556=DIRECTION ( 'NONE',  ( 0.5150380749100547106, 0.000000000000000000, -0.8571673007021120005 ) ) ;
#27558=ADVANCED_FACE ( 'NONE', ( #11436, #16779 ), #24122, .T. ) ;
#27570=ORIENTED_EDGE ( 'NONE', *, *, #23541, .T. ) ;
#27573=CARTESIAN_POINT ( 'NONE',  ( 24.11000000136559862, -2.892927487894331406, 1.570731468192932301 ) ) ;
#27579=DIRECTION ( 'NONE',  ( 0.000000000000000000, 1.000000000000000000, 0.000000000000000000 ) ) ;
#27582=ORIENTED_EDGE ( 'NONE', *, *, #29612, .F. ) ;
#27595=DIRECTION ( 'NONE',  ( 0.000000000000000000, 0.000000000000000000, -1.000000000000000000 ) ) ;
#27600=CARTESIAN_POINT ( 'NONE',  ( 10.56183597391177464, -4.753758587302148619, 0.000000000000000000 ) ) ;
#27624=DIRECTION ( 'NONE',  ( 2.219124775574837589E-17, 0.2588190451025108585, 0.9659258262890709767 ) ) ;
#27625=CARTESIAN_POINT ( 'NONE',  ( 25.11000000136559507, -3.156283516753370044, -0.9349337715887220401 ) ) ;
#27626=ADVANCED_FACE ( 'NONE', ( #21946 ), #9244, .T. ) ;
#27627=CARTESIAN_POINT ( 'NONE',  ( 10.00000000000000178, -0.6226916219171699796, -4.971152295393309828 ) ) ;
#27630=VERTEX_POINT ( 'NONE', #19282 ) ;
#27631=FACE_OUTER_BOUND ( 'NONE', #21371, .T. ) ;
#27637=FACE_OUTER_BOUND ( 'NONE', #24607, .T. ) ;
#27641=VERTEX_POINT ( 'NONE', #19469 ) ;
#27645=ORIENTED_EDGE ( 'NONE', *, *, #20577, .F. ) ;
#27646=CARTESIAN_POINT ( 'NONE',  ( 22.86000000136559862, -0.9349337715887247047, 3.156283516753367824 ) ) ;
#27647=ORIENTED_EDGE ( 'NONE', *, *, #1425, .T. ) ;
#27648=CARTESIAN_POINT ( 'NONE',  ( 4.104821569165004659E-16, 4.787500056513366076, 1.476463073999653819 ) ) ;
#27653=CARTESIAN_POINT ( 'NONE',  ( 10.55147673363118876, -2.376879293651094294, 4.116875700062075261 ) ) ;
#27662=CARTESIAN_POINT ( 'NONE',  ( 23.50111451137534857, -3.256483526998273983E-15, 2.499999999999998668 ) ) ;
#27671=CARTESIAN_POINT ( 'NONE',  ( 10.55147673363118876, -4.116875700062067267, -2.376879293651108060 ) ) ;
#27684=DIRECTION ( 'NONE',  ( -2.219124775574993204E-17, -0.2588190451025284555, 0.9659258262890663138 ) ) ;
#27687=CARTESIAN_POINT ( 'NONE',  ( 0.000000000000000000, 0.000000000000000000, 0.000000000000000000 ) ) ;
#27720=CARTESIAN_POINT ( 'NONE',  ( 23.73500000136559152, 3.156283516753366047, 0.9349337715887203748 ) ) ;
#27721=CARTESIAN_POINT ( 'NONE',  ( 10.00000000000000000, 0.8254815157535239090, 4.681538312723519724 ) ) ;
#27726=AXIS2_PLACEMENT_3D ( 'NONE', #23876, #6165, #26890 ) ;
#27738=EDGE_CURVE ( 'NONE', #14263, #32276, #6817, .T. ) ;
#27739=CARTESIAN_POINT ( 'NONE',  ( 21.11000000136559507, -2.892927487894331406, 1.570731468192932523 ) ) ;
#27742=FACE_OUTER_BOUND ( 'NONE', #15734, .T. ) ;
#27757=EDGE_LOOP ( 'NONE', ( #23930, #4558, #13052, #7198 ) ) ;
#27771=ORIENTED_EDGE ( 'NONE', *, *, #10428, .F. ) ;
#27777=CARTESIAN_POINT ( 'NONE',  ( 24.67250000136559507, 2.363507492473148286, 1.913930629741525058 ) ) ;
#27778=EDGE_CURVE ( 'NONE', #32682, #22025, #14323, .T. ) ;
#27793=VECTOR ( 'NONE', #28568, 1000.000000000000114 ) ;
#27800=VECTOR ( 'NONE', #17744, 1000.000000000000000 ) ;
#27805=ORIENTED_EDGE ( 'NONE', *, *, #30829, .F. ) ;
#27808=ORIENTED_EDGE ( 'NONE', *, *, #1838, .T. ) ;
#27811=ORIENTED_EDGE ( 'NONE', *, *, #568, .F. ) ;
#27815=LINE ( 'NONE', #25328, #32237 ) ;
#27822=AXIS2_PLACEMENT_3D ( 'NONE', #29568, #16671, #1822 ) ;
#27827=CARTESIAN_POINT ( 'NONE',  ( 22.75111450864416085, -1.241879311143409511E-16, -2.499999999999998668 ) ) ;
#27859=CARTESIAN_POINT ( 'NONE',  ( 10.00000000000000000, -0.2499999999999472089, -5.003758587302151284 ) ) ;
#27863=CARTESIAN_POINT ( 'NONE',  ( 21.48500000273118715, 0.2613211581691317065, 2.486304738420681559 ) ) ;
#27876=ORIENTED_EDGE ( 'NONE', *, *, #23034, .F. ) ;
#27880=CARTESIAN_POINT ( 'NONE',  ( 23.48500000136559862, 0.9349337715887185984, -3.156283516753368268 ) ) ;
#27900=VECTOR ( 'NONE', #2565, 1000.000000000000000 ) ;
#27904=CARTESIAN_POINT ( 'NONE',  ( 10.57125986779756843, -0.8254815157534942660, -4.681538312723525053 ) ) ;
#27905=VECTOR ( 'NONE', #14171, 1000.000000000000000 ) ;
#27906=CARTESIAN_POINT ( 'NONE',  ( 24.48500000136559507, 0.9349337715887185984, -3.156283516753368268 ) ) ;
#27907=AXIS2_PLACEMENT_3D ( 'NONE', #29977, #7071, #2063 ) ;
#27910=ORIENTED_EDGE ( 'NONE', *, *, #22336, .F. ) ;
#27914=CARTESIAN_POINT ( 'NONE',  ( 10.56870887191539587, -1.625881193364669297, -4.467071865485488402 ) ) ;
#27922=CARTESIAN_POINT ( 'NONE',  ( 22.73500000136559862, 3.156283516753366047, 0.9349337715887203748 ) ) ;
#27934=CIRCLE ( 'NONE', #1815, 5.009999999999999787 ) ;
#27941=EDGE_LOOP ( 'NONE', ( #6343, #29911, #18971, #6590 ) ) ;
#27944=ORIENTED_EDGE ( 'NONE', *, *, #9460, .T. ) ;
#27945=EDGE_CURVE ( 'NONE', #28295, #29275, #29048, .T. ) ;
#27946=ORIENTED_EDGE ( 'NONE', *, *, #29823, .T. ) ;
#27966=CARTESIAN_POINT ( 'NONE',  ( 22.86000000136559507, -0.9349337715887248157, 3.156283516753367824 ) ) ;
#27974=CARTESIAN_POINT ( 'NONE',  ( 9.560873106162060372E-17, 1.115095498423308351, 4.884328206559839458 ) ) ;
#27987=ORIENTED_EDGE ( 'NONE', *, *, #26769, .F. ) ;
#28006=AXIS2_PLACEMENT_3D ( 'NONE', #3954, #9937, #19999 ) ;
#28007=LINE ( 'NONE', #22963, #1123 ) ;
#28023=ORIENTED_EDGE ( 'NONE', *, *, #13748, .T. ) ;
#28026=CIRCLE ( 'NONE', #20568, 5.009999999999999787 ) ;
#28041=CARTESIAN_POINT ( 'NONE',  ( 10.52034268205830614, 3.055657119358800244, 3.641590349731939735 ) ) ;
#28043=ORIENTED_EDGE ( 'NONE', *, *, #5783, .F. ) ;
#28048=LINE ( 'NONE', #10318, #15153 ) ;
#28058=CARTESIAN_POINT ( 'NONE',  ( 22.67250000136559507, 3.024605502323846729, -0.3178988483021056854 ) ) ;
#28072=ORIENTED_EDGE ( 'NONE', *, *, #22254, .F. ) ;
#28075=CARTESIAN_POINT ( 'NONE',  ( 23.79750000136559507, 2.363507492473148286, 1.913930629741525058 ) ) ;
#28080=CARTESIAN_POINT ( 'NONE',  ( 10.55147673363119232, -2.376879293651037006, -4.116875700062107235 ) ) ;
#28089=CARTESIAN_POINT ( 'NONE',  ( 23.11000000136559862, -2.892927487894331406, 1.570731468192932523 ) ) ;
#28090=EDGE_CURVE ( 'NONE', #7526, #7281, #9288, .T. ) ;
#28105=VERTEX_POINT ( 'NONE', #4272 ) ;
#28112=CARTESIAN_POINT ( 'NONE',  ( 22.05656763645045260, 0.8852964313267434049, -2.499999999999998224 ) ) ;
#28117=CARTESIAN_POINT ( 'NONE',  ( 21.04750000136559507, -1.913930629741527500, 2.363507492473149618 ) ) ;
#28124=CARTESIAN_POINT ( 'NONE',  ( 22.54750000136559507, 3.024605502323846729, -0.3178988483021056854 ) ) ;
#28128=ORIENTED_EDGE ( 'NONE', *, *, #2985, .T. ) ;
#28141=DIRECTION ( 'NONE',  ( -7.472768010111142456E-18, -0.08715574274765799934, -0.9961946980917455452 ) ) ;
#28146=ORIENTED_EDGE ( 'NONE', *, *, #10169, .F. ) ;
#28166=EDGE_CURVE ( 'NONE', #5237, #26955, #22678, .T. ) ;
#28180=ORIENTED_EDGE ( 'NONE', *, *, #26158, .F. ) ;
#28184=LINE ( 'NONE', #3126, #603 ) ;
#28185=CARTESIAN_POINT ( 'NONE',  ( 10.52034268205830614, -3.993798362933330015, 3.024842911000676704 ) ) ;
#28186=VERTEX_POINT ( 'NONE', #30717 ) ;
#28192=ORIENTED_EDGE ( 'NONE', *, *, #20016, .F. ) ;
#28203=ORIENTED_EDGE ( 'NONE', *, *, #1440, .F. ) ;
#28212=EDGE_CURVE ( 'NONE', #30361, #14569, #32710, .T. ) ;
#28222=DIRECTION ( 'NONE',  ( 8.574039729943018344E-17, 1.000000000000000000, 0.000000000000000000 ) ) ;
#28223=LINE ( 'NONE', #12677, #9656 ) ;
#28225=CARTESIAN_POINT ( 'NONE',  ( 22.04750000136559507, -1.913930629741527500, 2.363507492473149618 ) ) ;
#28227=DIRECTION ( 'NONE',  ( 7.023442172597885211E-17, 0.8191520442889951292, -0.5735764363510412744 ) ) ;
#28228=EDGE_LOOP ( 'NONE', ( #7312, #8689, #4031, #11592 ) ) ;
#28232=CARTESIAN_POINT ( 'NONE',  ( 21.80656763371926488, 0.8852964313267427388, -2.499999999999999112 ) ) ;
#28238=CARTESIAN_POINT ( 'NONE',  ( 21.48500000136559507, 0.9349337715887185984, -3.156283516753368268 ) ) ;
#28241=CARTESIAN_POINT ( 'NONE',  ( 10.56870887191539587, -1.625881193364728805, 4.467071865485467086 ) ) ;
#28259=CARTESIAN_POINT ( 'NONE',  ( -1.394036994807634510E-16, -1.625881193364727917, 4.467071865485467086 ) ) ;
#28262=DIRECTION ( 'NONE',  ( 0.000000000000000000, 1.000000000000000000, 0.000000000000000000 ) ) ;
#28268=CARTESIAN_POINT ( 'NONE',  ( 23.54750000136559507, 3.024605502323846729, -0.3178988483021056854 ) ) ;
#28273=CARTESIAN_POINT ( 'NONE',  ( 21.54750000136559507, 3.024605502323846729, -0.3178988483021056854 ) ) ;
#28286=DIRECTION ( 'NONE',  ( 1.000000000000000000, -8.574039729943018344E-17, -0.000000000000000000 ) ) ;
#28291=CARTESIAN_POINT ( 'NONE',  ( 10.55147673363118876, -4.208382051008173974, -2.718385644597219208 ) ) ;
#28294=FACE_OUTER_BOUND ( 'NONE', #32713, .T. ) ;
#28295=VERTEX_POINT ( 'NONE', #20506 ) ;
#28297=DIRECTION ( 'NONE',  ( 1.000000000000000000, -0.000000000000000000, -0.000000000000000000 ) ) ;
#28298=EDGE_CURVE ( 'NONE', #9752, #5237, #728, .T. ) ;
#28301=CIRCLE ( 'NONE', #13343, 5.009999999999999787 ) ;
#28307=DIRECTION ( 'NONE',  ( 7.770718973608924422E-17, 0.9063077870366440525, 0.4226182617407120978 ) ) ;
#28310=CARTESIAN_POINT ( 'NONE',  ( 10.52034268205830614, -3.024842911000663825, -3.993798362933340229 ) ) ;
#28313=CARTESIAN_POINT ( 'NONE',  ( 10.00000000000000000, -4.467071865485484850, 1.625881193364682620 ) ) ;
#28338=VERTEX_POINT ( 'NONE', #16107 ) ;
#28343=CARTESIAN_POINT ( 'NONE',  ( 10.00000000000000178, -8.574039729943018837E-16, 0.000000000000000000 ) ) ;
#28347=LINE ( 'NONE', #28686, #3712 ) ;
#28355=CIRCLE ( 'NONE', #32641, 5.999999999999999112 ) ;
#28363=VECTOR ( 'NONE', #32724, 1000.000000000000000 ) ;
#28365=LINE ( 'NONE', #23349, #18258 ) ;
#28366=CARTESIAN_POINT ( 'NONE',  ( 22.61000000273118715, -1.573300977624594976, 1.942864903642425700 ) ) ;
#28387=VECTOR ( 'NONE', #3896, 1000.000000000000114 ) ;
#28390=CIRCLE ( 'NONE', #21441, 5.009999999999999787 ) ;
#28391=CARTESIAN_POINT ( 'NONE',  ( 10.56870887191539587, -4.467071865485462645, -1.625881193364742572 ) ) ;
#28394=ORIENTED_EDGE ( 'NONE', *, *, #28752, .F. ) ;
#28397=DIRECTION ( 'NONE',  ( -1.000000000000000000, 8.574039729943018344E-17, 0.000000000000000000 ) ) ;
#28404=DIRECTION ( 'NONE',  ( 1.000000000000000000, -8.574039729943018344E-17, -0.000000000000000000 ) ) ;
#28415=CARTESIAN_POINT ( 'NONE',  ( 22.54750000136559507, 1.913930629741522838, -2.363507492473150062 ) ) ;
#28419=FACE_OUTER_BOUND ( 'NONE', #26891, .T. ) ;
#28430=VECTOR ( 'NONE', #26595, 1000.000000000000000 ) ;
#28438=VECTOR ( 'NONE', #21444, 1000.000000000000114 ) ;
#28449=CARTESIAN_POINT ( 'NONE',  ( -2.143509932485295136E-17, -0.2499999999999467648, -5.003758587302151284 ) ) ;
#28452=CARTESIAN_POINT ( 'NONE',  ( 21.36000000136559507, 0.9349337715887185984, -3.156283516753368268 ) ) ;
#28453=DIRECTION ( 'NONE',  ( 1.000000000000000000, -8.574039729943018344E-17, -0.000000000000000000 ) ) ;
#28462=CARTESIAN_POINT ( 'NONE',  ( 21.98500000136559507, -2.892927487894331406, 1.570731468192932301 ) ) ;
#28473=EDGE_CURVE ( 'NONE', #15697, #7137, #31199, .T. ) ;
#28489=DIRECTION ( 'NONE',  ( -7.770718973608921957E-17, -0.9063077870366440525, -0.4226182617407121533 ) ) ;
#28500=CARTESIAN_POINT ( 'NONE',  ( 1.394036994807660394E-16, 1.625881193364758337, -4.467071865485455540 ) ) ;
#28501=DIRECTION ( 'NONE',  ( -4.917867153432989168E-17, -0.5735764363510442720, -0.8191520442889931308 ) ) ;
#28504=LINE ( 'NONE', #28802, #3313 ) ;
#28508=AXIS2_PLACEMENT_3D ( 'NONE', #6420, #29025, #29516 ) ;
#28515=EDGE_CURVE ( 'NONE', #32366, #8466, #20914, .T. ) ;
#28516=DIRECTION ( 'NONE',  ( 0.000000000000000000, 0.000000000000000000, -1.000000000000000000 ) ) ;
#28523=ORIENTED_EDGE ( 'NONE', *, *, #9947, .T. ) ;
#28529=CARTESIAN_POINT ( 'NONE',  ( 23.11000000000000298, 1.942864903642424146, 1.573300977624592534 ) ) ;
#28531=ORIENTED_EDGE ( 'NONE', *, *, #18077, .T. ) ;
#28534=CARTESIAN_POINT ( 'NONE',  ( 3.148734258548781612E-16, 3.672404558090038851, 3.407865132560194077 ) ) ;
#28548=EDGE_CURVE ( 'NONE', #10880, #22618, #30680, .T. ) ;
#28568=DIRECTION ( 'NONE',  ( 7.472768010110236499E-18, 0.08715574274764813223, 0.9961946980917464334 ) ) ;
#28571=ORIENTED_EDGE ( 'NONE', *, *, #26498, .T. ) ;
#28575=CARTESIAN_POINT ( 'NONE',  ( 22.23500000136559862, -3.156283516753370044, -0.9349337715887220401 ) ) ;
#28577=ORIENTED_EDGE ( 'NONE', *, *, #8760, .F. ) ;
#28583=VERTEX_POINT ( 'NONE', #9746 ) ;
#28585=DIRECTION ( 'NONE',  ( 0.000000000000000000, -0.9961946980917461003, 0.08715574274765118534 ) ) ;
#28591=DIRECTION ( 'NONE',  ( 7.472768010111415168E-18, 0.08715574274766135776, -0.9961946980917453232 ) ) ;
#28594=ORIENTED_EDGE ( 'NONE', *, *, #2324, .F. ) ;
#28600=EDGE_CURVE ( 'NONE', #22010, #19432, #17946, .T. ) ;
#28602=ORIENTED_EDGE ( 'NONE', *, *, #18621, .F. ) ;
#28612=ORIENTED_EDGE ( 'NONE', *, *, #21033, .T. ) ;
#28623=CARTESIAN_POINT ( 'NONE',  ( 21.67250000136559507, 2.363507492473148286, 1.913930629741525058 ) ) ;
#28633=DIRECTION ( 'NONE',  ( -7.472768010110877448E-18, -0.08715574274765462703, -0.9961946980917457672 ) ) ;
#28644=EDGE_LOOP ( 'NONE', ( #20728, #10826, #29261, #897 ) ) ;
#28645=ORIENTED_EDGE ( 'NONE', *, *, #10429, .F. ) ;
#28650=ORIENTED_EDGE ( 'NONE', *, *, #22060, .T. ) ;
#28651=DIRECTION ( 'NONE',  ( 1.000000000000000000, -8.574039729943018344E-17, -0.000000000000000000 ) ) ;
#28655=LINE ( 'NONE', #30856, #8193 ) ;
#28667=CARTESIAN_POINT ( 'NONE',  ( 23.86000000136559507, 1.570731468192929858, 2.892927487894329186 ) ) ;
#28668=CARTESIAN_POINT ( 'NONE',  ( 25.49905227492783766, -1.632004223636194684, -2.257790968203141624 ) ) ;
#28669=DIRECTION ( 'NONE',  ( 0.000000000000000000, 1.000000000000000000, 0.000000000000000000 ) ) ;
#28670=ORIENTED_EDGE ( 'NONE', *, *, #27738, .T. ) ;
#28680=CARTESIAN_POINT ( 'NONE',  ( 24.61000000136559152, 3.156283516753366047, 0.9349337715887203748 ) ) ;
#28681=ORIENTED_EDGE ( 'NONE', *, *, #26966, .T. ) ;
#28686=CARTESIAN_POINT ( 'NONE',  ( 10.00000000000000000, 0.8254815157535864145, -4.681538312723508177 ) ) ;
#28687=EDGE_CURVE ( 'NONE', #15557, #11002, #8059, .T. ) ;
#28694=CARTESIAN_POINT ( 'NONE',  ( 10.55147673363119232, 4.116875700062115229, -2.376879293651021019 ) ) ;
#28699=CARTESIAN_POINT ( 'NONE',  ( 10.00000000000000178, -4.458382051008212166, 2.285372942704935628 ) ) ;
#28718=ORIENTED_EDGE ( 'NONE', *, *, #28166, .F. ) ;
#28733=DIRECTION ( 'NONE',  ( -4.917867153432990401E-17, -0.5735764363510447161, -0.8191520442889927978 ) ) ;
#28752=EDGE_CURVE ( 'NONE', #30689, #2062, #7456, .T. ) ;
#28762=CARTESIAN_POINT ( 'NONE',  ( 21.17250000136559507, -2.363507492473152283, -1.913930629741525280 ) ) ;
#28763=CARTESIAN_POINT ( 'NONE',  ( -3.608283490412349620E-16, -4.208382051008211278, 2.718385644597158812 ) ) ;
#28766=EDGE_CURVE ( 'NONE', #28105, #6480, #23602, .T. ) ;
#28768=CARTESIAN_POINT ( 'NONE',  ( 22.79750000273118715, -2.594547506269383685, -0.7685399846772043020 ) ) ;
#28775=ORIENTED_EDGE ( 'NONE', *, *, #1258, .F. ) ;
#28786=ORIENTED_EDGE ( 'NONE', *, *, #9329, .T. ) ;
#28797=ADVANCED_FACE ( 'NONE', ( #5185 ), #20081, .T. ) ;
#28799=DIRECTION ( 'NONE',  ( 0.000000000000000000, 1.000000000000000000, 0.000000000000000000 ) ) ;
#28802=CARTESIAN_POINT ( 'NONE',  ( -2.619932554246537343E-16, -3.055657119358776264, -3.641590349731960163 ) ) ;
#28803=CARTESIAN_POINT ( 'NONE',  ( 10.00000000000000000, 1.625881193364757449, -4.467071865485455540 ) ) ;
#28815=CARTESIAN_POINT ( 'NONE',  ( 23.92250000136559507, 0.3178988483021036315, 3.024605502323848949 ) ) ;
#28827=LINE ( 'NONE', #16438, #3731 ) ;
#28833=AXIS2_PLACEMENT_3D ( 'NONE', #5216, #5377, #20760 ) ;
#28837=CARTESIAN_POINT ( 'NONE',  ( 21.79750000273118715, -2.594547506269383685, -0.7685399846772043020 ) ) ;
#28840=DIRECTION ( 'NONE',  ( 3.623545766764145597E-17, 0.4226182617406914477, 0.9063077870366536004 ) ) ;
#28848=EDGE_CURVE ( 'NONE', #32470, #27641, #20293, .T. ) ;
#28854=CARTESIAN_POINT ( 'NONE',  ( 21.48499999999999943, -2.486304738420683780, 0.2613211581691335383 ) ) ;
#28887=CARTESIAN_POINT ( 'NONE',  ( 10.56183597391177464, 5.003758587302147731, 0.2500000000000008882 ) ) ;
#28892=VECTOR ( 'NONE', #510, 1000.000000000000114 ) ;
#28895=VECTOR ( 'NONE', #5027, 1000.000000000000000 ) ;
#28925=ORIENTED_EDGE ( 'NONE', *, *, #11876, .T. ) ;
#28930=CARTESIAN_POINT ( 'NONE',  ( 20.98500000136559862, -2.892927487894331406, 1.570731468192932301 ) ) ;
#28931=VECTOR ( 'NONE', #6722, 999.9999999999998863 ) ;
#28933=ORIENTED_EDGE ( 'NONE', *, *, #25553, .T. ) ;
#28935=B_SPLINE_CURVE_WITH_KNOTS ( 'NONE', 3,
 ( #15906, #18261, #20279, #25617, #26116, #12906, #30483, #17769, #30679, #10725 ),
 .UNSPECIFIED., .F., .F.,
 ( 4, 2, 2, 2, 4 ),
 ( 3.252606517456513302E-19, 0.0009730977530606437073, 0.001946195506121287198, 0.002919293259181930580, 0.003892391012242573962 ),
 .UNSPECIFIED. ) ;
#28936=VECTOR ( 'NONE', #28489, 1000.000000000000000 ) ;
#28937=DIRECTION ( 'NONE',  ( -3.623545766764141283E-17, -0.4226182617406913922, -0.9063077870366536004 ) ) ;
#28938=CARTESIAN_POINT ( 'NONE',  ( 23.17250000273118715, 2.378061970571979433, -1.291182301015470824 ) ) ;
#28943=VECTOR ( 'NONE', #24511, 1000.000000000000114 ) ;
#28947=AXIS2_PLACEMENT_3D ( 'NONE', #22781, #2560, #5071 ) ;
#28950=ORIENTED_EDGE ( 'NONE', *, *, #19200, .T. ) ;
#28952=VECTOR ( 'NONE', #18962, 1000.000000000000000 ) ;
#28953=VECTOR ( 'NONE', #24701, 1000.000000000000000 ) ;
#28957=CARTESIAN_POINT ( 'NONE',  ( 25.75999999999999801, -2.208672634433321348E-15, -2.499999999999997780 ) ) ;
#28967=ADVANCED_FACE ( 'NONE', ( #24992 ), #19509, .F. ) ;
#28969=DIRECTION ( 'NONE',  ( 1.000000000000000000, -8.574039729943018344E-17, -0.000000000000000000 ) ) ;
#28988=CARTESIAN_POINT ( 'NONE',  ( -7.077711312404032898E-17, -0.8254815157534933778, -4.681538312723525053 ) ) ;
#28992=ORIENTED_EDGE ( 'NONE', *, *, #22420, .T. ) ;
#28998=ORIENTED_EDGE ( 'NONE', *, *, #13931, .T. ) ;
#28999=CIRCLE ( 'NONE', #8706, 5.009999999999999787 ) ;
#29001=CARTESIAN_POINT ( 'NONE',  ( 25.29462333114494044, -1.188618013303065268, 2.273567320650588641 ) ) ;
#29006=ADVANCED_FACE ( 'NONE', ( #27520 ), #24840, .F. ) ;
#29009=ORIENTED_EDGE ( 'NONE', *, *, #6346, .F. ) ;
#29015=DIRECTION ( 'NONE',  ( 0.000000000000000000, 0.08715574274766894891, -0.9961946980917446570 ) ) ;
#29024=CARTESIAN_POINT ( 'NONE',  ( 10.56870887191539587, 1.625881193364696831, 4.467071865485476856 ) ) ;
#29025=DIRECTION ( 'NONE',  ( 6.062761635205510427E-17, 0.7071067811865392461, 0.7071067811865558994 ) ) ;
#29039=CARTESIAN_POINT ( 'NONE',  ( 24.17249999999999943, 1.291182301015469047, 2.378061970571981654 ) ) ;
#29043=DIRECTION ( 'NONE',  ( -1.000000000000000000, 8.574039729943018344E-17, -0.000000000000000000 ) ) ;
#29048=LINE ( 'NONE', #15977, #1810 ) ;
#29059=EDGE_CURVE ( 'NONE', #24998, #17028, #1605, .T. ) ;
#29062=DIRECTION ( 'NONE',  ( 1.000000000000000000, -8.574039729943018344E-17, -0.000000000000000000 ) ) ;
#29070=ORIENTED_EDGE ( 'NONE', *, *, #24429, .F. ) ;
#29076=DIRECTION ( 'NONE',  ( 1.000000000000000000, -0.000000000000000000, -0.000000000000000000 ) ) ;
#29079=PLANE ( 'NONE',  #27726 ) ;
#29080=EDGE_CURVE ( 'NONE', #13277, #4411, #1959, .T. ) ;
#29090=ORIENTED_EDGE ( 'NONE', *, *, #13748, .F. ) ;
#29096=DIRECTION ( 'NONE',  ( 1.000000000000000000, -8.574039729943018344E-17, -0.000000000000000000 ) ) ;
#29101=CARTESIAN_POINT ( 'NONE',  ( 25.73499999999999943, -0.2613211581691358698, -2.486304738420681559 ) ) ;
#29102=CARTESIAN_POINT ( 'NONE',  ( 10.00000000000000000, 2.376879293651121383, -4.116875700062057497 ) ) ;
#29106=CARTESIAN_POINT ( 'NONE',  ( 4.262285728429967575E-16, 4.971152295393310716, -0.6226916219171529931 ) ) ;
#29114=FACE_OUTER_BOUND ( 'NONE', #4001, .T. ) ;
#29115=CARTESIAN_POINT ( 'NONE',  ( 21.48500000273118715, 0.2613211581691317065, 2.486304738420681559 ) ) ;
#29124=CARTESIAN_POINT ( 'NONE',  ( 0.000000000000000000, 0.000000000000000000, 0.000000000000000000 ) ) ;
#29133=ORIENTED_EDGE ( 'NONE', *, *, #9066, .T. ) ;
#29141=DIRECTION ( 'NONE',  ( 0.000000000000000000, 1.000000000000000000, 0.000000000000000000 ) ) ;
#29155=CARTESIAN_POINT ( 'NONE',  ( 25.43504868974586941, -2.579632542568791376, -0.8162045923261349589 ) ) ;
#29163=CARTESIAN_POINT ( 'NONE',  ( 10.55147673363119054, 4.116875700062082366, 2.376879293651078751 ) ) ;
#29165=CARTESIAN_POINT ( 'NONE',  ( 23.17250000000000298, 1.291182301015469047, 2.378061970571981654 ) ) ;
#29168=PLANE ( 'NONE',  #19851 ) ;
#29183=LINE ( 'NONE', #24161, #9294 ) ;
#29188=CARTESIAN_POINT ( 'NONE',  ( 10.00000000000000000, -2.376879293651094294, 4.116875700062075261 ) ) ;
#29204=DIRECTION ( 'NONE',  ( 0.000000000000000000, 1.000000000000000000, 0.000000000000000000 ) ) ;
#29233=( BOUNDED_CURVE ( )  B_SPLINE_CURVE ( 2, ( #7154, #30560, #27863, #9819, #7302, #5141, #30891, #9974, #25369, #2807, #10477 ),
 .UNSPECIFIED., .F., .F. ) 
 B_SPLINE_CURVE_WITH_KNOTS ( ( 3, 2, 2, 2, 2, 3 ),
 ( 0.7966116191895004084, 0.8000000000000000444, 0.8249999999999999556, 0.8499999999999999778, 0.8750000000000000000, 0.8966116191895003862 ),
 .UNSPECIFIED. ) 
 CURVE ( )  GEOMETRIC_REPRESENTATION_ITEM ( )  RATIONAL_B_SPLINE_CURVE ( ( 0.9821626249036858880, 0.9896829947469992783, 1.000000000000000000, 0.9238795325112867385, 1.000000000000000000, 0.9238795325112867385, 1.000000000000000000, 0.9238795325112867385, 1.000000000000000000, 0.9341965377642874602, 0.9821626249036858880 ) ) 
 REPRESENTATION_ITEM ( '' )  );
#29247=ORIENTED_EDGE ( 'NONE', *, *, #26530, .T. ) ;
#29248=EDGE_LOOP ( 'NONE', ( #32217, #1930, #24568, #14639 ) ) ;
#29251=CARTESIAN_POINT ( 'NONE',  ( 25.48499999999999943, -2.486304738420683780, 0.2613211581691335383 ) ) ;
#29261=ORIENTED_EDGE ( 'NONE', *, *, #30008, .F. ) ;
#29262=CARTESIAN_POINT ( 'NONE',  ( 21.17250000273118715, 2.378061970571979433, -1.291182301015470824 ) ) ;
#29263=LINE ( 'NONE', #31453, #1199 ) ;
#29266=CARTESIAN_POINT ( 'NONE',  ( 10.00000000000000000, 4.116875700062082366, 2.376879293651078751 ) ) ;
#29275=VERTEX_POINT ( 'NONE', #26161 ) ;
#29287=CARTESIAN_POINT ( 'NONE',  ( 25.75999999999999801, 2.805042440084548172, 1.132414195126726364 ) ) ;
#29303=FACE_OUTER_BOUND ( 'NONE', #25622, .T. ) ;
#29306=CARTESIAN_POINT ( 'NONE',  ( 25.23500000000000654, 2.486304733690583912, -0.2613212031729839624 ) ) ;
#29307=CARTESIAN_POINT ( 'NONE',  ( 10.00000000000000000, -4.884328206559844787, 1.115095498423292364 ) ) ;
#29312=ADVANCED_FACE ( 'NONE', ( #11443 ), #6400, .F. ) ;
#29319=CARTESIAN_POINT ( 'NONE',  ( 25.29750000136559507, -0.3178988483021076838, -3.024605502323848949 ) ) ;
#29324=ORIENTED_EDGE ( 'NONE', *, *, #10873, .F. ) ;
#29334=CARTESIAN_POINT ( 'NONE',  ( 2.593512329575641137E-16, 3.024842911000690471, 3.993798362933319357 ) ) ;
#29338=DIRECTION ( 'NONE',  ( 1.000000000000000000, -8.574039729943018344E-17, -0.000000000000000000 ) ) ;
#29359=DIRECTION ( 'NONE',  ( 0.000000000000000000, 1.000000000000000000, 0.000000000000000000 ) ) ;
#29368=AXIS2_PLACEMENT_3D ( 'NONE', #26920, #11685, #10165 ) ;
#29375=FACE_OUTER_BOUND ( 'NONE', #8360, .T. ) ;
#29384=ADVANCED_FACE ( 'NONE', ( #22453 ), #22643, .F. ) ;
#29385=CARTESIAN_POINT ( 'NONE',  ( 20.50111451137534857, -3.256483526998273983E-15, 2.499999999999998668 ) ) ;
#29389=VECTOR ( 'NONE', #10047, 1000.000000000000000 ) ;
#29411=CARTESIAN_POINT ( 'NONE',  ( 25.04750000000000298, 2.594547506269380133, 0.7685399846772031918 ) ) ;
#29430=CARTESIAN_POINT ( 'NONE',  ( 21.42250000273118715, 1.291182301015469047, 2.378061970571981654 ) ) ;
#29446=DIRECTION ( 'NONE',  ( 1.000000000000000000, -0.000000000000000000, -0.000000000000000000 ) ) ;
#29450=CIRCLE ( 'NONE', #15559, 2.499999999999998224 ) ;
#29456=ORIENTED_EDGE ( 'NONE', *, *, #4138, .F. ) ;
#29461=CIRCLE ( 'NONE', #24126, 5.009999999999999787 ) ;
#29465=CARTESIAN_POINT ( 'NONE',  ( 10.00000000000000000, 2.376879293651063652, 4.116875700062091248 ) ) ;
#29467=PLANE ( 'NONE',  #18757 ) ;
#29474=CARTESIAN_POINT ( 'NONE',  ( 10.52034268205830614, -3.055657119358777152, -3.641590349731960163 ) ) ;
#29475=DIRECTION ( 'NONE',  ( -6.062761635205655873E-17, -0.7071067811865558994, 0.7071067811865392461 ) ) ;
#29477=VECTOR ( 'NONE', #29480, 1000.000000000000000 ) ;
#29480=DIRECTION ( 'NONE',  ( -1.000000000000000000, 8.574039729943018344E-17, 0.000000000000000000 ) ) ;
#29481=VERTEX_POINT ( 'NONE', #15592 ) ;
#29487=EDGE_LOOP ( 'NONE', ( #5351, #4712, #24768, #16405 ) ) ;
#29501=CARTESIAN_POINT ( 'NONE',  ( 21.42250000136559507, 1.913930629741522838, -2.363507492473150062 ) ) ;
#29505=ORIENTED_EDGE ( 'NONE', *, *, #28212, .T. ) ;
#29510=ORIENTED_EDGE ( 'NONE', *, *, #6525, .F. ) ;
#29516=DIRECTION ( 'NONE',  ( 0.000000000000000000, -0.7071067811865558994, 0.7071067811865392461 ) ) ;
#29517=VECTOR ( 'NONE', #24890, 1000.000000000000000 ) ;
#29520=LINE ( 'NONE', #21979, #19286 ) ;
#29525=FACE_BOUND ( 'NONE', #27078, .T. ) ;
#29530=VECTOR ( 'NONE', #5269, 1000.000000000000000 ) ;
#29534=VECTOR ( 'NONE', #14321, 1000.000000000000000 ) ;
#29535=VECTOR ( 'NONE', #9193, 1000.000000000000000 ) ;
#29558=CARTESIAN_POINT ( 'NONE',  ( 1.394036994807608625E-16, 1.625881193364697719, 4.467071865485476856 ) ) ;
#29563=CARTESIAN_POINT ( 'NONE',  ( 25.75181271650331993, 2.887405513829538251, 0.9065264845798409743 ) ) ;
#29568=CARTESIAN_POINT ( 'NONE',  ( 25.75999999999999801, -2.208672634433321348E-15, 0.000000000000000000 ) ) ;
#29572=DIRECTION ( 'NONE',  ( 0.000000000000000000, 0.7071067811865465735, 0.7071067811865484609 ) ) ;
#29579=FACE_OUTER_BOUND ( 'NONE', #27941, .T. ) ;
#29596=ORIENTED_EDGE ( 'NONE', *, *, #11444, .F. ) ;
#29600=CARTESIAN_POINT ( 'NONE',  ( 23.92249999999999943, 2.378061970571979433, -1.291182301015470824 ) ) ;
#29608=EDGE_CURVE ( 'NONE', #14457, #24661, #24096, .T. ) ;
#29610=DIRECTION ( 'NONE',  ( -1.000000000000000000, 8.574039729943017111E-17, -0.000000000000000000 ) ) ;
#29612=EDGE_CURVE ( 'NONE', #19939, #21907, #3225, .T. ) ;
#29637=ORIENTED_EDGE ( 'NONE', *, *, #10065, .F. ) ;
#29645=DIRECTION ( 'NONE',  ( -1.000000000000000000, 8.574039729943022041E-17, -1.232595164407830946E-32 ) ) ;
#29647=EDGE_CURVE ( 'NONE', #18404, #21855, #1031, .T. ) ;
#29657=VERTEX_POINT ( 'NONE', #8250 ) ;
#29659=CYLINDRICAL_SURFACE ( 'NONE', #30031, 5.010000000000000675 ) ;
#29670=CARTESIAN_POINT ( 'NONE',  ( 10.00000000000000178, -8.574039729943018837E-16, 0.000000000000000000 ) ) ;
#29675=CARTESIAN_POINT ( 'NONE',  ( 23.73500000136559507, 1.570731468192929858, 2.892927487894329630 ) ) ;
#29680=DIRECTION ( 'NONE',  ( 0.000000000000000000, 1.000000000000000000, 0.000000000000000000 ) ) ;
#29685=CARTESIAN_POINT ( 'NONE',  ( 24.92250000136559507, -1.913930629741527500, 2.363507492473149618 ) ) ;
#29689=PLANE ( 'NONE',  #6115 ) ;
#29690=DIRECTION ( 'NONE',  ( 8.574039729943018344E-17, 1.000000000000000000, 0.000000000000000000 ) ) ;
#29694=ADVANCED_FACE ( 'NONE', ( #1210 ), #13385, .T. ) ;
#29696=ORIENTED_EDGE ( 'NONE', *, *, #23763, .T. ) ;
#29698=DIRECTION ( 'NONE',  ( 1.000000000000000000, -0.000000000000000000, -0.000000000000000000 ) ) ;
#29717=B_SPLINE_CURVE_WITH_KNOTS ( 'NONE', 3,
 ( #9311, #8966, #26693, #4297, #31748, #29723, #11997, #11496, #24356, #32057, #16989, #1627, #27036, #14476, #3810, #24686, #29563, #32249 ),
 .UNSPECIFIED., .F., .F.,
 ( 4, 2, 2, 2, 2, 2, 2, 2, 4 ),
 ( 0.008622242838676193177, 0.009334878258772234122, 0.01004751367886827507, 0.01076014909896431601, 0.01147278451906035696, 0.01218541993915639790, 0.01289805535925243885, 0.01361069077934847805, 0.01432332619944451900 ),
 .UNSPECIFIED. ) ;
#29719=ORIENTED_EDGE ( 'NONE', *, *, #17517, .T. ) ;
#29723=CARTESIAN_POINT ( 'NONE',  ( 25.62190975187500896, 1.596356670451427817, -2.417129575599294533 ) ) ;
#29733=DIRECTION ( 'NONE',  ( 0.000000000000000000, 1.000000000000000000, 0.000000000000000000 ) ) ;
#29736=EDGE_LOOP ( 'NONE', ( #26544, #31081, #4214, #29090 ) ) ;
#29738=CARTESIAN_POINT ( 'NONE',  ( 25.86000000136559862, 1.570731468192929858, 2.892927487894329186 ) ) ;
#29755=CARTESIAN_POINT ( 'NONE',  ( 24.04749999999999943, 2.594547506269380133, 0.7685399846772031918 ) ) ;
#29762=CARTESIAN_POINT ( 'NONE',  ( 10.00000000000000000, -4.467071865485484850, 1.625881193364682620 ) ) ;
#29763=ORIENTED_EDGE ( 'NONE', *, *, #9947, .F. ) ;
#29765=ORIENTED_EDGE ( 'NONE', *, *, #18500, .T. ) ;
#29768=APPLICATION_CONTEXT ( 'configuration controlled 3d designs of mechanical parts and assemblies' ) ;
#29794=EDGE_LOOP ( 'NONE', ( #16990, #19116, #26070, #23736 ) ) ;
#29798=CARTESIAN_POINT ( 'NONE',  ( 25.75999999999999801, 2.788229309062804084, 1.188575764268269053 ) ) ;
#29800=CARTESIAN_POINT ( 'NONE',  ( 25.75999999999999801, 5.999999999999997335, 0.000000000000000000 ) ) ;
#29801=CARTESIAN_POINT ( 'NONE',  ( 22.42250000000000298, -2.378061970571983430, 1.291182301015471490 ) ) ;
#29803=DIRECTION ( 'NONE',  ( 8.574039729943018344E-17, 1.000000000000000000, 0.000000000000000000 ) ) ;
#29808=LINE ( 'NONE', #4217, #9682 ) ;
#29809=CARTESIAN_POINT ( 'NONE',  ( 23.29750000136559862, -0.3178988483021076838, -3.024605502323848949 ) ) ;
#29814=LINE ( 'NONE', #25107, #10292 ) ;
#29821=ORIENTED_EDGE ( 'NONE', *, *, #5859, .F. ) ;
#29823=EDGE_CURVE ( 'NONE', #9887, #19305, #32673, .T. ) ;
#29831=CARTESIAN_POINT ( 'NONE',  ( 22.36000000136559507, 0.9349337715887185984, -3.156283516753368268 ) ) ;
#29840=CARTESIAN_POINT ( 'NONE',  ( 24.17250000136559507, -2.363507492473152283, -1.913930629741525280 ) ) ;
#29889=VERTEX_POINT ( 'NONE', #30910 ) ;
#29896=LINE ( 'NONE', #32269, #11946 ) ;
#29907=VECTOR ( 'NONE', #28227, 1000.000000000000000 ) ;
#29908=DIRECTION ( 'NONE',  ( 0.000000000000000000, 0.5735764363510558184, -0.8191520442889850262 ) ) ;
#29911=ORIENTED_EDGE ( 'NONE', *, *, #17541, .T. ) ;
#29913=CYLINDRICAL_SURFACE ( 'NONE', #14994, 2.499999999999997780 ) ;
#29914=CARTESIAN_POINT ( 'NONE',  ( 24.23499999999999943, 0.2613211581691317065, 2.486304738420681559 ) ) ;
#29918=VERTEX_POINT ( 'NONE', #23519 ) ;
#29922=CARTESIAN_POINT ( 'NONE',  ( -2.619932554246537343E-16, -3.055657119358776264, -3.641590349731960163 ) ) ;
#29929=CARTESIAN_POINT ( 'NONE',  ( 24.36000000136559507, -1.570731468192933633, -2.892927487894330962 ) ) ;
#29934=DIRECTION ( 'NONE',  ( 0.000000000000000000, 1.000000000000000000, 0.000000000000000000 ) ) ;
#29953=VECTOR ( 'NONE', #18144, 1000.000000000000000 ) ;
#29962=VECTOR ( 'NONE', #28397, 1000.000000000000000 ) ;
#29963=DIRECTION ( 'NONE',  ( 4.917867153433014437E-17, 0.5735764363510474917, -0.8191520442889907994 ) ) ;
#29968=VECTOR ( 'NONE', #27260, 1000.000000000000000 ) ;
#29977=CARTESIAN_POINT ( 'NONE',  ( 10.52034268205830614, -3.641590349731950393, 3.055657119358789142 ) ) ;
#29978=AXIS2_PLACEMENT_3D ( 'NONE', #2958, #30348, #7419 ) ;
#29979=EDGE_CURVE ( 'NONE', #21128, #3186, #12364, .T. ) ;
#29980=CARTESIAN_POINT ( 'NONE',  ( 25.75999999999999801, -2.208672634433321348E-15, 0.000000000000000000 ) ) ;
#29983=CIRCLE ( 'NONE', #6447, 5.000000000000003553 ) ;
#29989=ORIENTED_EDGE ( 'NONE', *, *, #5515, .F. ) ;
#30001=CARTESIAN_POINT ( 'NONE',  ( 23.67250000136559507, 2.363507492473148286, 1.913930629741525058 ) ) ;
#30004=CARTESIAN_POINT ( 'NONE',  ( 10.56870887191539587, 4.467071865485493731, -1.625881193364653088 ) ) ;
#30006=DIRECTION ( 'NONE',  ( 7.472768010111444442E-18, 0.08715574274766196838, -0.9961946980917452121 ) ) ;
#30008=EDGE_CURVE ( 'NONE', #15630, #2062, #30536, .T. ) ;
#30011=CARTESIAN_POINT ( 'NONE',  ( 23.86000000136559507, -0.9349337715887248157, 3.156283516753367824 ) ) ;
#30014=CIRCLE ( 'NONE', #19870, 5.010000000000000675 ) ;
#30031=AXIS2_PLACEMENT_3D ( 'NONE', #29980, #24443, #17280 ) ;
#30043=CARTESIAN_POINT ( 'NONE',  ( 0.000000000000000000, 0.000000000000000000, 0.000000000000000000 ) ) ;
#30059=AXIS2_PLACEMENT_3D ( 'NONE', #4021, #6681, #12032 ) ;
#30066=CARTESIAN_POINT ( 'NONE',  ( -3.529825581556942343E-16, -4.116875700062099241, 2.376879293651050329 ) ) ;
#30074=VECTOR ( 'NONE', #28591, 999.9999999999998863 ) ;
#30075=CARTESIAN_POINT ( 'NONE',  ( 1.394036994807660394E-16, 1.625881193364758337, -4.467071865485455540 ) ) ;
#30083=EDGE_LOOP ( 'NONE', ( #26949, #21542, #13690, #12372 ) ) ;
#30091=CARTESIAN_POINT ( 'NONE',  ( 10.00000000000000178, 5.003758587302149508, 0.2500000000000014988 ) ) ;
#30108=DIRECTION ( 'NONE',  ( 1.000000000000000000, -8.574039729943018344E-17, -0.000000000000000000 ) ) ;
#30111=CARTESIAN_POINT ( 'NONE',  ( 25.54750000136559507, 1.913930629741522838, -2.363507492473150062 ) ) ;
#30117=DIRECTION ( 'NONE',  ( -7.770718973609008239E-17, -0.9063077870366540445, 0.4226182617406906705 ) ) ;
#30130=LINE ( 'NONE', #24756, #31154 ) ;
#30147=EDGE_LOOP ( 'NONE', ( #20048, #589 ) ) ;
#30148=EDGE_CURVE ( 'NONE', #16254, #17299, #668, .T. ) ;
#30162=DIRECTION ( 'NONE',  ( -8.541412920197222280E-17, -0.9961946980917462113, 0.08715574274765119922 ) ) ;
#30163=LINE ( 'NONE', #14895, #17180 ) ;
#30164=CARTESIAN_POINT ( 'NONE',  ( 23.48500000136559862, 2.892927487894327410, -1.570731468192931635 ) ) ;
#30166=DIRECTION ( 'NONE',  ( 0.000000000000000000, 1.000000000000000000, 0.000000000000000000 ) ) ;
#30179=EDGE_CURVE ( 'NONE', #30672, #7133, #23816, .T. ) ;
#30181=DIRECTION ( 'NONE',  ( -1.000000000000000000, 8.574039729943022041E-17, -1.232595164407830946E-32 ) ) ;
#30183=ORIENTED_EDGE ( 'NONE', *, *, #31283, .T. ) ;
#30185=CARTESIAN_POINT ( 'NONE',  ( 20.98500000136559862, -2.892927487894331406, 1.570731468192932523 ) ) ;
#30190=ORIENTED_EDGE ( 'NONE', *, *, #10994, .T. ) ;
#30194=CARTESIAN_POINT ( 'NONE',  ( 10.00000000000000000, 1.946309384392590491, 4.616489984850538519 ) ) ;
#30210=DIRECTION ( 'NONE',  ( 7.770718973608956470E-17, 0.9063077870366479383, 0.4226182617407038267 ) ) ;
#30211=VERTEX_POINT ( 'NONE', #14257 ) ;
#30216=EDGE_CURVE ( 'NONE', #25185, #13681, #8771, .T. ) ;
#30235=EDGE_CURVE ( 'NONE', #12555, #13277, #19880, .T. ) ;
#30250=DIRECTION ( 'NONE',  ( -1.000000000000000000, 8.574039729943022041E-17, -1.232595164407830946E-32 ) ) ;
#30256=ADVANCED_FACE ( 'NONE', ( #17597 ), #1928, .F. ) ;
#30257=CARTESIAN_POINT ( 'NONE',  ( 10.57125986779756843, -1.115095498423276155, -4.884328206559847452 ) ) ;
#30262=DIRECTION ( 'NONE',  ( 1.000000000000000000, -8.574039729943018344E-17, -0.000000000000000000 ) ) ;
#30264=CARTESIAN_POINT ( 'NONE',  ( 25.48500000136559862, 0.9349337715887185984, -3.156283516753368268 ) ) ;
#30267=ORIENTED_EDGE ( 'NONE', *, *, #21218, .F. ) ;
#30271=CARTESIAN_POINT ( 'NONE',  ( 22.24290772321994325, 0.1310194482076003919, 2.499999999999998668 ) ) ;
#30275=EDGE_CURVE ( 'NONE', #5926, #6901, #14915, .T. ) ;
#30278=CARTESIAN_POINT ( 'NONE',  ( 24.11000000136559507, -2.892927487894331406, 1.570731468192932523 ) ) ;
#30289=EDGE_LOOP ( 'NONE', ( #8807, #15654, #2030, #16225 ) ) ;
#30290=CARTESIAN_POINT ( 'NONE',  ( 10.00000000000000178, 3.672404558090038851, 3.407865132560194521 ) ) ;
#30299=CARTESIAN_POINT ( 'NONE',  ( 3.529825581556927552E-16, 4.116875700062083254, 2.376879293651078751 ) ) ;
#30310=LINE ( 'NONE', #20117, #23059 ) ;
#30311=CARTESIAN_POINT ( 'NONE',  ( 23.73500000136559152, 1.570731468192929858, 2.892927487894329186 ) ) ;
#30318=CARTESIAN_POINT ( 'NONE',  ( 10.52034268205830259, 3.055657119358849094, -3.641590349731898879 ) ) ;
#30321=EDGE_CURVE ( 'NONE', #13159, #3186, #32508, .T. ) ;
#30329=ORIENTED_EDGE ( 'NONE', *, *, #9978, .F. ) ;
#30334=CARTESIAN_POINT ( 'NONE',  ( 10.56870887191539587, -4.616489984850518979, -1.946309384392639119 ) ) ;
#30348=DIRECTION ( 'NONE',  ( 1.000000000000000000, -8.574039729943018344E-17, -0.000000000000000000 ) ) ;
#30356=ORIENTED_EDGE ( 'NONE', *, *, #1191, .F. ) ;
#30361=VERTEX_POINT ( 'NONE', #10251 ) ;
#30365=ORIENTED_EDGE ( 'NONE', *, *, #18827, .F. ) ;
#30376=DIRECTION ( 'NONE',  ( 0.000000000000000000, 1.000000000000000000, 0.000000000000000000 ) ) ;
#30378=DIRECTION ( 'NONE',  ( -8.541412920197213652E-17, -0.9961946980917453232, -0.08715574274766135776 ) ) ;
#30382=CARTESIAN_POINT ( 'NONE',  ( 10.56870887191539587, -1.625881193364728805, 4.467071865485467086 ) ) ;
#30387=DIRECTION ( 'NONE',  ( 4.917867153433085927E-17, 0.5735764363510558184, -0.8191520442889850262 ) ) ;
#30394=CARTESIAN_POINT ( 'NONE',  ( 21.67250000136559507, 3.024605502323846729, -0.3178988483021056854 ) ) ;
#30399=VERTEX_POINT ( 'NONE', #2578 ) ;
#30407=DIRECTION ( 'NONE',  ( -1.000000000000000000, 8.574039729943019576E-17, 0.000000000000000000 ) ) ;
#30412=DIRECTION ( 'NONE',  ( -2.219124775575025560E-17, -0.2588190451025318972, 0.9659258262890653146 ) ) ;
#30413=CARTESIAN_POINT ( 'NONE',  ( 22.54750000136559507, 1.913930629741522838, -2.363507492473150062 ) ) ;
#30418=DIRECTION ( 'NONE',  ( 1.000000000000000000, -8.574039729943018344E-17, -0.000000000000000000 ) ) ;
#30421=LINE ( 'NONE', #5026, #6513 ) ;
#30423=VERTEX_POINT ( 'NONE', #18273 ) ;
#30431=CARTESIAN_POINT ( 'NONE',  ( 23.42250000136559862, -0.3178988483021076838, -3.024605502323848949 ) ) ;
#30434=CARTESIAN_POINT ( 'NONE',  ( 25.17249999999999233, 1.291182301015473710, 2.378061970571975436 ) ) ;
#30435=DIRECTION ( 'NONE',  ( -3.623545766764170865E-17, -0.4226182617406944453, -0.9063077870366522681 ) ) ;
#30440=AXIS2_PLACEMENT_3D ( 'NONE', #25414, #22895, #14589 ) ;
#30443=LINE ( 'NONE', #9527, #7521 ) ;
#30444=ORIENTED_EDGE ( 'NONE', *, *, #30216, .F. ) ;
#30445=ADVANCED_FACE ( 'NONE', ( #31965 ), #10920, .F. ) ;
#30449=CARTESIAN_POINT ( 'NONE',  ( 0.000000000000000000, 0.000000000000000000, 0.000000000000000000 ) ) ;
#30451=ORIENTED_EDGE ( 'NONE', *, *, #21248, .T. ) ;
#30457=DIRECTION ( 'NONE',  ( -1.000000000000000000, 8.574039729943019576E-17, -0.000000000000000000 ) ) ;
#30464=ORIENTED_EDGE ( 'NONE', *, *, #11602, .F. ) ;
#30468=VECTOR ( 'NONE', #9894, 999.9999999999998863 ) ;
#30469=CARTESIAN_POINT ( 'NONE',  ( 10.56870887191539587, -4.467071865485462645, -1.625881193364742572 ) ) ;
#30470=CARTESIAN_POINT ( 'NONE',  ( 25.61000000136559507, 3.156283516753366047, 0.9349337715887203748 ) ) ;
#30475=VECTOR ( 'NONE', #23294, 1000.000000000000000 ) ;
#30483=CARTESIAN_POINT ( 'NONE',  ( 25.42231079161887308, 2.505942517978533957, 1.022343137445100636 ) ) ;
#30487=ORIENTED_EDGE ( 'NONE', *, *, #19096, .T. ) ;
#30510=LINE ( 'NONE', #12263, #9805 ) ;
#30520=DIRECTION ( 'NONE',  ( -1.000000000000000000, 8.574039729943018344E-17, -0.000000000000000000 ) ) ;
#30521=FACE_OUTER_BOUND ( 'NONE', #8884, .T. ) ;
#30523=VECTOR ( 'NONE', #31401, 1000.000000000000000 ) ;
#30536=LINE ( 'NONE', #2611, #27333 ) ;
#30545=ORIENTED_EDGE ( 'NONE', *, *, #12479, .T. ) ;
#30547=DIRECTION ( 'NONE',  ( 0.000000000000000000, 0.9063077870366468280, 0.4226182617407062136 ) ) ;
#30558=AXIS2_PLACEMENT_3D ( 'NONE', #5740, #28969, #16259 ) ;
#30560=CARTESIAN_POINT ( 'NONE',  ( 21.49290772595112387, 0.1310194482076003919, 2.499999999999998668 ) ) ;
#30563=CARTESIAN_POINT ( 'NONE',  ( 3.122314033877864698E-16, 3.641590349731929965, 3.055657119358814011 ) ) ;
#30566=DIRECTION ( 'NONE',  ( 7.472768010110837389E-18, 0.08715574274765461316, 0.9961946980917457672 ) ) ;
#30578=CARTESIAN_POINT ( 'NONE',  ( 23.29750000136559862, -2.363507492473152283, -1.913930629741525280 ) ) ;
#30584=CARTESIAN_POINT ( 'NONE',  ( 10.52034268205830614, 3.993798362933350887, -3.024842911000649615 ) ) ;
#30592=VECTOR ( 'NONE', #2546, 1000.000000000000000 ) ;
#30597=VECTOR ( 'NONE', #32069, 1000.000000000000114 ) ;
#30601=CARTESIAN_POINT ( 'NONE',  ( 25.36000000136559862, -1.570731468192933633, -2.892927487894330074 ) ) ;
#30605=ORIENTED_EDGE ( 'NONE', *, *, #5248, .T. ) ;
#30618=CARTESIAN_POINT ( 'NONE',  ( 21.36000000136559507, -1.570731468192933633, -2.892927487894330962 ) ) ;
#30636=CARTESIAN_POINT ( 'NONE',  ( 25.75999999999999801, -2.208672634433321348E-15, 0.000000000000000000 ) ) ;
#30637=ORIENTED_EDGE ( 'NONE', *, *, #1411, .T. ) ;
#30639=ORIENTED_EDGE ( 'NONE', *, *, #31970, .F. ) ;
#30647=PLANE ( 'NONE',  #31048 ) ;
#30657=CARTESIAN_POINT ( 'NONE',  ( 23.23500000136559862, -1.570731468192933633, -2.892927487894330074 ) ) ;
#30662=ORIENTED_EDGE ( 'NONE', *, *, #25289, .F. ) ;
#30667=CARTESIAN_POINT ( 'NONE',  ( 23.73500000273118715, -2.486304738420683780, 0.2613211581691335383 ) ) ;
#30672=VERTEX_POINT ( 'NONE', #1706 ) ;
#30673=DIRECTION ( 'NONE',  ( 8.281886410780543074E-17, 0.9659258262890716429, -0.2588190451025081940 ) ) ;
#30679=CARTESIAN_POINT ( 'NONE',  ( 25.28110583668922473, 2.565906573285401393, 0.05495561580884226333 ) ) ;
#30680=LINE ( 'NONE', #9915, #3438 ) ;
#30689=VERTEX_POINT ( 'NONE', #7220 ) ;
#30698=ORIENTED_EDGE ( 'NONE', *, *, #13931, .F. ) ;
#30700=CARTESIAN_POINT ( 'NONE',  ( 21.23499999999999943, 0.2613211581691317065, 2.486304738420681559 ) ) ;
#30715=ORIENTED_EDGE ( 'NONE', *, *, #14280, .F. ) ;
#30717=CARTESIAN_POINT ( 'NONE',  ( 3.958196854299272687E-16, 4.616489984850558947, -1.946309384392544972 ) ) ;
#30728=ORIENTED_EDGE ( 'NONE', *, *, #9242, .F. ) ;
#30747=CARTESIAN_POINT ( 'NONE',  ( 10.00000000000000000, 4.681538312723528605, -0.8254815157534771686 ) ) ;
#30752=ORIENTED_EDGE ( 'NONE', *, *, #10140, .F. ) ;
#30778=DIRECTION ( 'NONE',  ( -1.000000000000000000, 8.574039729943017111E-17, -3.081487911019577365E-33 ) ) ;
#30780=ORIENTED_EDGE ( 'NONE', *, *, #3466, .F. ) ;
#30784=CARTESIAN_POINT ( 'NONE',  ( 23.17250000136559862, -3.024605502323851169, 0.3178988483021052969 ) ) ;
#30794=EDGE_CURVE ( 'NONE', #17553, #30211, #11349, .T. ) ;
#30801=EDGE_LOOP ( 'NONE', ( #32718, #19537, #4418, #30698 ) ) ;
#30810=CARTESIAN_POINT ( 'NONE',  ( 22.17250000273118715, 2.378061970571979433, -1.291182301015470602 ) ) ;
#30811=ORIENTED_EDGE ( 'NONE', *, *, #23669, .T. ) ;
#30815=CARTESIAN_POINT ( 'NONE',  ( 25.29750000136559507, -0.3178988483021076838, -3.024605502323848949 ) ) ;
#30822=CARTESIAN_POINT ( 'NONE',  ( 21.04750000136559507, -3.024605502323851169, 0.3178988483021052969 ) ) ;
#30823=CARTESIAN_POINT ( 'NONE',  ( 22.00111451137534502, -1.241879311143409511E-16, -2.499999999999998668 ) ) ;
#30829=EDGE_CURVE ( 'NONE', #29275, #5198, #13352, .T. ) ;
#30836=EDGE_CURVE ( 'NONE', #15946, #5049, #25771, .T. ) ;
#30840=ORIENTED_EDGE ( 'NONE', *, *, #32900, .F. ) ;
#30854=CARTESIAN_POINT ( 'NONE',  ( 4.285194126261599773E-30, 4.979297819079224069E-14, -4.753758587302147731 ) ) ;
#30856=CARTESIAN_POINT ( 'NONE',  ( 10.00000000000000000, -3.055657119358826446, 3.641590349731918863 ) ) ;
#30858=FACE_OUTER_BOUND ( 'NONE', #316, .T. ) ;
#30860=CARTESIAN_POINT ( 'NONE',  ( 10.55147673363118876, -2.718385644597205442, 4.208382051008182856 ) ) ;
#30865=ADVANCED_FACE ( 'NONE', ( #1351 ), #26434, .F. ) ;
#30866=PLANE ( 'NONE',  #17235 ) ;
#30879=ORIENTED_EDGE ( 'NONE', *, *, #23541, .F. ) ;
#30884=PLANE ( 'NONE',  #17072 ) ;
#30891=CARTESIAN_POINT ( 'NONE',  ( 21.23500000273118715, 2.486304738420679783, -0.2613211581691337604 ) ) ;
#30897=CARTESIAN_POINT ( 'NONE',  ( 23.80656763371926843, 0.8852964313267427388, -2.499999999999999112 ) ) ;
#30905=CARTESIAN_POINT ( 'NONE',  ( -3.424298583717139316E-16, -3.993798362933287383, -3.024842911000732215 ) ) ;
#30910=CARTESIAN_POINT ( 'NONE',  ( -1.265925305626697234E-16, -1.476463073999670028, 4.787500056513361635 ) ) ;
#30928=ORIENTED_EDGE ( 'NONE', *, *, #1566, .T. ) ;
#30929=EDGE_CURVE ( 'NONE', #10505, #10948, #8361, .T. ) ;
#30933=CARTESIAN_POINT ( 'NONE',  ( 22.17250000136559507, -3.024605502323851169, 0.3178988483021052969 ) ) ;
#30936=LINE ( 'NONE', #2528, #25787 ) ;
#30948=ORIENTED_EDGE ( 'NONE', *, *, #4698, .F. ) ;
#30950=FACE_OUTER_BOUND ( 'NONE', #20790, .T. ) ;
#30965=EDGE_CURVE ( 'NONE', #15944, #31023, #22063, .T. ) ;
#30967=CARTESIAN_POINT ( 'NONE',  ( 22.11000000136559507, -3.156283516753370044, -0.9349337715887220401 ) ) ;
#30977=( BOUNDED_CURVE ( )  B_SPLINE_CURVE ( 2, ( #16997, #11505, #4312, #26889, #24700, #12501, #33057, #32568, #15171, #19863, #20538 ),
 .UNSPECIFIED., .F., .F. ) 
 B_SPLINE_CURVE_WITH_KNOTS ( ( 3, 2, 2, 2, 2, 3 ),
 ( 0.1966116191895003751, 0.2000000000000000111, 0.2250000000000000056, 0.2500000000000000000, 0.2750000000000000222, 0.2966116191895003529 ),
 .UNSPECIFIED. ) 
 CURVE ( )  GEOMETRIC_REPRESENTATION_ITEM ( )  RATIONAL_B_SPLINE_CURVE ( ( 0.9821626249036858880, 0.9896829947469992783, 1.000000000000000000, 0.9238795325112867385, 1.000000000000000000, 0.9238795325112867385, 1.000000000000000000, 0.9238795325112867385, 1.000000000000000000, 0.9341965377642874602, 0.9821626249036858880 ) ) 
 REPRESENTATION_ITEM ( '' )  );
#30997=VECTOR ( 'NONE', #32684, 1000.000000000000000 ) ;
#31003=AXIS2_PLACEMENT_3D ( 'NONE', #28694, #31525, #5641 ) ;
#31013=ADVANCED_FACE ( 'NONE', ( #27221 ), #9342, .T. ) ;
#31014=VECTOR ( 'NONE', #30407, 1000.000000000000000 ) ;
#31020=CARTESIAN_POINT ( 'NONE',  ( 25.32128608521642832, -1.774145575271474540, 1.889914159312680919 ) ) ;
#31023=VERTEX_POINT ( 'NONE', #11853 ) ;
#31026=ORIENTED_EDGE ( 'NONE', *, *, #1343, .F. ) ;
#31027=DIRECTION ( 'NONE',  ( -1.000000000000000000, 8.574039729943019576E-17, 0.000000000000000000 ) ) ;
#31034=CARTESIAN_POINT ( 'NONE',  ( 10.56183597391177464, -0.2499999999999476807, -5.003758587302151284 ) ) ;
#31047=ORIENTED_EDGE ( 'NONE', *, *, #4582, .T. ) ;
#31048=AXIS2_PLACEMENT_3D ( 'NONE', #21, #5553, #10205 ) ;
#31055=CARTESIAN_POINT ( 'NONE',  ( 10.00000000000000000, 4.467071865485493731, -1.625881193364653088 ) ) ;
#31058=EDGE_LOOP ( 'NONE', ( #1307, #15416, #7099, #27237 ) ) ;
#31066=VECTOR ( 'NONE', #13512, 1000.000000000000114 ) ;
#31079=DIRECTION ( 'NONE',  ( 1.000000000000000000, -8.574039729943018344E-17, -0.000000000000000000 ) ) ;
#31081=ORIENTED_EDGE ( 'NONE', *, *, #19838, .T. ) ;
#31086=CARTESIAN_POINT ( 'NONE',  ( 21.36000000136559507, -1.570731468192933633, -2.892927487894330074 ) ) ;
#31092=DIRECTION ( 'NONE',  ( 1.000000000000000000, -8.574039729943018344E-17, -0.000000000000000000 ) ) ;
#31095=EDGE_LOOP ( 'NONE', ( #5053, #24928, #9064, #9614 ) ) ;
#31099=AXIS2_PLACEMENT_3D ( 'NONE', #31480, #8562, #19603 ) ;
#31100=CARTESIAN_POINT ( 'NONE',  ( 10.52034268205830259, -3.641590349731909537, -3.055657119358837992 ) ) ;
#31107=LINE ( 'NONE', #20581, #30074 ) ;
#31116=DIRECTION ( 'NONE',  ( 1.000000000000000000, -8.574039729943018344E-17, -0.000000000000000000 ) ) ;
#31149=CARTESIAN_POINT ( 'NONE',  ( 24.61000000273118715, -1.573300977624594976, 1.942864903642425700 ) ) ;
#31151=EDGE_CURVE ( 'NONE', #27630, #9752, #16413, .T. ) ;
#31154=VECTOR ( 'NONE', #12198, 1000.000000000000000 ) ;
#31159=LINE ( 'NONE', #6057, #21475 ) ;
#31160=DIRECTION ( 'NONE',  ( -1.000000000000000000, 8.574039729943018344E-17, -3.081487911019577365E-33 ) ) ;
#31161=DIRECTION ( 'NONE',  ( 8.574039729943018344E-17, 1.000000000000000000, 0.000000000000000000 ) ) ;
#31165=VERTEX_POINT ( 'NONE', #20378 ) ;
#31168=ORIENTED_EDGE ( 'NONE', *, *, #28687, .F. ) ;
#31173=ORIENTED_EDGE ( 'NONE', *, *, #20385, .T. ) ;
#31181=ORIENTED_EDGE ( 'NONE', *, *, #13228, .T. ) ;
#31196=VERTEX_POINT ( 'NONE', #159 ) ;
#31199=CIRCLE ( 'NONE', #17286, 5.000000000000002665 ) ;
#31201=DIRECTION ( 'NONE',  ( 1.000000000000000000, -0.000000000000000000, -0.000000000000000000 ) ) ;
#31203=CARTESIAN_POINT ( 'NONE',  ( 24.61000000136559862, 2.892927487894327410, -1.570731468192931635 ) ) ;
#31210=ORIENTED_EDGE ( 'NONE', *, *, #14754, .F. ) ;
#31216=CARTESIAN_POINT ( 'NONE',  ( 24.73500000136559507, 1.570731468192929858, 2.892927487894329630 ) ) ;
#31219=AXIS2_PLACEMENT_3D ( 'NONE', #24826, #19651, #20151 ) ;
#31224=CARTESIAN_POINT ( 'NONE',  ( 10.00000000000000000, -3.672404558090063276, 3.407865132560168320 ) ) ;
#31235=CARTESIAN_POINT ( 'NONE',  ( 22.50111451137534502, -3.256483526998273983E-15, 2.499999999999998668 ) ) ;
#31239=ORIENTED_EDGE ( 'NONE', *, *, #4463, .T. ) ;
#31241=VECTOR ( 'NONE', #32452, 1000.000000000000000 ) ;
#31258=CARTESIAN_POINT ( 'NONE',  ( 21.98500000136559507, -0.9349337715887248157, 3.156283516753367824 ) ) ;
#31283=EDGE_CURVE ( 'NONE', #6630, #3234, #2770, .T. ) ;
#31291=DIRECTION ( 'NONE',  ( 1.000000000000000000, -8.574039729943018344E-17, -0.000000000000000000 ) ) ;
#31295=LINE ( 'NONE', #13541, #26800 ) ;
#31301=CARTESIAN_POINT ( 'NONE',  ( 22.36000000136559152, 0.9349337715887185984, -3.156283516753368268 ) ) ;
#31307=CARTESIAN_POINT ( 'NONE',  ( 21.48500000136559507, 2.892927487894327410, -1.570731468192931635 ) ) ;
#31312=ADVANCED_FACE ( 'NONE', ( #1576 ), #11763, .F. ) ;
#31324=DIRECTION ( 'NONE',  ( -1.000000000000000000, 8.574039729943018344E-17, -0.000000000000000000 ) ) ;
#31331=ORIENTED_EDGE ( 'NONE', *, *, #20380, .F. ) ;
#31332=ORIENTED_EDGE ( 'NONE', *, *, #27056, .F. ) ;
#31335=DIRECTION ( 'NONE',  ( 6.062761635205522753E-17, 0.7071067811865410224, 0.7071067811865540120 ) ) ;
#31341=ADVANCED_FACE ( 'NONE', ( #16948 ), #20866, .T. ) ;
#31350=CARTESIAN_POINT ( 'NONE',  ( 22.42250000136559507, -0.3178988483021076838, -3.024605502323848949 ) ) ;
#31351=CARTESIAN_POINT ( 'NONE',  ( 25.55608012950906982, -0.1743803405538818241, -2.821080129508247936 ) ) ;
#31352=CARTESIAN_POINT ( 'NONE',  ( 17.75999999999999801, -1.902510934646483477E-15, 2.499999999999996891 ) ) ;
#31356=ORIENTED_EDGE ( 'NONE', *, *, #25009, .F. ) ;
#31363=CARTESIAN_POINT ( 'NONE',  ( 24.36000000136559507, 0.9349337715887185984, -3.156283516753368268 ) ) ;
#31369=CARTESIAN_POINT ( 'NONE',  ( -7.077711312404032898E-17, -0.8254815157534933778, -4.681538312723525053 ) ) ;
#31374=CARTESIAN_POINT ( 'NONE',  ( 10.00000000000000178, -2.718385644597206330, 4.208382051008184632 ) ) ;
#31397=DIRECTION ( 'NONE',  ( 0.000000000000000000, -0.7071067811865465735, -0.7071067811865484609 ) ) ;
#31401=DIRECTION ( 'NONE',  ( -1.000000000000000000, 8.574039729943018344E-17, -0.000000000000000000 ) ) ;
#31403=ADVANCED_FACE ( 'NONE', ( #14615 ), #32859, .T. ) ;
#31405=ORIENTED_EDGE ( 'NONE', *, *, #23840, .F. ) ;
#31424=VERTEX_POINT ( 'NONE', #27648 ) ;
#31426=ORIENTED_EDGE ( 'NONE', *, *, #3260, .T. ) ;
#31429=DIRECTION ( 'NONE',  ( 1.000000000000000000, -8.574039729943018344E-17, -0.000000000000000000 ) ) ;
#31434=ORIENTED_EDGE ( 'NONE', *, *, #25300, .T. ) ;
#31446=ADVANCED_FACE ( 'NONE', ( #14771 ), #17105, .F. ) ;
#31447=DIRECTION ( 'NONE',  ( 6.062761635205574522E-17, 0.7071067811865465735, -0.7071067811865484609 ) ) ;
#31451=CARTESIAN_POINT ( 'NONE',  ( 21.73500000273118715, -2.486304738420683780, 0.2613211581691335383 ) ) ;
#31453=CARTESIAN_POINT ( 'NONE',  ( 10.00000000000000000, 3.641590349731929077, 3.055657119358814011 ) ) ;
#31462=DIRECTION ( 'NONE',  ( 1.000000000000000000, -8.574039729943018344E-17, -0.000000000000000000 ) ) ;
#31480=CARTESIAN_POINT ( 'NONE',  ( 10.00000000000000178, -8.574039729943018837E-16, 0.000000000000000000 ) ) ;
#31499=CARTESIAN_POINT ( 'NONE',  ( 25.42165046702202602, -2.650206603605265610, -0.4742644350702509004 ) ) ;
#31503=VERTEX_POINT ( 'NONE', #10583 ) ;
#31511=CARTESIAN_POINT ( 'NONE',  ( 20.50111451137534857, -3.256483526998273983E-15, 2.499999999999998668 ) ) ;
#31515=AXIS2_PLACEMENT_3D ( 'NONE', #3286, #10970, #13455 ) ;
#31525=DIRECTION ( 'NONE',  ( -2.219124775575043125E-17, -0.2588190451025343397, 0.9659258262890646485 ) ) ;
#31530=AXIS2_PLACEMENT_3D ( 'NONE', #1016, #23582, #8377 ) ;
#31533=CARTESIAN_POINT ( 'NONE',  ( 22.86000000273118715, -1.942864903642428587, -1.573300977624592756 ) ) ;
#31554=VECTOR ( 'NONE', #16343, 1000.000000000000114 ) ;
#31556=PLANE ( 'NONE',  #21895 ) ;
#31562=CARTESIAN_POINT ( 'NONE',  ( 4.285194126261599773E-30, 4.979297819079224069E-14, -4.753758587302147731 ) ) ;
#31569=LINE ( 'NONE', #23719, #31554 ) ;
#31574=CARTESIAN_POINT ( 'NONE',  ( 10.00000000000000000, 4.616489984850557171, -1.946309384392544528 ) ) ;
#31591=VECTOR ( 'NONE', #22653, 1000.000000000000000 ) ;
#31605=CARTESIAN_POINT ( 'NONE',  ( 26.23500000000000298, 0.2613211581691317065, 2.486304738420681559 ) ) ;
#31614=CARTESIAN_POINT ( 'NONE',  ( 22.23500000136559862, -1.570731468192933633, -2.892927487894330074 ) ) ;
#31621=CARTESIAN_POINT ( 'NONE',  ( 22.92250000273118715, -1.291182301015472378, -2.378061970571982098 ) ) ;
#31629=VECTOR ( 'NONE', #2720, 1000.000000000000114 ) ;
#31637=VECTOR ( 'NONE', #20110, 999.9999999999998863 ) ;
#31644=VERTEX_POINT ( 'NONE', #14228 ) ;
#31651=ORIENTED_EDGE ( 'NONE', *, *, #21227, .T. ) ;
#31652=DIRECTION ( 'NONE',  ( 0.000000000000000000, 1.000000000000000000, 0.000000000000000000 ) ) ;
#31657=VECTOR ( 'NONE', #7160, 1000.000000000000000 ) ;
#31665=CYLINDRICAL_SURFACE ( 'NONE', #26864, 5.010000000000000675 ) ;
#31677=CARTESIAN_POINT ( 'NONE',  ( 10.00000000000000000, -1.625881193364728805, 4.467071865485467086 ) ) ;
#31680=DIRECTION ( 'NONE',  ( 0.000000000000000000, 1.000000000000000000, 0.000000000000000000 ) ) ;
#31690=ORIENTED_EDGE ( 'NONE', *, *, #9034, .F. ) ;
#31691=CIRCLE ( 'NONE', #2883, 5.010000000000000675 ) ;
#31698=CARTESIAN_POINT ( 'NONE',  ( 25.67250000136559507, 2.363507492473148286, 1.913930629741525058 ) ) ;
#31705=CARTESIAN_POINT ( 'NONE',  ( 21.55656763645044904, -0.8852964313267484009, 2.499999999999997780 ) ) ;
#31721=CARTESIAN_POINT ( 'NONE',  ( 23.99290772595112742, -0.1310194482076044442, -2.499999999999998668 ) ) ;
#31726=EDGE_CURVE ( 'NONE', #502, #1423, #6224, .T. ) ;
#31748=CARTESIAN_POINT ( 'NONE',  ( 25.60517990396913390, 1.170994586158331296, -2.631221474790117032 ) ) ;
#31767=LINE ( 'NONE', #5685, #21534 ) ;
#31769=ORIENTED_EDGE ( 'NONE', *, *, #12479, .F. ) ;
#31774=VECTOR ( 'NONE', #24749, 1000.000000000000000 ) ;
#31776=VERTEX_POINT ( 'NONE', #19098 ) ;
#31777=DIRECTION ( 'NONE',  ( 0.000000000000000000, 1.000000000000000000, 0.000000000000000000 ) ) ;
#31778=ORIENTED_EDGE ( 'NONE', *, *, #23916, .T. ) ;
#31782=CARTESIAN_POINT ( 'NONE',  ( 22.54750000000000654, -2.594547506269383685, -0.7685399846772043020 ) ) ;
#31793=CARTESIAN_POINT ( 'NONE',  ( 21.67250000273118715, -2.378061970571983430, 1.291182301015471712 ) ) ;
#31794=EDGE_CURVE ( 'NONE', #15946, #28338, #6372, .T. ) ;
#31796=FACE_OUTER_BOUND ( 'NONE', #11637, .T. ) ;
#31797=EDGE_CURVE ( 'NONE', #10158, #14757, #12389, .T. ) ;
#31800=CARTESIAN_POINT ( 'NONE',  ( 0.000000000000000000, 0.000000000000000000, 0.000000000000000000 ) ) ;
#31802=CARTESIAN_POINT ( 'NONE',  ( -7.077711312404582636E-17, -0.8254815157535566605, 4.681538312723514395 ) ) ;
#31804=DIRECTION ( 'NONE',  ( 1.000000000000000000, -8.574039729943018344E-17, -0.000000000000000000 ) ) ;
#31805=PLANE ( 'NONE',  #11416 ) ;
#31808=ORIENTED_EDGE ( 'NONE', *, *, #17071, .T. ) ;
#31824=DIRECTION ( 'NONE',  ( 0.000000000000000000, 1.000000000000000000, 0.000000000000000000 ) ) ;
#31846=ORIENTED_EDGE ( 'NONE', *, *, #431, .F. ) ;
#31853=EDGE_CURVE ( 'NONE', #32058, #32142, #12715, .T. ) ;
#31871=CARTESIAN_POINT ( 'NONE',  ( 10.55147673363118876, 2.376879293651121383, -4.116875700062057497 ) ) ;
#31873=DIRECTION ( 'NONE',  ( 0.000000000000000000, 1.000000000000000000, 0.000000000000000000 ) ) ;
#31874=CARTESIAN_POINT ( 'NONE',  ( -3.830085165118321606E-16, -4.467071865485483961, 1.625881193364682620 ) ) ;
#31888=ORIENTED_EDGE ( 'NONE', *, *, #10169, .T. ) ;
#31895=PLANE ( 'NONE',  #761 ) ;
#31899=CARTESIAN_POINT ( 'NONE',  ( 2.921917104085851403E-16, 3.407865132560179866, 3.672404558090050397 ) ) ;
#31905=CARTESIAN_POINT ( 'NONE',  ( 10.56183597391177464, 4.753758587302147731, 0.000000000000000000 ) ) ;
#31909=DIRECTION ( 'NONE',  ( 0.000000000000000000, 1.000000000000000000, 0.000000000000000000 ) ) ;
#31912=ORIENTED_EDGE ( 'NONE', *, *, #12412, .F. ) ;
#31915=ORIENTED_EDGE ( 'NONE', *, *, #25836, .T. ) ;
#31921=PLANE ( 'NONE',  #25813 ) ;
#31932=VERTEX_POINT ( 'NONE', #18909 ) ;
#31936=CARTESIAN_POINT ( 'NONE',  ( 21.85999999999999943, 1.573300977624590313, -1.942864903642426144 ) ) ;
#31949=CARTESIAN_POINT ( 'NONE',  ( 22.61000000273118715, -1.573300977624594976, 1.942864903642425700 ) ) ;
#31957=VERTEX_POINT ( 'NONE', #29102 ) ;
#31958=DIRECTION ( 'NONE',  ( 8.541412920197212419E-17, 0.9961946980917449901, 0.08715574274766461904 ) ) ;
#31959=DIRECTION ( 'NONE',  ( 1.000000000000000000, -0.000000000000000000, -0.000000000000000000 ) ) ;
#31965=FACE_OUTER_BOUND ( 'NONE', #12778, .T. ) ;
#31967=ORIENTED_EDGE ( 'NONE', *, *, #18407, .F. ) ;
#31970=EDGE_CURVE ( 'NONE', #17030, #3611, #31295, .T. ) ;
#31972=PLANE ( 'NONE',  #22977 ) ;
#31977=DIRECTION ( 'NONE',  ( 1.000000000000000000, -8.574039729943018344E-17, -0.000000000000000000 ) ) ;
#31991=ORIENTED_EDGE ( 'NONE', *, *, #10526, .T. ) ;
#31996=EDGE_LOOP ( 'NONE', ( #4525, #10700, #2081, #27645 ) ) ;
#32007=DIRECTION ( 'NONE',  ( 4.917867153432920143E-17, 0.5735764363510367225, 0.8191520442889984599 ) ) ;
#32032=VECTOR ( 'NONE', #31324, 1000.000000000000000 ) ;
#32039=ORIENTED_EDGE ( 'NONE', *, *, #1094, .T. ) ;
#32044=EDGE_CURVE ( 'NONE', #23098, #19482, #15351, .T. ) ;
#32057=CARTESIAN_POINT ( 'NONE',  ( 25.67092775740384170, 2.589206504880454229, -1.404329851040918342 ) ) ;
#32058=VERTEX_POINT ( 'NONE', #20721 ) ;
#32065=EDGE_CURVE ( 'NONE', #32100, #3931, #18037, .T. ) ;
#32067=CARTESIAN_POINT ( 'NONE',  ( 25.75999999999999801, -2.208672634433321348E-15, -2.499999999999997780 ) ) ;
#32069=DIRECTION ( 'NONE',  ( -7.770718973608973726E-17, -0.9063077870366497146, 0.4226182617406998854 ) ) ;
#32082=EDGE_CURVE ( 'NONE', #4614, #8864, #16653, .T. ) ;
#32084=AXIS2_PLACEMENT_3D ( 'NONE', #2470, #12485, #32898 ) ;
#32097=CARTESIAN_POINT ( 'NONE',  ( 22.36000000000000298, -1.573300977624594976, 1.942864903642425700 ) ) ;
#32099=DIRECTION ( 'NONE',  ( 8.574039729943018344E-17, 1.000000000000000000, 0.000000000000000000 ) ) ;
#32100=VERTEX_POINT ( 'NONE', #27721 ) ;
#32120=LINE ( 'NONE', #880, #8177 ) ;
#32136=LINE ( 'NONE', #19589, #29968 ) ;
#32142=VERTEX_POINT ( 'NONE', #16739 ) ;
#32149=ORIENTED_EDGE ( 'NONE', *, *, #24714, .F. ) ;
#32150=CARTESIAN_POINT ( 'NONE',  ( 3.958196854299250007E-16, 4.616489984850531414, 1.946309384392607811 ) ) ;
#32157=CARTESIAN_POINT ( 'NONE',  ( 10.00000000000000000, -3.641590349731909537, -3.055657119358837992 ) ) ;
#32170=AXIS2_PLACEMENT_3D ( 'NONE', #32446, #27422, #16878 ) ;
#32171=FACE_OUTER_BOUND ( 'NONE', #27757, .T. ) ;
#32184=DIRECTION ( 'NONE',  ( 0.000000000000000000, 1.000000000000000000, 0.000000000000000000 ) ) ;
#32189=CARTESIAN_POINT ( 'NONE',  ( 20.86000000136559507, -0.9349337715887247047, 3.156283516753367824 ) ) ;
#32193=DIRECTION ( 'NONE',  ( -4.917867153433010739E-17, -0.5735764363510469366, -0.8191520442889912434 ) ) ;
#32195=PLANE ( 'NONE',  #6934 ) ;
#32197=LINE ( 'NONE', #17562, #24688 ) ;
#32211=LINE ( 'NONE', #1777, #7034 ) ;
#32214=AXIS2_PLACEMENT_3D ( 'NONE', #18883, #19038, #20884 ) ;
#32217=ORIENTED_EDGE ( 'NONE', *, *, #32065, .T. ) ;
#32236=FACE_OUTER_BOUND ( 'NONE', #7263, .T. ) ;
#32237=VECTOR ( 'NONE', #2088, 1000.000000000000000 ) ;
#32239=CYLINDRICAL_SURFACE ( 'NONE', #6657, 5.000000000000002665 ) ;
#32246=CIRCLE ( 'NONE', #32797, 5.009999999999999787 ) ;
#32249=CARTESIAN_POINT ( 'NONE',  ( 25.75999999999999801, 2.805042440084548172, 1.132414195126726364 ) ) ;
#32268=CIRCLE ( 'NONE', #6610, 5.010000000000000675 ) ;
#32269=CARTESIAN_POINT ( 'NONE',  ( 17.75999999999999801, -2.208672634433321348E-15, -2.499999999999996891 ) ) ;
#32276=VERTEX_POINT ( 'NONE', #11891 ) ;
#32285=CARTESIAN_POINT ( 'NONE',  ( 24.73499999999999943, -0.2613211581691358698, -2.486304738420681559 ) ) ;
#32287=CARTESIAN_POINT ( 'NONE',  ( 25.54750000000000298, -2.594547506269383685, -0.7685399846772043020 ) ) ;
#32304=CARTESIAN_POINT ( 'NONE',  ( 24.67250000136559507, 3.024605502323846729, -0.3178988483021056854 ) ) ;
#32310=ORIENTED_EDGE ( 'NONE', *, *, #19958, .T. ) ;
#32315=( NAMED_UNIT ( * ) PLANE_ANGLE_UNIT ( ) SI_UNIT ( $, .RADIAN. ) );
#32329=CARTESIAN_POINT ( 'NONE',  ( 25.75999999999999801, 2.769709385801040646, 1.244424427642012221 ) ) ;
#32332=CARTESIAN_POINT ( 'NONE',  ( 22.54750000000000654, -2.594547506269383685, -0.7685399846772043020 ) ) ;
#32334=DIRECTION ( 'NONE',  ( 1.000000000000000000, -8.574039729943018344E-17, -0.000000000000000000 ) ) ;
#32336=VERTEX_POINT ( 'NONE', #2531 ) ;
#32338=DIRECTION ( 'NONE',  ( -1.000000000000000000, 8.574039729943022041E-17, 6.162975822039154730E-33 ) ) ;
#32346=CARTESIAN_POINT ( 'NONE',  ( 10.00000000000000000, -3.641590349731909537, -3.055657119358837992 ) ) ;
#32353=EDGE_CURVE ( 'NONE', #19944, #20824, #23579, .T. ) ;
#32359=ORIENTED_EDGE ( 'NONE', *, *, #30794, .F. ) ;
#32360=CARTESIAN_POINT ( 'NONE',  ( 22.67250000136559507, 2.363507492473148286, 1.913930629741525058 ) ) ;
#32366=VERTEX_POINT ( 'NONE', #22753 ) ;
#32370=CARTESIAN_POINT ( 'NONE',  ( 23.36000000136559507, 0.9349337715887185984, -3.156283516753368268 ) ) ;
#32375=LINE ( 'NONE', #7416, #22506 ) ;
#32378=CARTESIAN_POINT ( 'NONE',  ( 3.608283490412365891E-16, 4.208382051008230818, -2.718385644597129502 ) ) ;
#32385=DIRECTION ( 'NONE',  ( -7.472768010112085392E-18, -0.08715574274766894891, 0.9961946980917446570 ) ) ;
#32405=CARTESIAN_POINT ( 'NONE',  ( -4.290242492657217039E-16, -5.003758587302148619, -0.2500000000000008882 ) ) ;
#32406=ORIENTED_EDGE ( 'NONE', *, *, #4395, .T. ) ;
#32412=DIRECTION ( 'NONE',  ( 7.770718973609021797E-17, 0.9063077870366551547, -0.4226182617406882280 ) ) ;
#32413=DIRECTION ( 'NONE',  ( 6.062761635205589313E-17, 0.7071067811865484609, -0.7071067811865465735 ) ) ;
#32414=DIRECTION ( 'NONE',  ( 7.770718973608935516E-17, 0.9063077870366456068, 0.4226182617407089337 ) ) ;
#32415=DIRECTION ( 'NONE',  ( 1.000000000000000000, -8.574039729943018344E-17, -0.000000000000000000 ) ) ;
#32417=CARTESIAN_POINT ( 'NONE',  ( 10.00000000000000000, 4.467071865485470639, 1.625881193364712596 ) ) ;
#32432=DIRECTION ( 'NONE',  ( 1.000000000000000000, -8.574039729943018344E-17, -0.000000000000000000 ) ) ;
#32433=CARTESIAN_POINT ( 'NONE',  ( 10.52034268205830614, 3.055657119358800244, 3.641590349731939735 ) ) ;
#32438=CARTESIAN_POINT ( 'NONE',  ( 25.23499999999999943, 0.2613211581691317065, 2.486304738420681559 ) ) ;
#32444=CARTESIAN_POINT ( 'NONE',  ( 10.00000000000000178, 4.616489984850531414, 1.946309384392610031 ) ) ;
#32446=CARTESIAN_POINT ( 'NONE',  ( 10.00000000000000178, -8.574039729943018837E-16, 0.000000000000000000 ) ) ;
#32449=EDGE_LOOP ( 'NONE', ( #31769, #21175, #30451, #15459 ) ) ;
#32452=DIRECTION ( 'NONE',  ( -1.000000000000000000, 8.574039729943017111E-17, -0.000000000000000000 ) ) ;
#32463=ORIENTED_EDGE ( 'NONE', *, *, #24039, .F. ) ;
#32468=VERTEX_POINT ( 'NONE', #3527 ) ;
#32469=CARTESIAN_POINT ( 'NONE',  ( -4.290242492657217039E-16, -5.003758587302148619, 0.2499999999999991951 ) ) ;
#32470=VERTEX_POINT ( 'NONE', #3035 ) ;
#32481=DIRECTION ( 'NONE',  ( 1.000000000000000000, -8.574039729943018344E-17, -0.000000000000000000 ) ) ;
#32482=CARTESIAN_POINT ( 'NONE',  ( 10.55147673363119232, -4.116875700062100130, 2.376879293651050329 ) ) ;
#32490=CARTESIAN_POINT ( 'NONE',  ( 24.17250000136559507, -2.363507492473152283, -1.913930629741525280 ) ) ;
#32506=ORIENTED_EDGE ( 'NONE', *, *, #4870, .F. ) ;
#32507=ORIENTED_EDGE ( 'NONE', *, *, #6263, .T. ) ;
#32508=LINE ( 'NONE', #16941, #6521 ) ;
#32512=CARTESIAN_POINT ( 'NONE',  ( 22.42250000136559507, 1.913930629741522838, -2.363507492473150062 ) ) ;
#32519=LINE ( 'NONE', #22659, #11712 ) ;
#32520=CARTESIAN_POINT ( 'NONE',  ( 4.013969549054183686E-16, 4.681538312723517059, 0.8254815157535410064 ) ) ;
#32521=CARTESIAN_POINT ( 'NONE',  ( 25.17250000136559507, -2.363507492473152283, -1.913930629741525280 ) ) ;
#32530=CARTESIAN_POINT ( 'NONE',  ( 10.00000000000000178, -0.2500000000000201505, 5.003758587302149508 ) ) ;
#32549=VECTOR ( 'NONE', #29645, 1000.000000000000000 ) ;
#32568=CARTESIAN_POINT ( 'NONE',  ( 24.17250000273118715, 2.378061970571979433, -1.291182301015470602 ) ) ;
#32579=PLANE ( 'NONE',  #8202 ) ;
#32583=ADVANCED_FACE ( 'NONE', ( #6822 ), #8842, .F. ) ;
#32584=VERTEX_POINT ( 'NONE', #4325 ) ;
#32585=ADVANCED_FACE ( 'NONE', ( #1842 ), #16693, .T. ) ;
#32589=LINE ( 'NONE', #22726, #31014 ) ;
#32592=LINE ( 'NONE', #9664, #4913 ) ;
#32594=DIRECTION ( 'NONE',  ( 0.000000000000000000, 0.000000000000000000, -1.000000000000000000 ) ) ;
#32596=CARTESIAN_POINT ( 'NONE',  ( 21.48499999999999943, -2.486304738420683780, 0.2613211581691335383 ) ) ;
#32602=LINE ( 'NONE', #6340, #19254 ) ;
#32604=CARTESIAN_POINT ( 'NONE',  ( 22.04750000000000298, 2.594547506269380133, 0.7685399846772031918 ) ) ;
#32611=CARTESIAN_POINT ( 'NONE',  ( 25.54750000136559507, 1.913930629741522838, -2.363507492473150062 ) ) ;
#32617=VECTOR ( 'NONE', #12716, 1000.000000000000000 ) ;
#32622=ORIENTED_EDGE ( 'NONE', *, *, #6160, .T. ) ;
#32641=AXIS2_PLACEMENT_3D ( 'NONE', #18189, #15008, #2350 ) ;
#32647=DIRECTION ( 'NONE',  ( 0.000000000000000000, 1.000000000000000000, 0.000000000000000000 ) ) ;
#32651=CARTESIAN_POINT ( 'NONE',  ( 24.98500000136559507, -2.892927487894331406, 1.570731468192932301 ) ) ;
#32663=AXIS2_PLACEMENT_3D ( 'NONE', #9904, #8048, #25604 ) ;
#32670=CARTESIAN_POINT ( 'NONE',  ( 10.56183597391177464, 4.888740217817763464E-14, -4.753758587302147731 ) ) ;
#32673=CIRCLE ( 'NONE', #8100, 2.499999999999996891 ) ;
#32675=ORIENTED_EDGE ( 'NONE', *, *, #7960, .F. ) ;
#32678=VERTEX_POINT ( 'NONE', #27399 ) ;
#32680=CARTESIAN_POINT ( 'NONE',  ( 22.11000000136559507, -3.156283516753370488, -0.9349337715887220401 ) ) ;
#32682=VERTEX_POINT ( 'NONE', #19386 ) ;
#32684=DIRECTION ( 'NONE',  ( -1.000000000000000000, 8.574039729943019576E-17, -6.162975822039154730E-33 ) ) ;
#32687=VECTOR ( 'NONE', #8941, 999.9999999999998863 ) ;
#32689=CARTESIAN_POINT ( 'NONE',  ( 24.54750000136559507, 3.024605502323846729, -0.3178988483021056854 ) ) ;
#32697=AXIS2_PLACEMENT_3D ( 'NONE', #30043, #12289, #15143 ) ;
#32710=LINE ( 'NONE', #10102, #9812 ) ;
#32711=CARTESIAN_POINT ( 'NONE',  ( 10.00000000000000178, 4.884328206559836794, 1.115095498423327225 ) ) ;
#32713=EDGE_LOOP ( 'NONE', ( #16252, #10452, #10710, #21965 ) ) ;
#32718=ORIENTED_EDGE ( 'NONE', *, *, #14515, .T. ) ;
#32724=DIRECTION ( 'NONE',  ( -8.281886410780478979E-17, -0.9659258262890646485, -0.2588190451025343397 ) ) ;
#32734=DIRECTION ( 'NONE',  ( -1.000000000000000000, 8.574039729943015878E-17, 1.232595164407830946E-32 ) ) ;
#32737=DIRECTION ( 'NONE',  ( -1.000000000000000000, 8.574039729943019576E-17, 0.000000000000000000 ) ) ;
#32743=PLANE ( 'NONE',  #3797 ) ;
#32744=CARTESIAN_POINT ( 'NONE',  ( 20.74999999999999645, -1.779113243963175696E-15, 0.000000000000000000 ) ) ;
#32745=DIRECTION ( 'NONE',  ( 1.000000000000000000, -8.574039729943018344E-17, -0.000000000000000000 ) ) ;
#32750=CARTESIAN_POINT ( 'NONE',  ( 10.56183597391177464, -4.753758587302148619, 0.000000000000000000 ) ) ;
#32753=EDGE_LOOP ( 'NONE', ( #12976, #28925, #21885, #25563 ) ) ;
#32756=VERTEX_POINT ( 'NONE', #15492 ) ;
#32778=CARTESIAN_POINT ( 'NONE',  ( 22.92250000136559862, 0.3178988483021036315, 3.024605502323848949 ) ) ;
#32781=VERTEX_POINT ( 'NONE', #150 ) ;
#32797=AXIS2_PLACEMENT_3D ( 'NONE', #12908, #28286, #31161 ) ;
#32801=CARTESIAN_POINT ( 'NONE',  ( 24.85999999999999943, 1.573300977624590313, -1.942864903642426144 ) ) ;
#32806=ORIENTED_EDGE ( 'NONE', *, *, #27284, .F. ) ;
#32810=ORIENTED_EDGE ( 'NONE', *, *, #4395, .F. ) ;
#32816=VERTEX_POINT ( 'NONE', #30091 ) ;
#32818=CARTESIAN_POINT ( 'NONE',  ( 23.61000000000000298, -1.942864903642428587, -1.573300977624592756 ) ) ;
#32821=VERTEX_POINT ( 'NONE', #5000 ) ;
#32823=DIRECTION ( 'NONE',  ( 0.000000000000000000, 0.9063077870366493816, 0.4226182617407006070 ) ) ;
#32832=PLANE ( 'NONE',  #32663 ) ;
#32833=CARTESIAN_POINT ( 'NONE',  ( 25.23500000136559507, -1.570731468192933633, -2.892927487894330074 ) ) ;
#32842=VERTEX_POINT ( 'NONE', #14991 ) ;
#32843=B_SPLINE_CURVE_WITH_KNOTS ( 'NONE', 3,
 ( #7633, #15652, #25862, #8120 ),
 .UNSPECIFIED., .F., .F.,
 ( 4, 4 ),
 ( 0.0005429330443435420768, 0.0007203473150553858393 ),
 .UNSPECIFIED. ) ;
#32859=CYLINDRICAL_SURFACE ( 'NONE', #5434, 5.010000000000000675 ) ;
#32875=EDGE_CURVE ( 'NONE', #1268, #16254, #7666, .T. ) ;
#32880=DIRECTION ( 'NONE',  ( 3.623545766764247286E-17, 0.4226182617407038267, -0.9063077870366479383 ) ) ;
#32887=VERTEX_POINT ( 'NONE', #5803 ) ;
#32898=DIRECTION ( 'NONE',  ( 0.000000000000000000, 1.000000000000000000, 0.000000000000000000 ) ) ;
#32899=DIRECTION ( 'NONE',  ( 1.000000000000000000, -8.574039729943018344E-17, -0.000000000000000000 ) ) ;
#32900=EDGE_CURVE ( 'NONE', #4647, #24556, #908, .T. ) ;
#32906=CARTESIAN_POINT ( 'NONE',  ( 3.822634483660936850E-16, 4.458382051008224600, -2.285372942704906762 ) ) ;
#32918=CARTESIAN_POINT ( 'NONE',  ( 21.86000000136559507, 1.570731468192929858, 2.892927487894329186 ) ) ;
#32937=CARTESIAN_POINT ( 'NONE',  ( 25.42250000136559507, -0.3178988483021076838, -3.024605502323848949 ) ) ;
#32951=CARTESIAN_POINT ( 'NONE',  ( 22.79750000136559862, 2.363507492473148286, 1.913930629741525058 ) ) ;
#32957=DIRECTION ( 'NONE',  ( -8.541412920197218582E-17, -0.9961946980917459893, 0.08715574274765194862 ) ) ;
#32958=CARTESIAN_POINT ( 'NONE',  ( 3.529825581556927552E-16, 4.116875700062083254, 2.376879293651078751 ) ) ;
#32976=CARTESIAN_POINT ( 'NONE',  ( -2.147796952350726040E-16, 1.841529640130565566E-32, 0.000000000000000000 ) ) ;
#32979=CARTESIAN_POINT ( 'NONE',  ( 25.75999999999999801, -6.000000000000002665, 7.347880794884119736E-16 ) ) ;
#32984=DIRECTION ( 'NONE',  ( 4.917867153432934934E-17, 0.5735764363510388320, 0.8191520442889969056 ) ) ;
#32985=CARTESIAN_POINT ( 'NONE',  ( 10.00000000000000178, 5.999999999999998224, 0.000000000000000000 ) ) ;
#32986=CARTESIAN_POINT ( 'NONE',  ( 25.48500000136559862, 2.892927487894327410, -1.570731468192931635 ) ) ;
#33008=ORIENTED_EDGE ( 'NONE', *, *, #27007, .F. ) ;
#33009=DIRECTION ( 'NONE',  ( 0.000000000000000000, 1.000000000000000000, 0.000000000000000000 ) ) ;
#33016=DIRECTION ( 'NONE',  ( 8.541412920197229675E-17, 0.9961946980917466554, -0.08715574274764535667 ) ) ;
#33039=CARTESIAN_POINT ( 'NONE',  ( 10.00000000000000000, -4.116875700062067267, -2.376879293651108060 ) ) ;
#33054=DIRECTION ( 'NONE',  ( -1.000000000000000000, 8.574039729943018344E-17, -0.000000000000000000 ) ) ;
#33057=CARTESIAN_POINT ( 'NONE',  ( 24.23500000273118715, 2.486304738420679783, -0.2613211581691337604 ) ) ;
#33062=ORIENTED_EDGE ( 'NONE', *, *, #1917, .T. ) ;
#33064=CARTESIAN_POINT ( 'NONE',  ( 24.04750000136559507, -1.913930629741527500, 2.363507492473149618 ) ) ;
#33084=CARTESIAN_POINT ( 'NONE',  ( 23.29750000136559862, -2.363507492473152283, -1.913930629741525280 ) ) ;
#33134=COLOUR_RGB('Light Gray', 0.08235294, 0.09019608, 0.10196078);
#33135=FILL_AREA_STYLE_COLOUR('',#33134);
#33136=FILL_AREA_STYLE('',(#33135));
#33137=SURFACE_STYLE_FILL_AREA(#33136);
#33138=SURFACE_SIDE_STYLE('',(#33137));
#33139=SURFACE_STYLE_USAGE(.BOTH.,#33138);
#33140=PRESENTATION_STYLE_ASSIGNMENT((#33139));
#33154=STYLED_ITEM('',(#33140),#21237);
#33155=MECHANICAL_DESIGN_GEOMETRIC_PRESENTATION_REPRESENTATION('',(#33154),#13509);
ENDSEC;
END-ISO-10303-21;
